ISO-10303-21;
HEADER;
/* Generated by software containing ST-Developer
 * from STEP Tools, Inc. (www.steptools.com) 
 */

FILE_DESCRIPTION(
/* description */ (''),
/* implementation_level */ '2;1');

FILE_NAME(
/* name */ 'Flanged Screw M3x16.step',
/* time_stamp */ '2026-10-28T16:47:13+01:00',
/* author */ (''),
/* organization */ (''),
/* preprocessor_version */ 'ST-DEVELOPER v20.2',
/* originating_system */ 'Autodesk Translation Framework v15.17.0.0',
/* authorisation */ '');

FILE_SCHEMA (('AUTOMOTIVE_DESIGN { 1 0 10303 214 3 1 1 }'));
ENDSEC;

DATA;
#10=MECHANICAL_DESIGN_GEOMETRIC_PRESENTATION_REPRESENTATION('',(#4587),#459242);
#142=SPHERICAL_SURFACE('',#99121,3.10691712599126);
#2307=(
BOUNDED_SURFACE()
B_SPLINE_SURFACE(1,2,((#362051,#362052,#362053,#362054,#362055,#362056,
#362057,#362058,#362059,#362060,#362061,#362062,#362063,#362064,#362065,
#362066,#362067,#362068,#362069,#362070,#362071,#362072,#362073,#362074,
#362075,#362076,#362077,#362078,#362079,#362080,#362081,#362082,#362083,
#362084,#362085,#362086,#362087,#362088,#362089,#362090,#362091,#362092,
#362093,#362094,#362095,#362096,#362097,#362098,#362099,#362100,#362101,
#362102,#362103,#362104,#362105,#362106,#362107,#362108,#362109,#362110,
#362111,#362112,#362113,#362114,#362115,#362116,#362117,#362118,#362119,
#362120,#362121,#362122,#362123,#362124,#362125,#362126,#362127,#362128,
#362129,#362130,#362131,#362132,#362133,#362134,#362135,#362136,#362137,
#362138,#362139,#362140,#362141,#362142,#362143,#362144,#362145,#362146,
#362147,#362148,#362149,#362150,#362151,#362152,#362153,#362154,#362155,
#362156,#362157,#362158,#362159,#362160,#362161,#362162,#362163,#362164,
#362165,#362166,#362167,#362168,#362169,#362170,#362171,#362172,#362173,
#362174,#362175,#362176,#362177,#362178,#362179,#362180,#362181,#362182,
#362183,#362184,#362185,#362186,#362187,#362188,#362189,#362190,#362191,
#362192,#362193,#362194,#362195,#362196,#362197,#362198,#362199,#362200,
#362201,#362202,#362203,#362204,#362205,#362206,#362207,#362208,#362209,
#362210,#362211,#362212,#362213,#362214,#362215,#362216,#362217,#362218,
#362219,#362220,#362221,#362222,#362223,#362224,#362225,#362226,#362227,
#362228,#362229,#362230,#362231,#362232,#362233,#362234,#362235,#362236,
#362237,#362238,#362239,#362240,#362241,#362242,#362243,#362244,#362245,
#362246,#362247,#362248,#362249,#362250,#362251,#362252,#362253,#362254,
#362255,#362256,#362257,#362258,#362259,#362260,#362261,#362262,#362263,
#362264,#362265,#362266,#362267,#362268,#362269,#362270,#362271,#362272,
#362273,#362274,#362275,#362276,#362277,#362278,#362279,#362280,#362281,
#362282,#362283,#362284,#362285,#362286,#362287,#362288,#362289,#362290,
#362291,#362292,#362293,#362294,#362295,#362296,#362297,#362298,#362299,
#362300,#362301,#362302,#362303,#362304,#362305,#362306,#362307,#362308,
#362309,#362310,#362311,#362312,#362313,#362314,#362315,#362316,#362317,
#362318,#362319,#362320,#362321,#362322,#362323,#362324,#362325,#362326,
#362327,#362328,#362329,#362330,#362331,#362332,#362333,#362334,#362335,
#362336,#362337,#362338,#362339,#362340,#362341,#362342,#362343,#362344,
#362345,#362346,#362347,#362348,#362349,#362350,#362351,#362352,#362353,
#362354,#362355,#362356,#362357,#362358,#362359,#362360,#362361,#362362,
#362363,#362364,#362365,#362366,#362367,#362368,#362369,#362370,#362371,
#362372,#362373,#362374,#362375,#362376,#362377,#362378,#362379,#362380,
#362381,#362382,#362383,#362384,#362385,#362386,#362387,#362388,#362389,
#362390,#362391,#362392,#362393,#362394,#362395,#362396,#362397,#362398,
#362399,#362400,#362401,#362402,#362403,#362404,#362405,#362406,#362407,
#362408,#362409,#362410,#362411,#362412,#362413,#362414,#362415,#362416,
#362417,#362418,#362419,#362420,#362421,#362422,#362423,#362424,#362425,
#362426,#362427,#362428,#362429,#362430,#362431,#362432,#362433,#362434,
#362435,#362436,#362437,#362438,#362439,#362440,#362441,#362442,#362443,
#362444,#362445,#362446,#362447),(#362448,#362449,#362450,#362451,#362452,
#362453,#362454,#362455,#362456,#362457,#362458,#362459,#362460,#362461,
#362462,#362463,#362464,#362465,#362466,#362467,#362468,#362469,#362470,
#362471,#362472,#362473,#362474,#362475,#362476,#362477,#362478,#362479,
#362480,#362481,#362482,#362483,#362484,#362485,#362486,#362487,#362488,
#362489,#362490,#362491,#362492,#362493,#362494,#362495,#362496,#362497,
#362498,#362499,#362500,#362501,#362502,#362503,#362504,#362505,#362506,
#362507,#362508,#362509,#362510,#362511,#362512,#362513,#362514,#362515,
#362516,#362517,#362518,#362519,#362520,#362521,#362522,#362523,#362524,
#362525,#362526,#362527,#362528,#362529,#362530,#362531,#362532,#362533,
#362534,#362535,#362536,#362537,#362538,#362539,#362540,#362541,#362542,
#362543,#362544,#362545,#362546,#362547,#362548,#362549,#362550,#362551,
#362552,#362553,#362554,#362555,#362556,#362557,#362558,#362559,#362560,
#362561,#362562,#362563,#362564,#362565,#362566,#362567,#362568,#362569,
#362570,#362571,#362572,#362573,#362574,#362575,#362576,#362577,#362578,
#362579,#362580,#362581,#362582,#362583,#362584,#362585,#362586,#362587,
#362588,#362589,#362590,#362591,#362592,#362593,#362594,#362595,#362596,
#362597,#362598,#362599,#362600,#362601,#362602,#362603,#362604,#362605,
#362606,#362607,#362608,#362609,#362610,#362611,#362612,#362613,#362614,
#362615,#362616,#362617,#362618,#362619,#362620,#362621,#362622,#362623,
#362624,#362625,#362626,#362627,#362628,#362629,#362630,#362631,#362632,
#362633,#362634,#362635,#362636,#362637,#362638,#362639,#362640,#362641,
#362642,#362643,#362644,#362645,#362646,#362647,#362648,#362649,#362650,
#362651,#362652,#362653,#362654,#362655,#362656,#362657,#362658,#362659,
#362660,#362661,#362662,#362663,#362664,#362665,#362666,#362667,#362668,
#362669,#362670,#362671,#362672,#362673,#362674,#362675,#362676,#362677,
#362678,#362679,#362680,#362681,#362682,#362683,#362684,#362685,#362686,
#362687,#362688,#362689,#362690,#362691,#362692,#362693,#362694,#362695,
#362696,#362697,#362698,#362699,#362700,#362701,#362702,#362703,#362704,
#362705,#362706,#362707,#362708,#362709,#362710,#362711,#362712,#362713,
#362714,#362715,#362716,#362717,#362718,#362719,#362720,#362721,#362722,
#362723,#362724,#362725,#362726,#362727,#362728,#362729,#362730,#362731,
#362732,#362733,#362734,#362735,#362736,#362737,#362738,#362739,#362740,
#362741,#362742,#362743,#362744,#362745,#362746,#362747,#362748,#362749,
#362750,#362751,#362752,#362753,#362754,#362755,#362756,#362757,#362758,
#362759,#362760,#362761,#362762,#362763,#362764,#362765,#362766,#362767,
#362768,#362769,#362770,#362771,#362772,#362773,#362774,#362775,#362776,
#362777,#362778,#362779,#362780,#362781,#362782,#362783,#362784,#362785,
#362786,#362787,#362788,#362789,#362790,#362791,#362792,#362793,#362794,
#362795,#362796,#362797,#362798,#362799,#362800,#362801,#362802,#362803,
#362804,#362805,#362806,#362807,#362808,#362809,#362810,#362811,#362812,
#362813,#362814,#362815,#362816,#362817,#362818,#362819,#362820,#362821,
#362822,#362823,#362824,#362825,#362826,#362827,#362828,#362829,#362830,
#362831,#362832,#362833,#362834,#362835,#362836,#362837,#362838,#362839,
#362840,#362841,#362842,#362843,#362844)),.UNSPECIFIED.,.F.,.F.,.F.)
B_SPLINE_SURFACE_WITH_KNOTS((2,2),(3,2,2,2,2,2,2,2,2,2,2,2,2,2,2,2,2,2,
2,2,2,2,2,2,2,2,2,2,2,2,2,2,2,2,2,2,2,2,2,2,2,2,2,2,2,2,2,2,2,2,2,2,2,2,
2,2,2,2,2,2,2,2,2,2,2,2,2,2,2,2,2,2,2,2,2,2,2,2,2,2,2,2,2,2,2,2,2,2,2,2,
2,2,2,2,2,2,2,2,2,2,2,2,2,2,2,2,2,2,2,2,2,2,2,2,2,2,2,2,2,2,2,2,2,2,2,2,
2,2,2,2,2,2,2,2,2,2,2,2,2,2,2,2,2,2,2,2,2,2,2,2,2,2,2,2,2,2,2,2,2,2,2,2,
2,2,2,2,2,2,2,2,2,2,2,2,2,2,2,2,2,2,2,2,2,2,2,2,2,2,2,2,2,2,2,2,2,2,2,2,
3),(0.,1.),(0.,0.00505050505050505,0.0101010101010101,0.0151515151515152,
0.0202020202020202,0.0252525252525253,0.0303030303030303,0.0353535353535354,
0.0404040404040404,0.0454545454545455,0.0505050505050505,0.0555555555555556,
0.0606060606060606,0.0656565656565657,0.0707070707070707,0.0757575757575758,
0.0808080808080808,0.0858585858585859,0.0909090909090909,0.095959595959596,
0.101010101010101,0.106060606060606,0.111111111111111,0.116161616161616,
0.121212121212121,0.126262626262626,0.131313131313131,0.136363636363636,
0.141414141414141,0.146464646464646,0.151515151515152,0.156565656565657,
0.161616161616162,0.166666666666667,0.171717171717172,0.176767676767677,
0.181818181818182,0.186868686868687,0.191919191919192,0.196969696969697,
0.202020202020202,0.207070707070707,0.212121212121212,0.217171717171717,
0.222222222222222,0.227272727272727,0.232323232323232,0.237373737373737,
0.242424242424242,0.247474747474747,0.252525252525253,0.257575757575758,
0.262626262626263,0.267676767676768,0.272727272727273,0.277777777777778,
0.282828282828283,0.287878787878788,0.292929292929293,0.297979797979798,
0.303030303030303,0.308080808080808,0.313131313131313,0.318181818181818,
0.323232323232323,0.328282828282828,0.333333333333333,0.338383838383838,
0.343434343434343,0.348484848484849,0.353535353535354,0.358585858585859,
0.363636363636364,0.368686868686869,0.373737373737374,0.378787878787879,
0.383838383838384,0.388888888888889,0.393939393939394,0.398989898989899,
0.404040404040404,0.409090909090909,0.414141414141414,0.419191919191919,
0.424242424242424,0.429292929292929,0.434343434343434,0.439393939393939,
0.444444444444444,0.44949494949495,0.454545454545455,0.45959595959596,0.464646464646465,
0.46969696969697,0.474747474747475,0.47979797979798,0.484848484848485,0.48989898989899,
0.494949494949495,0.5,0.505050505050505,0.51010101010101,0.515151515151515,
0.52020202020202,0.525252525252525,0.53030303030303,0.535353535353535,0.54040404040404,
0.545454545454545,0.55050505050505,0.555555555555556,0.560606060606061,
0.565656565656566,0.570707070707071,0.575757575757576,0.580808080808081,
0.585858585858586,0.590909090909091,0.595959595959596,0.601010101010101,
0.606060606060606,0.611111111111111,0.616161616161616,0.621212121212121,
0.626262626262626,0.631313131313131,0.636363636363636,0.641414141414141,
0.646464646464647,0.651515151515151,0.656565656565657,0.661616161616162,
0.666666666666667,0.671717171717172,0.676767676767677,0.681818181818182,
0.686868686868687,0.691919191919192,0.696969696969697,0.702020202020202,
0.707070707070707,0.712121212121212,0.717171717171717,0.722222222222222,
0.727272727272727,0.732323232323232,0.737373737373737,0.742424242424242,
0.747474747474748,0.752525252525252,0.757575757575758,0.762626262626263,
0.767676767676768,0.772727272727273,0.777777777777778,0.782828282828283,
0.787878787878788,0.792929292929293,0.797979797979798,0.803030303030303,
0.808080808080808,0.813131313131313,0.818181818181818,0.823232323232323,
0.828282828282828,0.833333333333333,0.838383838383838,0.843434343434343,
0.848484848484849,0.853535353535353,0.858585858585859,0.863636363636364,
0.868686868686869,0.873737373737374,0.878787878787879,0.883838383838384,
0.888888888888889,0.893939393939394,0.898989898989899,0.904040404040404,
0.909090909090909,0.914141414141414,0.919191919191919,0.924242424242424,
0.929292929292929,0.934343434343434,0.939393939393939,0.944444444444444,
0.94949494949495,0.954545454545455,0.95959595959596,0.964646464646465,0.96969696969697,
0.974747474747475,0.97979797979798,0.984848484848485,0.98989898989899,0.994949494949495,
1.),.UNSPECIFIED.)
GEOMETRIC_REPRESENTATION_ITEM()
RATIONAL_B_SPLINE_SURFACE(((1.,0.866025403784439,1.,0.866025403784439,1.,
0.866025403784439,1.,0.866025403784439,1.,0.866025403784439,1.,0.866025403784439,
1.,0.866025403784439,1.,0.866025403784439,1.,0.866025403784439,1.,0.866025403784439,
1.,0.866025403784439,1.,0.866025403784439,1.,0.866025403784439,1.,0.866025403784439,
1.,0.866025403784439,1.,0.866025403784439,1.,0.866025403784439,1.,0.866025403784439,
1.,0.866025403784439,1.,0.866025403784439,1.,0.866025403784439,1.,0.866025403784439,
1.,0.866025403784439,1.,0.866025403784439,1.,0.866025403784439,1.,0.866025403784439,
1.,0.866025403784439,1.,0.866025403784439,1.,0.866025403784439,1.,0.866025403784439,
1.,0.866025403784439,1.,0.866025403784439,1.,0.866025403784439,1.,0.866025403784439,
1.,0.866025403784439,1.,0.866025403784439,1.,0.866025403784439,1.,0.866025403784439,
1.,0.866025403784439,1.,0.866025403784439,1.,0.866025403784439,1.,0.866025403784439,
1.,0.866025403784439,1.,0.866025403784439,1.,0.866025403784439,1.,0.866025403784439,
1.,0.866025403784439,1.,0.866025403784439,1.,0.866025403784439,1.,0.866025403784439,
1.,0.866025403784439,1.,0.866025403784439,1.,0.866025403784439,1.,0.866025403784439,
1.,0.866025403784439,1.,0.866025403784439,1.,0.866025403784439,1.,0.866025403784439,
1.,0.866025403784439,1.,0.866025403784439,1.,0.866025403784439,1.,0.866025403784439,
1.,0.866025403784439,1.,0.866025403784439,1.,0.866025403784439,1.,0.866025403784439,
1.,0.866025403784439,1.,0.866025403784439,1.,0.866025403784439,1.,0.866025403784439,
1.,0.866025403784439,1.,0.866025403784439,1.,0.866025403784439,1.,0.866025403784439,
1.,0.866025403784439,1.,0.866025403784439,1.,0.866025403784439,1.,0.866025403784439,
1.,0.866025403784439,1.,0.866025403784439,1.,0.866025403784439,1.,0.866025403784439,
1.,0.866025403784439,1.,0.866025403784439,1.,0.866025403784439,1.,0.866025403784439,
1.,0.866025403784439,1.,0.866025403784439,1.,0.866025403784439,1.,0.866025403784439,
1.,0.866025403784439,1.,0.866025403784439,1.,0.866025403784439,1.,0.866025403784439,
1.,0.866025403784439,1.,0.866025403784439,1.,0.866025403784439,1.,0.866025403784439,
1.,0.866025403784439,1.,0.866025403784439,1.,0.866025403784439,1.,0.866025403784439,
1.,0.866025403784439,1.,0.866025403784439,1.,0.866025403784439,1.,0.866025403784439,
1.,0.866025403784439,1.,0.866025403784439,1.,0.866025403784439,1.,0.866025403784439,
1.,0.866025403784439,1.,0.866025403784439,1.,0.866025403784439,1.,0.866025403784439,
1.,0.866025403784439,1.,0.866025403784439,1.,0.866025403784439,1.,0.866025403784439,
1.,0.866025403784439,1.,0.866025403784439,1.,0.866025403784439,1.,0.866025403784439,
1.,0.866025403784439,1.,0.866025403784439,1.,0.866025403784439,1.,0.866025403784439,
1.,0.866025403784439,1.,0.866025403784439,1.,0.866025403784439,1.,0.866025403784439,
1.,0.866025403784439,1.,0.866025403784439,1.,0.866025403784439,1.,0.866025403784439,
1.,0.866025403784439,1.,0.866025403784439,1.,0.866025403784439,1.,0.866025403784439,
1.,0.866025403784439,1.,0.866025403784439,1.,0.866025403784439,1.,0.866025403784439,
1.,0.866025403784439,1.,0.866025403784439,1.,0.866025403784439,1.,0.866025403784439,
1.,0.866025403784439,1.,0.866025403784439,1.,0.866025403784439,1.,0.866025403784439,
1.,0.866025403784439,1.,0.866025403784439,1.,0.866025403784439,1.,0.866025403784439,
1.,0.866025403784439,1.,0.866025403784439,1.,0.866025403784439,1.,0.866025403784439,
1.,0.866025403784439,1.,0.866025403784439,1.,0.866025403784439,1.,0.866025403784439,
1.,0.866025403784439,1.,0.866025403784439,1.,0.866025403784439,1.,0.866025403784439,
1.,0.866025403784439,1.,0.866025403784439,1.,0.866025403784439,1.,0.866025403784439,
1.,0.866025403784439,1.,0.866025403784439,1.,0.866025403784439,1.,0.866025403784439,
1.,0.866025403784439,1.,0.866025403784439,1.,0.866025403784439,1.,0.866025403784439,
1.,0.866025403784439,1.,0.866025403784439,1.,0.866025403784439,1.,0.866025403784439,
1.,0.866025403784439,1.,0.866025403784439,1.,0.866025403784439,1.,0.866025403784439,
1.,0.866025403784439,1.,0.866025403784439,1.,0.866025403784439,1.,0.866025403784439,
1.,0.866025403784439,1.,0.866025403784439,1.,0.866025403784439,1.,0.866025403784439,
1.,0.866025403784439,1.,0.866025403784439,1.,0.866025403784439,1.,0.866025403784439,
1.),(1.,0.866025403784439,1.,0.866025403784439,1.,0.866025403784439,1.,
0.866025403784439,1.,0.866025403784439,1.,0.866025403784439,1.,0.866025403784439,
1.,0.866025403784439,1.,0.866025403784439,1.,0.866025403784439,1.,0.866025403784439,
1.,0.866025403784439,1.,0.866025403784439,1.,0.866025403784439,1.,0.866025403784439,
1.,0.866025403784439,1.,0.866025403784439,1.,0.866025403784439,1.,0.866025403784439,
1.,0.866025403784439,1.,0.866025403784439,1.,0.866025403784439,1.,0.866025403784439,
1.,0.866025403784439,1.,0.866025403784439,1.,0.866025403784439,1.,0.866025403784439,
1.,0.866025403784439,1.,0.866025403784439,1.,0.866025403784439,1.,0.866025403784439,
1.,0.866025403784439,1.,0.866025403784439,1.,0.866025403784439,1.,0.866025403784439,
1.,0.866025403784439,1.,0.866025403784439,1.,0.866025403784439,1.,0.866025403784439,
1.,0.866025403784439,1.,0.866025403784439,1.,0.866025403784439,1.,0.866025403784439,
1.,0.866025403784439,1.,0.866025403784439,1.,0.866025403784439,1.,0.866025403784439,
1.,0.866025403784439,1.,0.866025403784439,1.,0.866025403784439,1.,0.866025403784439,
1.,0.866025403784439,1.,0.866025403784439,1.,0.866025403784439,1.,0.866025403784439,
1.,0.866025403784439,1.,0.866025403784439,1.,0.866025403784439,1.,0.866025403784439,
1.,0.866025403784439,1.,0.866025403784439,1.,0.866025403784439,1.,0.866025403784439,
1.,0.866025403784439,1.,0.866025403784439,1.,0.866025403784439,1.,0.866025403784439,
1.,0.866025403784439,1.,0.866025403784439,1.,0.866025403784439,1.,0.866025403784439,
1.,0.866025403784439,1.,0.866025403784439,1.,0.866025403784439,1.,0.866025403784439,
1.,0.866025403784439,1.,0.866025403784439,1.,0.866025403784439,1.,0.866025403784439,
1.,0.866025403784439,1.,0.866025403784439,1.,0.866025403784439,1.,0.866025403784439,
1.,0.866025403784439,1.,0.866025403784439,1.,0.866025403784439,1.,0.866025403784439,
1.,0.866025403784439,1.,0.866025403784439,1.,0.866025403784439,1.,0.866025403784439,
1.,0.866025403784439,1.,0.866025403784439,1.,0.866025403784439,1.,0.866025403784439,
1.,0.866025403784439,1.,0.866025403784439,1.,0.866025403784439,1.,0.866025403784439,
1.,0.866025403784439,1.,0.866025403784439,1.,0.866025403784439,1.,0.866025403784439,
1.,0.866025403784439,1.,0.866025403784439,1.,0.866025403784439,1.,0.866025403784439,
1.,0.866025403784439,1.,0.866025403784439,1.,0.866025403784439,1.,0.866025403784439,
1.,0.866025403784439,1.,0.866025403784439,1.,0.866025403784439,1.,0.866025403784439,
1.,0.866025403784439,1.,0.866025403784439,1.,0.866025403784439,1.,0.866025403784439,
1.,0.866025403784439,1.,0.866025403784439,1.,0.866025403784439,1.,0.866025403784439,
1.,0.866025403784439,1.,0.866025403784439,1.,0.866025403784439,1.,0.866025403784439,
1.,0.866025403784439,1.,0.866025403784439,1.,0.866025403784439,1.,0.866025403784439,
1.,0.866025403784439,1.,0.866025403784439,1.,0.866025403784439,1.,0.866025403784439,
1.,0.866025403784439,1.,0.866025403784439,1.,0.866025403784439,1.,0.866025403784439,
1.,0.866025403784439,1.,0.866025403784439,1.,0.866025403784439,1.,0.866025403784439,
1.,0.866025403784439,1.,0.866025403784439,1.,0.866025403784439,1.,0.866025403784439,
1.,0.866025403784439,1.,0.866025403784439,1.,0.866025403784439,1.,0.866025403784439,
1.,0.866025403784439,1.,0.866025403784439,1.,0.866025403784439,1.,0.866025403784439,
1.,0.866025403784439,1.,0.866025403784439,1.,0.866025403784439,1.,0.866025403784439,
1.,0.866025403784439,1.,0.866025403784439,1.,0.866025403784439,1.,0.866025403784439,
1.,0.866025403784439,1.,0.866025403784439,1.,0.866025403784439,1.,0.866025403784439,
1.,0.866025403784439,1.,0.866025403784439,1.,0.866025403784439,1.,0.866025403784439,
1.,0.866025403784439,1.,0.866025403784439,1.,0.866025403784439,1.,0.866025403784439,
1.,0.866025403784439,1.,0.866025403784439,1.,0.866025403784439,1.,0.866025403784439,
1.,0.866025403784439,1.,0.866025403784439,1.,0.866025403784439,1.,0.866025403784439,
1.,0.866025403784439,1.,0.866025403784439,1.,0.866025403784439,1.,0.866025403784439,
1.,0.866025403784439,1.,0.866025403784439,1.,0.866025403784439,1.,0.866025403784439,
1.,0.866025403784439,1.,0.866025403784439,1.,0.866025403784439,1.,0.866025403784439,
1.,0.866025403784439,1.,0.866025403784439,1.,0.866025403784439,1.)))
REPRESENTATION_ITEM('')
SURFACE()
);
#2308=(
BOUNDED_SURFACE()
B_SPLINE_SURFACE(1,2,((#362849,#362850,#362851,#362852,#362853,#362854,
#362855,#362856,#362857,#362858,#362859,#362860,#362861,#362862,#362863,
#362864,#362865,#362866,#362867,#362868,#362869,#362870,#362871,#362872,
#362873,#362874,#362875,#362876,#362877,#362878,#362879,#362880,#362881,
#362882,#362883,#362884,#362885,#362886,#362887,#362888,#362889,#362890,
#362891,#362892,#362893,#362894,#362895,#362896,#362897,#362898,#362899,
#362900,#362901,#362902,#362903,#362904,#362905,#362906,#362907,#362908,
#362909,#362910,#362911,#362912,#362913,#362914,#362915,#362916,#362917,
#362918,#362919,#362920,#362921,#362922,#362923,#362924,#362925,#362926,
#362927,#362928,#362929,#362930,#362931,#362932,#362933,#362934,#362935,
#362936,#362937,#362938,#362939,#362940,#362941,#362942,#362943,#362944,
#362945,#362946,#362947,#362948,#362949,#362950,#362951,#362952,#362953,
#362954,#362955,#362956,#362957,#362958,#362959,#362960,#362961,#362962,
#362963,#362964,#362965,#362966,#362967,#362968,#362969,#362970,#362971,
#362972,#362973,#362974,#362975,#362976,#362977,#362978,#362979,#362980,
#362981,#362982,#362983,#362984,#362985,#362986,#362987,#362988,#362989,
#362990,#362991,#362992,#362993,#362994,#362995,#362996,#362997,#362998,
#362999,#363000,#363001,#363002,#363003,#363004,#363005,#363006,#363007,
#363008,#363009,#363010,#363011,#363012,#363013,#363014,#363015,#363016,
#363017,#363018,#363019,#363020,#363021,#363022,#363023,#363024,#363025,
#363026,#363027,#363028,#363029,#363030,#363031,#363032,#363033,#363034,
#363035,#363036,#363037,#363038,#363039,#363040,#363041,#363042,#363043,
#363044,#363045,#363046,#363047,#363048,#363049,#363050,#363051,#363052,
#363053,#363054,#363055,#363056,#363057,#363058,#363059,#363060,#363061,
#363062,#363063,#363064,#363065,#363066,#363067,#363068,#363069,#363070,
#363071,#363072,#363073,#363074,#363075,#363076,#363077,#363078,#363079,
#363080,#363081,#363082,#363083,#363084,#363085,#363086,#363087,#363088,
#363089,#363090,#363091,#363092,#363093,#363094,#363095,#363096,#363097,
#363098,#363099,#363100,#363101,#363102,#363103,#363104,#363105,#363106,
#363107,#363108,#363109,#363110,#363111,#363112,#363113,#363114,#363115,
#363116,#363117,#363118,#363119,#363120,#363121,#363122,#363123,#363124,
#363125,#363126,#363127,#363128,#363129,#363130,#363131,#363132,#363133,
#363134,#363135,#363136,#363137,#363138,#363139,#363140,#363141,#363142,
#363143,#363144,#363145,#363146,#363147,#363148,#363149,#363150,#363151,
#363152,#363153,#363154,#363155,#363156,#363157,#363158,#363159,#363160,
#363161,#363162,#363163,#363164,#363165,#363166,#363167,#363168,#363169,
#363170,#363171,#363172,#363173,#363174,#363175,#363176,#363177,#363178,
#363179,#363180,#363181,#363182,#363183,#363184,#363185,#363186,#363187,
#363188,#363189,#363190,#363191,#363192,#363193,#363194,#363195,#363196,
#363197,#363198,#363199,#363200,#363201,#363202,#363203,#363204,#363205,
#363206,#363207,#363208,#363209,#363210,#363211,#363212,#363213,#363214,
#363215,#363216,#363217,#363218,#363219,#363220,#363221,#363222,#363223,
#363224,#363225,#363226,#363227,#363228,#363229,#363230,#363231,#363232,
#363233,#363234,#363235,#363236,#363237,#363238,#363239,#363240,#363241,
#363242,#363243,#363244,#363245),(#363246,#363247,#363248,#363249,#363250,
#363251,#363252,#363253,#363254,#363255,#363256,#363257,#363258,#363259,
#363260,#363261,#363262,#363263,#363264,#363265,#363266,#363267,#363268,
#363269,#363270,#363271,#363272,#363273,#363274,#363275,#363276,#363277,
#363278,#363279,#363280,#363281,#363282,#363283,#363284,#363285,#363286,
#363287,#363288,#363289,#363290,#363291,#363292,#363293,#363294,#363295,
#363296,#363297,#363298,#363299,#363300,#363301,#363302,#363303,#363304,
#363305,#363306,#363307,#363308,#363309,#363310,#363311,#363312,#363313,
#363314,#363315,#363316,#363317,#363318,#363319,#363320,#363321,#363322,
#363323,#363324,#363325,#363326,#363327,#363328,#363329,#363330,#363331,
#363332,#363333,#363334,#363335,#363336,#363337,#363338,#363339,#363340,
#363341,#363342,#363343,#363344,#363345,#363346,#363347,#363348,#363349,
#363350,#363351,#363352,#363353,#363354,#363355,#363356,#363357,#363358,
#363359,#363360,#363361,#363362,#363363,#363364,#363365,#363366,#363367,
#363368,#363369,#363370,#363371,#363372,#363373,#363374,#363375,#363376,
#363377,#363378,#363379,#363380,#363381,#363382,#363383,#363384,#363385,
#363386,#363387,#363388,#363389,#363390,#363391,#363392,#363393,#363394,
#363395,#363396,#363397,#363398,#363399,#363400,#363401,#363402,#363403,
#363404,#363405,#363406,#363407,#363408,#363409,#363410,#363411,#363412,
#363413,#363414,#363415,#363416,#363417,#363418,#363419,#363420,#363421,
#363422,#363423,#363424,#363425,#363426,#363427,#363428,#363429,#363430,
#363431,#363432,#363433,#363434,#363435,#363436,#363437,#363438,#363439,
#363440,#363441,#363442,#363443,#363444,#363445,#363446,#363447,#363448,
#363449,#363450,#363451,#363452,#363453,#363454,#363455,#363456,#363457,
#363458,#363459,#363460,#363461,#363462,#363463,#363464,#363465,#363466,
#363467,#363468,#363469,#363470,#363471,#363472,#363473,#363474,#363475,
#363476,#363477,#363478,#363479,#363480,#363481,#363482,#363483,#363484,
#363485,#363486,#363487,#363488,#363489,#363490,#363491,#363492,#363493,
#363494,#363495,#363496,#363497,#363498,#363499,#363500,#363501,#363502,
#363503,#363504,#363505,#363506,#363507,#363508,#363509,#363510,#363511,
#363512,#363513,#363514,#363515,#363516,#363517,#363518,#363519,#363520,
#363521,#363522,#363523,#363524,#363525,#363526,#363527,#363528,#363529,
#363530,#363531,#363532,#363533,#363534,#363535,#363536,#363537,#363538,
#363539,#363540,#363541,#363542,#363543,#363544,#363545,#363546,#363547,
#363548,#363549,#363550,#363551,#363552,#363553,#363554,#363555,#363556,
#363557,#363558,#363559,#363560,#363561,#363562,#363563,#363564,#363565,
#363566,#363567,#363568,#363569,#363570,#363571,#363572,#363573,#363574,
#363575,#363576,#363577,#363578,#363579,#363580,#363581,#363582,#363583,
#363584,#363585,#363586,#363587,#363588,#363589,#363590,#363591,#363592,
#363593,#363594,#363595,#363596,#363597,#363598,#363599,#363600,#363601,
#363602,#363603,#363604,#363605,#363606,#363607,#363608,#363609,#363610,
#363611,#363612,#363613,#363614,#363615,#363616,#363617,#363618,#363619,
#363620,#363621,#363622,#363623,#363624,#363625,#363626,#363627,#363628,
#363629,#363630,#363631,#363632,#363633,#363634,#363635,#363636,#363637,
#363638,#363639,#363640,#363641,#363642)),.UNSPECIFIED.,.F.,.F.,.F.)
B_SPLINE_SURFACE_WITH_KNOTS((2,2),(3,2,2,2,2,2,2,2,2,2,2,2,2,2,2,2,2,2,
2,2,2,2,2,2,2,2,2,2,2,2,2,2,2,2,2,2,2,2,2,2,2,2,2,2,2,2,2,2,2,2,2,2,2,2,
2,2,2,2,2,2,2,2,2,2,2,2,2,2,2,2,2,2,2,2,2,2,2,2,2,2,2,2,2,2,2,2,2,2,2,2,
2,2,2,2,2,2,2,2,2,2,2,2,2,2,2,2,2,2,2,2,2,2,2,2,2,2,2,2,2,2,2,2,2,2,2,2,
2,2,2,2,2,2,2,2,2,2,2,2,2,2,2,2,2,2,2,2,2,2,2,2,2,2,2,2,2,2,2,2,2,2,2,2,
2,2,2,2,2,2,2,2,2,2,2,2,2,2,2,2,2,2,2,2,2,2,2,2,2,2,2,2,2,2,2,2,2,2,2,2,
3),(-1.21782920567261E-5,1.),(0.,0.00505050505050505,0.0101010101010101,
0.0151515151515152,0.0202020202020202,0.0252525252525253,0.0303030303030303,
0.0353535353535354,0.0404040404040404,0.0454545454545455,0.0505050505050505,
0.0555555555555556,0.0606060606060606,0.0656565656565657,0.0707070707070707,
0.0757575757575758,0.0808080808080808,0.0858585858585859,0.0909090909090909,
0.095959595959596,0.101010101010101,0.106060606060606,0.111111111111111,
0.116161616161616,0.121212121212121,0.126262626262626,0.131313131313131,
0.136363636363636,0.141414141414141,0.146464646464646,0.151515151515152,
0.156565656565657,0.161616161616162,0.166666666666667,0.171717171717172,
0.176767676767677,0.181818181818182,0.186868686868687,0.191919191919192,
0.196969696969697,0.202020202020202,0.207070707070707,0.212121212121212,
0.217171717171717,0.222222222222222,0.227272727272727,0.232323232323232,
0.237373737373737,0.242424242424242,0.247474747474747,0.252525252525253,
0.257575757575758,0.262626262626263,0.267676767676768,0.272727272727273,
0.277777777777778,0.282828282828283,0.287878787878788,0.292929292929293,
0.297979797979798,0.303030303030303,0.308080808080808,0.313131313131313,
0.318181818181818,0.323232323232323,0.328282828282828,0.333333333333333,
0.338383838383838,0.343434343434343,0.348484848484849,0.353535353535354,
0.358585858585859,0.363636363636364,0.368686868686869,0.373737373737374,
0.378787878787879,0.383838383838384,0.388888888888889,0.393939393939394,
0.398989898989899,0.404040404040404,0.409090909090909,0.414141414141414,
0.419191919191919,0.424242424242424,0.429292929292929,0.434343434343434,
0.439393939393939,0.444444444444444,0.44949494949495,0.454545454545455,
0.45959595959596,0.464646464646465,0.46969696969697,0.474747474747475,0.47979797979798,
0.484848484848485,0.48989898989899,0.494949494949495,0.5,0.505050505050505,
0.51010101010101,0.515151515151515,0.52020202020202,0.525252525252525,0.53030303030303,
0.535353535353535,0.54040404040404,0.545454545454545,0.55050505050505,0.555555555555556,
0.560606060606061,0.565656565656566,0.570707070707071,0.575757575757576,
0.580808080808081,0.585858585858586,0.590909090909091,0.595959595959596,
0.601010101010101,0.606060606060606,0.611111111111111,0.616161616161616,
0.621212121212121,0.626262626262626,0.631313131313131,0.636363636363636,
0.641414141414141,0.646464646464647,0.651515151515151,0.656565656565657,
0.661616161616162,0.666666666666667,0.671717171717172,0.676767676767677,
0.681818181818182,0.686868686868687,0.691919191919192,0.696969696969697,
0.702020202020202,0.707070707070707,0.712121212121212,0.717171717171717,
0.722222222222222,0.727272727272727,0.732323232323232,0.737373737373737,
0.742424242424242,0.747474747474748,0.752525252525252,0.757575757575758,
0.762626262626263,0.767676767676768,0.772727272727273,0.777777777777778,
0.782828282828283,0.787878787878788,0.792929292929293,0.797979797979798,
0.803030303030303,0.808080808080808,0.813131313131313,0.818181818181818,
0.823232323232323,0.828282828282828,0.833333333333333,0.838383838383838,
0.843434343434343,0.848484848484849,0.853535353535353,0.858585858585859,
0.863636363636364,0.868686868686869,0.873737373737374,0.878787878787879,
0.883838383838384,0.888888888888889,0.893939393939394,0.898989898989899,
0.904040404040404,0.909090909090909,0.914141414141414,0.919191919191919,
0.924242424242424,0.929292929292929,0.934343434343434,0.939393939393939,
0.944444444444444,0.94949494949495,0.954545454545455,0.95959595959596,0.964646464646465,
0.96969696969697,0.974747474747475,0.97979797979798,0.984848484848485,0.98989898989899,
0.994949494949495,1.),.UNSPECIFIED.)
GEOMETRIC_REPRESENTATION_ITEM()
RATIONAL_B_SPLINE_SURFACE(((1.,0.866025403784439,1.,0.866025403784439,1.,
0.866025403784439,1.,0.866025403784439,1.,0.866025403784439,1.,0.866025403784439,
1.,0.866025403784439,1.,0.866025403784439,1.,0.866025403784439,1.,0.866025403784439,
1.,0.866025403784439,1.,0.866025403784439,1.,0.866025403784439,1.,0.866025403784439,
1.,0.866025403784439,1.,0.866025403784439,1.,0.866025403784439,1.,0.866025403784439,
1.,0.866025403784439,1.,0.866025403784439,1.,0.866025403784439,1.,0.866025403784439,
1.,0.866025403784439,1.,0.866025403784439,1.,0.866025403784439,1.,0.866025403784439,
1.,0.866025403784439,1.,0.866025403784439,1.,0.866025403784439,1.,0.866025403784439,
1.,0.866025403784439,1.,0.866025403784439,1.,0.866025403784439,1.,0.866025403784439,
1.,0.866025403784439,1.,0.866025403784439,1.,0.866025403784439,1.,0.866025403784439,
1.,0.866025403784439,1.,0.866025403784439,1.,0.866025403784439,1.,0.866025403784439,
1.,0.866025403784439,1.,0.866025403784439,1.,0.866025403784439,1.,0.866025403784439,
1.,0.866025403784439,1.,0.866025403784439,1.,0.866025403784439,1.,0.866025403784439,
1.,0.866025403784439,1.,0.866025403784439,1.,0.866025403784439,1.,0.866025403784439,
1.,0.866025403784439,1.,0.866025403784439,1.,0.866025403784439,1.,0.866025403784439,
1.,0.866025403784439,1.,0.866025403784439,1.,0.866025403784439,1.,0.866025403784439,
1.,0.866025403784439,1.,0.866025403784439,1.,0.866025403784439,1.,0.866025403784439,
1.,0.866025403784439,1.,0.866025403784439,1.,0.866025403784439,1.,0.866025403784439,
1.,0.866025403784439,1.,0.866025403784439,1.,0.866025403784439,1.,0.866025403784439,
1.,0.866025403784439,1.,0.866025403784439,1.,0.866025403784439,1.,0.866025403784439,
1.,0.866025403784439,1.,0.866025403784439,1.,0.866025403784439,1.,0.866025403784439,
1.,0.866025403784439,1.,0.866025403784439,1.,0.866025403784439,1.,0.866025403784439,
1.,0.866025403784439,1.,0.866025403784439,1.,0.866025403784439,1.,0.866025403784439,
1.,0.866025403784439,1.,0.866025403784439,1.,0.866025403784439,1.,0.866025403784439,
1.,0.866025403784439,1.,0.866025403784439,1.,0.866025403784439,1.,0.866025403784439,
1.,0.866025403784439,1.,0.866025403784439,1.,0.866025403784439,1.,0.866025403784439,
1.,0.866025403784439,1.,0.866025403784439,1.,0.866025403784439,1.,0.866025403784439,
1.,0.866025403784439,1.,0.866025403784439,1.,0.866025403784439,1.,0.866025403784439,
1.,0.866025403784439,1.,0.866025403784439,1.,0.866025403784439,1.,0.866025403784439,
1.,0.866025403784439,1.,0.866025403784439,1.,0.866025403784439,1.,0.866025403784439,
1.,0.866025403784439,1.,0.866025403784439,1.,0.866025403784439,1.,0.866025403784439,
1.,0.866025403784439,1.,0.866025403784439,1.,0.866025403784439,1.,0.866025403784439,
1.,0.866025403784439,1.,0.866025403784439,1.,0.866025403784439,1.,0.866025403784439,
1.,0.866025403784439,1.,0.866025403784439,1.,0.866025403784439,1.,0.866025403784439,
1.,0.866025403784439,1.,0.866025403784439,1.,0.866025403784439,1.,0.866025403784439,
1.,0.866025403784439,1.,0.866025403784439,1.,0.866025403784439,1.,0.866025403784439,
1.,0.866025403784439,1.,0.866025403784439,1.,0.866025403784439,1.,0.866025403784439,
1.,0.866025403784439,1.,0.866025403784439,1.,0.866025403784439,1.,0.866025403784439,
1.,0.866025403784439,1.,0.866025403784439,1.,0.866025403784439,1.,0.866025403784439,
1.,0.866025403784439,1.,0.866025403784439,1.,0.866025403784439,1.,0.866025403784439,
1.,0.866025403784439,1.,0.866025403784439,1.,0.866025403784439,1.,0.866025403784439,
1.,0.866025403784439,1.,0.866025403784439,1.,0.866025403784439,1.,0.866025403784439,
1.,0.866025403784439,1.,0.866025403784439,1.,0.866025403784439,1.,0.866025403784439,
1.,0.866025403784439,1.,0.866025403784439,1.,0.866025403784439,1.,0.866025403784439,
1.,0.866025403784439,1.,0.866025403784439,1.,0.866025403784439,1.,0.866025403784439,
1.,0.866025403784439,1.,0.866025403784439,1.,0.866025403784439,1.,0.866025403784439,
1.,0.866025403784439,1.,0.866025403784439,1.,0.866025403784439,1.,0.866025403784439,
1.,0.866025403784439,1.,0.866025403784439,1.,0.866025403784439,1.,0.866025403784439,
1.,0.866025403784439,1.,0.866025403784439,1.,0.866025403784439,1.,0.866025403784439,
1.,0.866025403784439,1.,0.866025403784439,1.,0.866025403784439,1.,0.866025403784439,
1.),(1.,0.866025403784439,1.,0.866025403784439,1.,0.866025403784439,1.,
0.866025403784439,1.,0.866025403784439,1.,0.866025403784439,1.,0.866025403784439,
1.,0.866025403784439,1.,0.866025403784439,1.,0.866025403784439,1.,0.866025403784439,
1.,0.866025403784439,1.,0.866025403784439,1.,0.866025403784439,1.,0.866025403784439,
1.,0.866025403784439,1.,0.866025403784439,1.,0.866025403784439,1.,0.866025403784439,
1.,0.866025403784439,1.,0.866025403784439,1.,0.866025403784439,1.,0.866025403784439,
1.,0.866025403784439,1.,0.866025403784439,1.,0.866025403784439,1.,0.866025403784439,
1.,0.866025403784439,1.,0.866025403784439,1.,0.866025403784439,1.,0.866025403784439,
1.,0.866025403784439,1.,0.866025403784439,1.,0.866025403784439,1.,0.866025403784439,
1.,0.866025403784439,1.,0.866025403784439,1.,0.866025403784439,1.,0.866025403784439,
1.,0.866025403784439,1.,0.866025403784439,1.,0.866025403784439,1.,0.866025403784439,
1.,0.866025403784439,1.,0.866025403784439,1.,0.866025403784439,1.,0.866025403784439,
1.,0.866025403784439,1.,0.866025403784439,1.,0.866025403784439,1.,0.866025403784439,
1.,0.866025403784439,1.,0.866025403784439,1.,0.866025403784439,1.,0.866025403784439,
1.,0.866025403784439,1.,0.866025403784439,1.,0.866025403784439,1.,0.866025403784439,
1.,0.866025403784439,1.,0.866025403784439,1.,0.866025403784439,1.,0.866025403784439,
1.,0.866025403784439,1.,0.866025403784439,1.,0.866025403784439,1.,0.866025403784439,
1.,0.866025403784439,1.,0.866025403784439,1.,0.866025403784439,1.,0.866025403784439,
1.,0.866025403784439,1.,0.866025403784439,1.,0.866025403784439,1.,0.866025403784439,
1.,0.866025403784439,1.,0.866025403784439,1.,0.866025403784439,1.,0.866025403784439,
1.,0.866025403784439,1.,0.866025403784439,1.,0.866025403784439,1.,0.866025403784439,
1.,0.866025403784439,1.,0.866025403784439,1.,0.866025403784439,1.,0.866025403784439,
1.,0.866025403784439,1.,0.866025403784439,1.,0.866025403784439,1.,0.866025403784439,
1.,0.866025403784439,1.,0.866025403784439,1.,0.866025403784439,1.,0.866025403784439,
1.,0.866025403784439,1.,0.866025403784439,1.,0.866025403784439,1.,0.866025403784439,
1.,0.866025403784439,1.,0.866025403784439,1.,0.866025403784439,1.,0.866025403784439,
1.,0.866025403784439,1.,0.866025403784439,1.,0.866025403784439,1.,0.866025403784439,
1.,0.866025403784439,1.,0.866025403784439,1.,0.866025403784439,1.,0.866025403784439,
1.,0.866025403784439,1.,0.866025403784439,1.,0.866025403784439,1.,0.866025403784439,
1.,0.866025403784439,1.,0.866025403784439,1.,0.866025403784439,1.,0.866025403784439,
1.,0.866025403784439,1.,0.866025403784439,1.,0.866025403784439,1.,0.866025403784439,
1.,0.866025403784439,1.,0.866025403784439,1.,0.866025403784439,1.,0.866025403784439,
1.,0.866025403784439,1.,0.866025403784439,1.,0.866025403784439,1.,0.866025403784439,
1.,0.866025403784439,1.,0.866025403784439,1.,0.866025403784439,1.,0.866025403784439,
1.,0.866025403784439,1.,0.866025403784439,1.,0.866025403784439,1.,0.866025403784439,
1.,0.866025403784439,1.,0.866025403784439,1.,0.866025403784439,1.,0.866025403784439,
1.,0.866025403784439,1.,0.866025403784439,1.,0.866025403784439,1.,0.866025403784439,
1.,0.866025403784439,1.,0.866025403784439,1.,0.866025403784439,1.,0.866025403784439,
1.,0.866025403784439,1.,0.866025403784439,1.,0.866025403784439,1.,0.866025403784439,
1.,0.866025403784439,1.,0.866025403784439,1.,0.866025403784439,1.,0.866025403784439,
1.,0.866025403784439,1.,0.866025403784439,1.,0.866025403784439,1.,0.866025403784439,
1.,0.866025403784439,1.,0.866025403784439,1.,0.866025403784439,1.,0.866025403784439,
1.,0.866025403784439,1.,0.866025403784439,1.,0.866025403784439,1.,0.866025403784439,
1.,0.866025403784439,1.,0.866025403784439,1.,0.866025403784439,1.,0.866025403784439,
1.,0.866025403784439,1.,0.866025403784439,1.,0.866025403784439,1.,0.866025403784439,
1.,0.866025403784439,1.,0.866025403784439,1.,0.866025403784439,1.,0.866025403784439,
1.,0.866025403784439,1.,0.866025403784439,1.,0.866025403784439,1.,0.866025403784439,
1.,0.866025403784439,1.,0.866025403784439,1.,0.866025403784439,1.,0.866025403784439,
1.,0.866025403784439,1.,0.866025403784439,1.,0.866025403784439,1.,0.866025403784439,
1.,0.866025403784439,1.,0.866025403784439,1.,0.866025403784439,1.)))
REPRESENTATION_ITEM('')
SURFACE()
);
#4112=(
BOUNDED_CURVE()
B_SPLINE_CURVE(2,(#358532,#358533,#358534,#358535,#358536,#358537,#358538,
#358539,#358540,#358541,#358542,#358543,#358544),.UNSPECIFIED.,.F.,.F.)
B_SPLINE_CURVE_WITH_KNOTS((3,2,2,2,2,2,3),(0.954545454545455,0.95959595959596,
0.964646464646465,0.96969696969697,0.974747474747475,0.97979797979798,0.984848484848485),
 .UNSPECIFIED.)
CURVE()
GEOMETRIC_REPRESENTATION_ITEM()
RATIONAL_B_SPLINE_CURVE((1.,0.866025403784439,1.,0.866025403784439,1.,0.866025403784439,
1.,0.866025403784439,1.,0.866025403784439,1.,0.866025403784439,1.))
REPRESENTATION_ITEM('')
);
#4113=(
BOUNDED_CURVE()
B_SPLINE_CURVE(2,(#358547,#358548,#358549,#358550,#358551,#358552,#358553,
#358554,#358555,#358556,#358557,#358558,#358559),.UNSPECIFIED.,.F.,.F.)
B_SPLINE_CURVE_WITH_KNOTS((3,2,2,2,2,2,3),(0.954545454545455,0.95959595959596,
0.964646464646465,0.96969696969697,0.974747474747475,0.97979797979798,0.981126180289492),
 .UNSPECIFIED.)
CURVE()
GEOMETRIC_REPRESENTATION_ITEM()
RATIONAL_B_SPLINE_CURVE((1.,0.866025403784439,1.,0.866025403784439,1.,0.866025403784439,
1.,0.866025403784439,1.,0.866025403784439,1.,0.964766865340363,0.948065210722611))
REPRESENTATION_ITEM('')
);
#4114=(
BOUNDED_CURVE()
B_SPLINE_CURVE(2,(#358564,#358565,#358566,#358567,#358568,#358569,#358570,
#358571,#358572,#358573,#358574,#358575,#358576),.UNSPECIFIED.,.F.,.F.)
B_SPLINE_CURVE_WITH_KNOTS((3,2,2,2,2,2,3),(0.924242424242424,0.929292929292929,
0.934343434343434,0.939393939393939,0.944444444444444,0.94949494949495,
0.954545454545455),.UNSPECIFIED.)
CURVE()
GEOMETRIC_REPRESENTATION_ITEM()
RATIONAL_B_SPLINE_CURVE((1.,0.866025403784439,1.,0.866025403784439,1.,0.866025403784439,
1.,0.866025403784439,1.,0.866025403784439,1.,0.866025403784439,1.))
REPRESENTATION_ITEM('')
);
#4115=(
BOUNDED_CURVE()
B_SPLINE_CURVE(2,(#358577,#358578,#358579,#358580,#358581,#358582,#358583,
#358584,#358585,#358586,#358587,#358588,#358589),.UNSPECIFIED.,.F.,.F.)
B_SPLINE_CURVE_WITH_KNOTS((3,2,2,2,2,2,3),(0.924242424242424,0.929292929292929,
0.934343434343434,0.939393939393939,0.944444444444444,0.94949494949495,
0.954545454545455),.UNSPECIFIED.)
CURVE()
GEOMETRIC_REPRESENTATION_ITEM()
RATIONAL_B_SPLINE_CURVE((1.,0.866025403784439,1.,0.866025403784439,1.,0.866025403784439,
1.,0.866025403784439,1.,0.866025403784439,1.,0.866025403784439,1.))
REPRESENTATION_ITEM('')
);
#4116=(
BOUNDED_CURVE()
B_SPLINE_CURVE(2,(#358594,#358595,#358596,#358597,#358598,#358599,#358600,
#358601,#358602,#358603,#358604,#358605,#358606),.UNSPECIFIED.,.F.,.F.)
B_SPLINE_CURVE_WITH_KNOTS((3,2,2,2,2,2,3),(0.893939393939394,0.898989898989899,
0.904040404040404,0.909090909090909,0.914141414141414,0.919191919191919,
0.924242424242424),.UNSPECIFIED.)
CURVE()
GEOMETRIC_REPRESENTATION_ITEM()
RATIONAL_B_SPLINE_CURVE((1.,0.866025403784439,1.,0.866025403784439,1.,0.866025403784439,
1.,0.866025403784439,1.,0.866025403784439,1.,0.866025403784439,1.))
REPRESENTATION_ITEM('')
);
#4117=(
BOUNDED_CURVE()
B_SPLINE_CURVE(2,(#358607,#358608,#358609,#358610,#358611,#358612,#358613,
#358614,#358615,#358616,#358617,#358618,#358619),.UNSPECIFIED.,.F.,.F.)
B_SPLINE_CURVE_WITH_KNOTS((3,2,2,2,2,2,3),(0.893939393939394,0.898989898989899,
0.904040404040404,0.909090909090909,0.914141414141414,0.919191919191919,
0.924242424242424),.UNSPECIFIED.)
CURVE()
GEOMETRIC_REPRESENTATION_ITEM()
RATIONAL_B_SPLINE_CURVE((1.,0.866025403784439,1.,0.866025403784439,1.,0.866025403784439,
1.,0.866025403784439,1.,0.866025403784439,1.,0.866025403784439,1.))
REPRESENTATION_ITEM('')
);
#4118=(
BOUNDED_CURVE()
B_SPLINE_CURVE(2,(#358624,#358625,#358626,#358627,#358628,#358629,#358630,
#358631,#358632,#358633,#358634,#358635,#358636),.UNSPECIFIED.,.F.,.F.)
B_SPLINE_CURVE_WITH_KNOTS((3,2,2,2,2,2,3),(0.863636363636364,0.868686868686869,
0.873737373737374,0.878787878787879,0.883838383838384,0.888888888888889,
0.893939393939394),.UNSPECIFIED.)
CURVE()
GEOMETRIC_REPRESENTATION_ITEM()
RATIONAL_B_SPLINE_CURVE((1.,0.866025403784439,1.,0.866025403784439,1.,0.866025403784439,
1.,0.866025403784439,1.,0.866025403784439,1.,0.866025403784439,1.))
REPRESENTATION_ITEM('')
);
#4119=(
BOUNDED_CURVE()
B_SPLINE_CURVE(2,(#358637,#358638,#358639,#358640,#358641,#358642,#358643,
#358644,#358645,#358646,#358647,#358648,#358649),.UNSPECIFIED.,.F.,.F.)
B_SPLINE_CURVE_WITH_KNOTS((3,2,2,2,2,2,3),(0.863636363636364,0.868686868686869,
0.873737373737374,0.878787878787879,0.883838383838384,0.888888888888889,
0.893939393939394),.UNSPECIFIED.)
CURVE()
GEOMETRIC_REPRESENTATION_ITEM()
RATIONAL_B_SPLINE_CURVE((1.,0.866025403784439,1.,0.866025403784439,1.,0.866025403784439,
1.,0.866025403784439,1.,0.866025403784439,1.,0.866025403784439,1.))
REPRESENTATION_ITEM('')
);
#4120=(
BOUNDED_CURVE()
B_SPLINE_CURVE(2,(#358654,#358655,#358656,#358657,#358658,#358659,#358660,
#358661,#358662,#358663,#358664,#358665,#358666),.UNSPECIFIED.,.F.,.F.)
B_SPLINE_CURVE_WITH_KNOTS((3,2,2,2,2,2,3),(0.833333333333333,0.838383838383838,
0.843434343434343,0.848484848484849,0.853535353535353,0.858585858585859,
0.863636363636364),.UNSPECIFIED.)
CURVE()
GEOMETRIC_REPRESENTATION_ITEM()
RATIONAL_B_SPLINE_CURVE((1.,0.866025403784439,1.,0.866025403784439,1.,0.866025403784439,
1.,0.866025403784439,1.,0.866025403784439,1.,0.866025403784439,1.))
REPRESENTATION_ITEM('')
);
#4121=(
BOUNDED_CURVE()
B_SPLINE_CURVE(2,(#358667,#358668,#358669,#358670,#358671,#358672,#358673,
#358674,#358675,#358676,#358677,#358678,#358679),.UNSPECIFIED.,.F.,.F.)
B_SPLINE_CURVE_WITH_KNOTS((3,2,2,2,2,2,3),(0.833333333333333,0.838383838383838,
0.843434343434343,0.848484848484849,0.853535353535353,0.858585858585859,
0.863636363636364),.UNSPECIFIED.)
CURVE()
GEOMETRIC_REPRESENTATION_ITEM()
RATIONAL_B_SPLINE_CURVE((1.,0.866025403784439,1.,0.866025403784439,1.,0.866025403784439,
1.,0.866025403784439,1.,0.866025403784439,1.,0.866025403784439,1.))
REPRESENTATION_ITEM('')
);
#4122=(
BOUNDED_CURVE()
B_SPLINE_CURVE(2,(#358684,#358685,#358686,#358687,#358688,#358689,#358690,
#358691,#358692,#358693,#358694,#358695,#358696),.UNSPECIFIED.,.F.,.F.)
B_SPLINE_CURVE_WITH_KNOTS((3,2,2,2,2,2,3),(0.803030303030303,0.808080808080808,
0.813131313131313,0.818181818181818,0.823232323232323,0.828282828282828,
0.833333333333333),.UNSPECIFIED.)
CURVE()
GEOMETRIC_REPRESENTATION_ITEM()
RATIONAL_B_SPLINE_CURVE((1.,0.866025403784439,1.,0.866025403784439,1.,0.866025403784439,
1.,0.866025403784439,1.,0.866025403784439,1.,0.866025403784439,1.))
REPRESENTATION_ITEM('')
);
#4123=(
BOUNDED_CURVE()
B_SPLINE_CURVE(2,(#358697,#358698,#358699,#358700,#358701,#358702,#358703,
#358704,#358705,#358706,#358707,#358708,#358709),.UNSPECIFIED.,.F.,.F.)
B_SPLINE_CURVE_WITH_KNOTS((3,2,2,2,2,2,3),(0.803030303030303,0.808080808080808,
0.813131313131313,0.818181818181818,0.823232323232323,0.828282828282828,
0.833333333333333),.UNSPECIFIED.)
CURVE()
GEOMETRIC_REPRESENTATION_ITEM()
RATIONAL_B_SPLINE_CURVE((1.,0.866025403784439,1.,0.866025403784439,1.,0.866025403784439,
1.,0.866025403784439,1.,0.866025403784439,1.,0.866025403784439,1.))
REPRESENTATION_ITEM('')
);
#4124=(
BOUNDED_CURVE()
B_SPLINE_CURVE(2,(#358714,#358715,#358716,#358717,#358718,#358719,#358720,
#358721,#358722,#358723,#358724,#358725,#358726),.UNSPECIFIED.,.F.,.F.)
B_SPLINE_CURVE_WITH_KNOTS((3,2,2,2,2,2,3),(0.772727272727273,0.777777777777778,
0.782828282828283,0.787878787878788,0.792929292929293,0.797979797979798,
0.803030303030303),.UNSPECIFIED.)
CURVE()
GEOMETRIC_REPRESENTATION_ITEM()
RATIONAL_B_SPLINE_CURVE((1.,0.866025403784439,1.,0.866025403784439,1.,0.866025403784439,
1.,0.866025403784439,1.,0.866025403784439,1.,0.866025403784439,1.))
REPRESENTATION_ITEM('')
);
#4125=(
BOUNDED_CURVE()
B_SPLINE_CURVE(2,(#358727,#358728,#358729,#358730,#358731,#358732,#358733,
#358734,#358735,#358736,#358737,#358738,#358739),.UNSPECIFIED.,.F.,.F.)
B_SPLINE_CURVE_WITH_KNOTS((3,2,2,2,2,2,3),(0.772727272727273,0.777777777777778,
0.782828282828283,0.787878787878788,0.792929292929293,0.797979797979798,
0.803030303030303),.UNSPECIFIED.)
CURVE()
GEOMETRIC_REPRESENTATION_ITEM()
RATIONAL_B_SPLINE_CURVE((1.,0.866025403784439,1.,0.866025403784439,1.,0.866025403784439,
1.,0.866025403784439,1.,0.866025403784439,1.,0.866025403784439,1.))
REPRESENTATION_ITEM('')
);
#4126=(
BOUNDED_CURVE()
B_SPLINE_CURVE(2,(#358744,#358745,#358746,#358747,#358748,#358749,#358750,
#358751,#358752,#358753,#358754,#358755,#358756),.UNSPECIFIED.,.F.,.F.)
B_SPLINE_CURVE_WITH_KNOTS((3,2,2,2,2,2,3),(0.742424242424242,0.747474747474748,
0.752525252525252,0.757575757575758,0.762626262626263,0.767676767676768,
0.772727272727273),.UNSPECIFIED.)
CURVE()
GEOMETRIC_REPRESENTATION_ITEM()
RATIONAL_B_SPLINE_CURVE((1.,0.866025403784439,1.,0.866025403784439,1.,0.866025403784439,
1.,0.866025403784439,1.,0.866025403784439,1.,0.866025403784439,1.))
REPRESENTATION_ITEM('')
);
#4127=(
BOUNDED_CURVE()
B_SPLINE_CURVE(2,(#358757,#358758,#358759,#358760,#358761,#358762,#358763,
#358764,#358765,#358766,#358767,#358768,#358769),.UNSPECIFIED.,.F.,.F.)
B_SPLINE_CURVE_WITH_KNOTS((3,2,2,2,2,2,3),(0.742424242424242,0.747474747474748,
0.752525252525252,0.757575757575758,0.762626262626263,0.767676767676768,
0.772727272727273),.UNSPECIFIED.)
CURVE()
GEOMETRIC_REPRESENTATION_ITEM()
RATIONAL_B_SPLINE_CURVE((1.,0.866025403784439,1.,0.866025403784439,1.,0.866025403784439,
1.,0.866025403784439,1.,0.866025403784439,1.,0.866025403784439,1.))
REPRESENTATION_ITEM('')
);
#4128=(
BOUNDED_CURVE()
B_SPLINE_CURVE(2,(#358774,#358775,#358776,#358777,#358778,#358779,#358780,
#358781,#358782,#358783,#358784,#358785,#358786),.UNSPECIFIED.,.F.,.F.)
B_SPLINE_CURVE_WITH_KNOTS((3,2,2,2,2,2,3),(0.712121212121212,0.717171717171717,
0.722222222222222,0.727272727272727,0.732323232323232,0.737373737373737,
0.742424242424242),.UNSPECIFIED.)
CURVE()
GEOMETRIC_REPRESENTATION_ITEM()
RATIONAL_B_SPLINE_CURVE((1.,0.866025403784439,1.,0.866025403784439,1.,0.866025403784439,
1.,0.866025403784439,1.,0.866025403784439,1.,0.866025403784439,1.))
REPRESENTATION_ITEM('')
);
#4129=(
BOUNDED_CURVE()
B_SPLINE_CURVE(2,(#358787,#358788,#358789,#358790,#358791,#358792,#358793,
#358794,#358795,#358796,#358797,#358798,#358799),.UNSPECIFIED.,.F.,.F.)
B_SPLINE_CURVE_WITH_KNOTS((3,2,2,2,2,2,3),(0.712121212121212,0.717171717171717,
0.722222222222222,0.727272727272727,0.732323232323232,0.737373737373737,
0.742424242424242),.UNSPECIFIED.)
CURVE()
GEOMETRIC_REPRESENTATION_ITEM()
RATIONAL_B_SPLINE_CURVE((1.,0.866025403784439,1.,0.866025403784439,1.,0.866025403784439,
1.,0.866025403784439,1.,0.866025403784439,1.,0.866025403784439,1.))
REPRESENTATION_ITEM('')
);
#4130=(
BOUNDED_CURVE()
B_SPLINE_CURVE(2,(#358804,#358805,#358806,#358807,#358808,#358809,#358810,
#358811,#358812,#358813,#358814,#358815,#358816),.UNSPECIFIED.,.F.,.F.)
B_SPLINE_CURVE_WITH_KNOTS((3,2,2,2,2,2,3),(0.681818181818182,0.686868686868687,
0.691919191919192,0.696969696969697,0.702020202020202,0.707070707070707,
0.712121212121212),.UNSPECIFIED.)
CURVE()
GEOMETRIC_REPRESENTATION_ITEM()
RATIONAL_B_SPLINE_CURVE((1.,0.866025403784439,1.,0.866025403784439,1.,0.866025403784439,
1.,0.866025403784439,1.,0.866025403784439,1.,0.866025403784439,1.))
REPRESENTATION_ITEM('')
);
#4131=(
BOUNDED_CURVE()
B_SPLINE_CURVE(2,(#358817,#358818,#358819,#358820,#358821,#358822,#358823,
#358824,#358825,#358826,#358827,#358828,#358829),.UNSPECIFIED.,.F.,.F.)
B_SPLINE_CURVE_WITH_KNOTS((3,2,2,2,2,2,3),(0.681818181818182,0.686868686868687,
0.691919191919192,0.696969696969697,0.702020202020202,0.707070707070707,
0.712121212121212),.UNSPECIFIED.)
CURVE()
GEOMETRIC_REPRESENTATION_ITEM()
RATIONAL_B_SPLINE_CURVE((1.,0.866025403784439,1.,0.866025403784439,1.,0.866025403784439,
1.,0.866025403784439,1.,0.866025403784439,1.,0.866025403784439,1.))
REPRESENTATION_ITEM('')
);
#4132=(
BOUNDED_CURVE()
B_SPLINE_CURVE(2,(#358834,#358835,#358836,#358837,#358838,#358839,#358840,
#358841,#358842,#358843,#358844,#358845,#358846),.UNSPECIFIED.,.F.,.F.)
B_SPLINE_CURVE_WITH_KNOTS((3,2,2,2,2,2,3),(0.651515151515151,0.656565656565657,
0.661616161616162,0.666666666666667,0.671717171717172,0.676767676767677,
0.681818181818182),.UNSPECIFIED.)
CURVE()
GEOMETRIC_REPRESENTATION_ITEM()
RATIONAL_B_SPLINE_CURVE((1.,0.866025403784439,1.,0.866025403784439,1.,0.866025403784439,
1.,0.866025403784439,1.,0.866025403784439,1.,0.866025403784439,1.))
REPRESENTATION_ITEM('')
);
#4133=(
BOUNDED_CURVE()
B_SPLINE_CURVE(2,(#358847,#358848,#358849,#358850,#358851,#358852,#358853,
#358854,#358855,#358856,#358857,#358858,#358859),.UNSPECIFIED.,.F.,.F.)
B_SPLINE_CURVE_WITH_KNOTS((3,2,2,2,2,2,3),(0.651515151515151,0.656565656565656,
0.661616161616162,0.666666666666667,0.671717171717172,0.676767676767677,
0.681818181818182),.UNSPECIFIED.)
CURVE()
GEOMETRIC_REPRESENTATION_ITEM()
RATIONAL_B_SPLINE_CURVE((1.,0.866025403784439,1.,0.866025403784439,1.,0.866025403784439,
1.,0.866025403784439,1.,0.866025403784439,1.,0.866025403784439,1.))
REPRESENTATION_ITEM('')
);
#4134=(
BOUNDED_CURVE()
B_SPLINE_CURVE(2,(#358864,#358865,#358866,#358867,#358868,#358869,#358870,
#358871,#358872,#358873,#358874,#358875,#358876),.UNSPECIFIED.,.F.,.F.)
B_SPLINE_CURVE_WITH_KNOTS((3,2,2,2,2,2,3),(0.621212121212121,0.626262626262626,
0.631313131313131,0.636363636363636,0.641414141414141,0.646464646464647,
0.651515151515151),.UNSPECIFIED.)
CURVE()
GEOMETRIC_REPRESENTATION_ITEM()
RATIONAL_B_SPLINE_CURVE((1.,0.866025403784439,1.,0.866025403784439,1.,0.866025403784439,
1.,0.866025403784439,1.,0.866025403784439,1.,0.866025403784439,1.))
REPRESENTATION_ITEM('')
);
#4135=(
BOUNDED_CURVE()
B_SPLINE_CURVE(2,(#358877,#358878,#358879,#358880,#358881,#358882,#358883,
#358884,#358885,#358886,#358887,#358888,#358889),.UNSPECIFIED.,.F.,.F.)
B_SPLINE_CURVE_WITH_KNOTS((3,2,2,2,2,2,3),(0.621212121212121,0.626262626262626,
0.631313131313131,0.636363636363636,0.641414141414141,0.646464646464647,
0.651515151515151),.UNSPECIFIED.)
CURVE()
GEOMETRIC_REPRESENTATION_ITEM()
RATIONAL_B_SPLINE_CURVE((1.,0.866025403784439,1.,0.866025403784439,1.,0.866025403784439,
1.,0.866025403784439,1.,0.866025403784439,1.,0.866025403784439,1.))
REPRESENTATION_ITEM('')
);
#4136=(
BOUNDED_CURVE()
B_SPLINE_CURVE(2,(#358894,#358895,#358896,#358897,#358898,#358899,#358900,
#358901,#358902,#358903,#358904,#358905,#358906),.UNSPECIFIED.,.F.,.F.)
B_SPLINE_CURVE_WITH_KNOTS((3,2,2,2,2,2,3),(0.590909090909091,0.595959595959596,
0.601010101010101,0.606060606060606,0.611111111111111,0.616161616161616,
0.621212121212121),.UNSPECIFIED.)
CURVE()
GEOMETRIC_REPRESENTATION_ITEM()
RATIONAL_B_SPLINE_CURVE((1.,0.866025403784439,1.,0.866025403784439,1.,0.866025403784439,
1.,0.866025403784439,1.,0.866025403784439,1.,0.866025403784439,1.))
REPRESENTATION_ITEM('')
);
#4137=(
BOUNDED_CURVE()
B_SPLINE_CURVE(2,(#358907,#358908,#358909,#358910,#358911,#358912,#358913,
#358914,#358915,#358916,#358917,#358918,#358919),.UNSPECIFIED.,.F.,.F.)
B_SPLINE_CURVE_WITH_KNOTS((3,2,2,2,2,2,3),(0.590909090909091,0.595959595959596,
0.601010101010101,0.606060606060606,0.611111111111111,0.616161616161616,
0.621212121212121),.UNSPECIFIED.)
CURVE()
GEOMETRIC_REPRESENTATION_ITEM()
RATIONAL_B_SPLINE_CURVE((1.,0.866025403784439,1.,0.866025403784439,1.,0.866025403784439,
1.,0.866025403784439,1.,0.866025403784439,1.,0.866025403784439,1.))
REPRESENTATION_ITEM('')
);
#4138=(
BOUNDED_CURVE()
B_SPLINE_CURVE(2,(#358924,#358925,#358926,#358927,#358928,#358929,#358930,
#358931,#358932,#358933,#358934,#358935,#358936),.UNSPECIFIED.,.F.,.F.)
B_SPLINE_CURVE_WITH_KNOTS((3,2,2,2,2,2,3),(0.560606060606061,0.565656565656566,
0.570707070707071,0.575757575757576,0.580808080808081,0.585858585858586,
0.590909090909091),.UNSPECIFIED.)
CURVE()
GEOMETRIC_REPRESENTATION_ITEM()
RATIONAL_B_SPLINE_CURVE((1.,0.866025403784439,1.,0.866025403784439,1.,0.866025403784439,
1.,0.866025403784439,1.,0.866025403784439,1.,0.866025403784439,1.))
REPRESENTATION_ITEM('')
);
#4139=(
BOUNDED_CURVE()
B_SPLINE_CURVE(2,(#358937,#358938,#358939,#358940,#358941,#358942,#358943,
#358944,#358945,#358946,#358947,#358948,#358949),.UNSPECIFIED.,.F.,.F.)
B_SPLINE_CURVE_WITH_KNOTS((3,2,2,2,2,2,3),(0.560606060606061,0.565656565656566,
0.570707070707071,0.575757575757576,0.580808080808081,0.585858585858586,
0.590909090909091),.UNSPECIFIED.)
CURVE()
GEOMETRIC_REPRESENTATION_ITEM()
RATIONAL_B_SPLINE_CURVE((1.,0.866025403784439,1.,0.866025403784439,1.,0.866025403784439,
1.,0.866025403784439,1.,0.866025403784439,1.,0.866025403784439,1.))
REPRESENTATION_ITEM('')
);
#4140=(
BOUNDED_CURVE()
B_SPLINE_CURVE(2,(#358954,#358955,#358956,#358957,#358958,#358959,#358960,
#358961,#358962,#358963,#358964,#358965,#358966),.UNSPECIFIED.,.F.,.F.)
B_SPLINE_CURVE_WITH_KNOTS((3,2,2,2,2,2,3),(0.53030303030303,0.535353535353535,
0.54040404040404,0.545454545454545,0.55050505050505,0.555555555555556,0.560606060606061),
 .UNSPECIFIED.)
CURVE()
GEOMETRIC_REPRESENTATION_ITEM()
RATIONAL_B_SPLINE_CURVE((1.,0.866025403784439,1.,0.866025403784439,1.,0.866025403784439,
1.,0.866025403784439,1.,0.866025403784439,1.,0.866025403784439,1.))
REPRESENTATION_ITEM('')
);
#4141=(
BOUNDED_CURVE()
B_SPLINE_CURVE(2,(#358967,#358968,#358969,#358970,#358971,#358972,#358973,
#358974,#358975,#358976,#358977,#358978,#358979),.UNSPECIFIED.,.F.,.F.)
B_SPLINE_CURVE_WITH_KNOTS((3,2,2,2,2,2,3),(0.53030303030303,0.535353535353535,
0.54040404040404,0.545454545454545,0.550505050505051,0.555555555555556,
0.560606060606061),.UNSPECIFIED.)
CURVE()
GEOMETRIC_REPRESENTATION_ITEM()
RATIONAL_B_SPLINE_CURVE((1.,0.866025403784439,1.,0.866025403784439,1.,0.866025403784439,
1.,0.866025403784439,1.,0.866025403784439,1.,0.866025403784439,1.))
REPRESENTATION_ITEM('')
);
#4142=(
BOUNDED_CURVE()
B_SPLINE_CURVE(2,(#358984,#358985,#358986,#358987,#358988,#358989,#358990,
#358991,#358992,#358993,#358994,#358995,#358996),.UNSPECIFIED.,.F.,.F.)
B_SPLINE_CURVE_WITH_KNOTS((3,2,2,2,2,2,3),(0.5,0.505050505050505,0.51010101010101,
0.515151515151515,0.52020202020202,0.525252525252525,0.53030303030303),
 .UNSPECIFIED.)
CURVE()
GEOMETRIC_REPRESENTATION_ITEM()
RATIONAL_B_SPLINE_CURVE((1.,0.866025403784439,1.,0.866025403784439,1.,0.866025403784439,
1.,0.866025403784439,1.,0.866025403784439,1.,0.866025403784439,1.))
REPRESENTATION_ITEM('')
);
#4143=(
BOUNDED_CURVE()
B_SPLINE_CURVE(2,(#358997,#358998,#358999,#359000,#359001,#359002,#359003,
#359004,#359005,#359006,#359007,#359008,#359009),.UNSPECIFIED.,.F.,.F.)
B_SPLINE_CURVE_WITH_KNOTS((3,2,2,2,2,2,3),(0.5,0.505050505050505,0.51010101010101,
0.515151515151515,0.52020202020202,0.525252525252525,0.53030303030303),
 .UNSPECIFIED.)
CURVE()
GEOMETRIC_REPRESENTATION_ITEM()
RATIONAL_B_SPLINE_CURVE((1.,0.866025403784439,1.,0.866025403784439,1.,0.866025403784439,
1.,0.866025403784439,1.,0.866025403784439,1.,0.866025403784439,1.))
REPRESENTATION_ITEM('')
);
#4144=(
BOUNDED_CURVE()
B_SPLINE_CURVE(2,(#359014,#359015,#359016,#359017,#359018,#359019,#359020,
#359021,#359022,#359023,#359024,#359025,#359026),.UNSPECIFIED.,.F.,.F.)
B_SPLINE_CURVE_WITH_KNOTS((3,2,2,2,2,2,3),(0.46969696969697,0.474747474747475,
0.47979797979798,0.484848484848485,0.48989898989899,0.494949494949495,0.5),
 .UNSPECIFIED.)
CURVE()
GEOMETRIC_REPRESENTATION_ITEM()
RATIONAL_B_SPLINE_CURVE((1.,0.866025403784439,1.,0.866025403784439,1.,0.866025403784439,
1.,0.866025403784439,1.,0.866025403784439,1.,0.866025403784439,1.))
REPRESENTATION_ITEM('')
);
#4145=(
BOUNDED_CURVE()
B_SPLINE_CURVE(2,(#359027,#359028,#359029,#359030,#359031,#359032,#359033,
#359034,#359035,#359036,#359037,#359038,#359039),.UNSPECIFIED.,.F.,.F.)
B_SPLINE_CURVE_WITH_KNOTS((3,2,2,2,2,2,3),(0.46969696969697,0.474747474747475,
0.47979797979798,0.484848484848485,0.48989898989899,0.494949494949495,0.5),
 .UNSPECIFIED.)
CURVE()
GEOMETRIC_REPRESENTATION_ITEM()
RATIONAL_B_SPLINE_CURVE((1.,0.866025403784439,1.,0.866025403784439,1.,0.866025403784439,
1.,0.866025403784439,1.,0.866025403784439,1.,0.866025403784439,1.))
REPRESENTATION_ITEM('')
);
#4146=(
BOUNDED_CURVE()
B_SPLINE_CURVE(2,(#359044,#359045,#359046,#359047,#359048,#359049,#359050,
#359051,#359052,#359053,#359054,#359055,#359056),.UNSPECIFIED.,.F.,.F.)
B_SPLINE_CURVE_WITH_KNOTS((3,2,2,2,2,2,3),(0.439393939393939,0.444444444444444,
0.44949494949495,0.454545454545455,0.45959595959596,0.464646464646465,0.46969696969697),
 .UNSPECIFIED.)
CURVE()
GEOMETRIC_REPRESENTATION_ITEM()
RATIONAL_B_SPLINE_CURVE((1.,0.866025403784439,1.,0.866025403784439,1.,0.866025403784439,
1.,0.866025403784439,1.,0.866025403784439,1.,0.866025403784439,1.))
REPRESENTATION_ITEM('')
);
#4147=(
BOUNDED_CURVE()
B_SPLINE_CURVE(2,(#359057,#359058,#359059,#359060,#359061,#359062,#359063,
#359064,#359065,#359066,#359067,#359068,#359069),.UNSPECIFIED.,.F.,.F.)
B_SPLINE_CURVE_WITH_KNOTS((3,2,2,2,2,2,3),(0.439393939393939,0.444444444444444,
0.44949494949495,0.454545454545455,0.45959595959596,0.464646464646465,0.46969696969697),
 .UNSPECIFIED.)
CURVE()
GEOMETRIC_REPRESENTATION_ITEM()
RATIONAL_B_SPLINE_CURVE((1.,0.866025403784439,1.,0.866025403784439,1.,0.866025403784439,
1.,0.866025403784439,1.,0.866025403784439,1.,0.866025403784439,1.))
REPRESENTATION_ITEM('')
);
#4148=(
BOUNDED_CURVE()
B_SPLINE_CURVE(2,(#359074,#359075,#359076,#359077,#359078,#359079,#359080,
#359081,#359082,#359083,#359084,#359085,#359086),.UNSPECIFIED.,.F.,.F.)
B_SPLINE_CURVE_WITH_KNOTS((3,2,2,2,2,2,3),(0.409090909090909,0.414141414141414,
0.419191919191919,0.424242424242424,0.429292929292929,0.434343434343434,
0.439393939393939),.UNSPECIFIED.)
CURVE()
GEOMETRIC_REPRESENTATION_ITEM()
RATIONAL_B_SPLINE_CURVE((1.,0.866025403784439,1.,0.866025403784439,1.,0.866025403784439,
1.,0.866025403784439,1.,0.866025403784439,1.,0.866025403784439,1.))
REPRESENTATION_ITEM('')
);
#4149=(
BOUNDED_CURVE()
B_SPLINE_CURVE(2,(#359087,#359088,#359089,#359090,#359091,#359092,#359093,
#359094,#359095,#359096,#359097,#359098,#359099),.UNSPECIFIED.,.F.,.F.)
B_SPLINE_CURVE_WITH_KNOTS((3,2,2,2,2,2,3),(0.409090909090909,0.414141414141414,
0.419191919191919,0.424242424242424,0.429292929292929,0.434343434343434,
0.439393939393939),.UNSPECIFIED.)
CURVE()
GEOMETRIC_REPRESENTATION_ITEM()
RATIONAL_B_SPLINE_CURVE((1.,0.866025403784439,1.,0.866025403784439,1.,0.866025403784439,
1.,0.866025403784439,1.,0.866025403784439,1.,0.866025403784439,1.))
REPRESENTATION_ITEM('')
);
#4150=(
BOUNDED_CURVE()
B_SPLINE_CURVE(2,(#359104,#359105,#359106,#359107,#359108,#359109,#359110,
#359111,#359112,#359113,#359114,#359115,#359116),.UNSPECIFIED.,.F.,.F.)
B_SPLINE_CURVE_WITH_KNOTS((3,2,2,2,2,2,3),(0.378787878787879,0.383838383838384,
0.388888888888889,0.393939393939394,0.398989898989899,0.404040404040404,
0.409090909090909),.UNSPECIFIED.)
CURVE()
GEOMETRIC_REPRESENTATION_ITEM()
RATIONAL_B_SPLINE_CURVE((1.,0.866025403784439,1.,0.866025403784439,1.,0.866025403784439,
1.,0.866025403784439,1.,0.866025403784439,1.,0.866025403784439,1.))
REPRESENTATION_ITEM('')
);
#4151=(
BOUNDED_CURVE()
B_SPLINE_CURVE(2,(#359117,#359118,#359119,#359120,#359121,#359122,#359123,
#359124,#359125,#359126,#359127,#359128,#359129),.UNSPECIFIED.,.F.,.F.)
B_SPLINE_CURVE_WITH_KNOTS((3,2,2,2,2,2,3),(0.378787878787879,0.383838383838384,
0.388888888888889,0.393939393939394,0.398989898989899,0.404040404040404,
0.409090909090909),.UNSPECIFIED.)
CURVE()
GEOMETRIC_REPRESENTATION_ITEM()
RATIONAL_B_SPLINE_CURVE((1.,0.866025403784439,1.,0.866025403784439,1.,0.866025403784439,
1.,0.866025403784439,1.,0.866025403784439,1.,0.866025403784439,1.))
REPRESENTATION_ITEM('')
);
#4152=(
BOUNDED_CURVE()
B_SPLINE_CURVE(2,(#359134,#359135,#359136,#359137,#359138,#359139,#359140,
#359141,#359142,#359143,#359144,#359145,#359146),.UNSPECIFIED.,.F.,.F.)
B_SPLINE_CURVE_WITH_KNOTS((3,2,2,2,2,2,3),(0.348484848484849,0.353535353535354,
0.358585858585859,0.363636363636364,0.368686868686869,0.373737373737374,
0.378787878787879),.UNSPECIFIED.)
CURVE()
GEOMETRIC_REPRESENTATION_ITEM()
RATIONAL_B_SPLINE_CURVE((1.,0.866025403784439,1.,0.866025403784439,1.,0.866025403784439,
1.,0.866025403784439,1.,0.866025403784439,1.,0.866025403784439,1.))
REPRESENTATION_ITEM('')
);
#4153=(
BOUNDED_CURVE()
B_SPLINE_CURVE(2,(#359147,#359148,#359149,#359150,#359151,#359152,#359153,
#359154,#359155,#359156,#359157,#359158,#359159),.UNSPECIFIED.,.F.,.F.)
B_SPLINE_CURVE_WITH_KNOTS((3,2,2,2,2,2,3),(0.348484848484849,0.353535353535354,
0.358585858585859,0.363636363636364,0.368686868686869,0.373737373737374,
0.378787878787879),.UNSPECIFIED.)
CURVE()
GEOMETRIC_REPRESENTATION_ITEM()
RATIONAL_B_SPLINE_CURVE((1.,0.866025403784439,1.,0.866025403784439,1.,0.866025403784439,
1.,0.866025403784439,1.,0.866025403784439,1.,0.866025403784439,1.))
REPRESENTATION_ITEM('')
);
#4154=(
BOUNDED_CURVE()
B_SPLINE_CURVE(2,(#359164,#359165,#359166,#359167,#359168,#359169,#359170,
#359171,#359172,#359173,#359174,#359175,#359176),.UNSPECIFIED.,.F.,.F.)
B_SPLINE_CURVE_WITH_KNOTS((3,2,2,2,2,2,3),(0.318181818181818,0.323232323232323,
0.328282828282828,0.333333333333333,0.338383838383838,0.343434343434343,
0.348484848484849),.UNSPECIFIED.)
CURVE()
GEOMETRIC_REPRESENTATION_ITEM()
RATIONAL_B_SPLINE_CURVE((1.,0.866025403784439,1.,0.866025403784439,1.,0.866025403784439,
1.,0.866025403784439,1.,0.866025403784439,1.,0.866025403784439,1.))
REPRESENTATION_ITEM('')
);
#4155=(
BOUNDED_CURVE()
B_SPLINE_CURVE(2,(#359177,#359178,#359179,#359180,#359181,#359182,#359183,
#359184,#359185,#359186,#359187,#359188,#359189),.UNSPECIFIED.,.F.,.F.)
B_SPLINE_CURVE_WITH_KNOTS((3,2,2,2,2,2,3),(0.318181818181818,0.323232323232323,
0.328282828282828,0.333333333333333,0.338383838383838,0.343434343434343,
0.348484848484849),.UNSPECIFIED.)
CURVE()
GEOMETRIC_REPRESENTATION_ITEM()
RATIONAL_B_SPLINE_CURVE((1.,0.866025403784439,1.,0.866025403784439,1.,0.866025403784439,
1.,0.866025403784439,1.,0.866025403784439,1.,0.866025403784439,1.))
REPRESENTATION_ITEM('')
);
#4156=(
BOUNDED_CURVE()
B_SPLINE_CURVE(2,(#359194,#359195,#359196,#359197,#359198,#359199,#359200,
#359201,#359202,#359203,#359204,#359205,#359206),.UNSPECIFIED.,.F.,.F.)
B_SPLINE_CURVE_WITH_KNOTS((3,2,2,2,2,2,3),(0.287878787878788,0.292929292929293,
0.297979797979798,0.303030303030303,0.308080808080808,0.313131313131313,
0.318181818181818),.UNSPECIFIED.)
CURVE()
GEOMETRIC_REPRESENTATION_ITEM()
RATIONAL_B_SPLINE_CURVE((1.,0.866025403784439,1.,0.866025403784439,1.,0.866025403784439,
1.,0.866025403784439,1.,0.866025403784439,1.,0.866025403784439,1.))
REPRESENTATION_ITEM('')
);
#4157=(
BOUNDED_CURVE()
B_SPLINE_CURVE(2,(#359207,#359208,#359209,#359210,#359211,#359212,#359213,
#359214,#359215,#359216,#359217,#359218,#359219),.UNSPECIFIED.,.F.,.F.)
B_SPLINE_CURVE_WITH_KNOTS((3,2,2,2,2,2,3),(0.287878787878788,0.292929292929293,
0.297979797979798,0.303030303030303,0.308080808080808,0.313131313131313,
0.318181818181818),.UNSPECIFIED.)
CURVE()
GEOMETRIC_REPRESENTATION_ITEM()
RATIONAL_B_SPLINE_CURVE((1.,0.866025403784439,1.,0.866025403784439,1.,0.866025403784439,
1.,0.866025403784439,1.,0.866025403784439,1.,0.866025403784439,1.))
REPRESENTATION_ITEM('')
);
#4158=(
BOUNDED_CURVE()
B_SPLINE_CURVE(2,(#359224,#359225,#359226,#359227,#359228,#359229,#359230,
#359231,#359232,#359233,#359234,#359235,#359236),.UNSPECIFIED.,.F.,.F.)
B_SPLINE_CURVE_WITH_KNOTS((3,2,2,2,2,2,3),(0.257575757575758,0.262626262626263,
0.267676767676768,0.272727272727273,0.277777777777778,0.282828282828283,
0.287878787878788),.UNSPECIFIED.)
CURVE()
GEOMETRIC_REPRESENTATION_ITEM()
RATIONAL_B_SPLINE_CURVE((1.,0.866025403784439,1.,0.866025403784439,1.,0.866025403784439,
1.,0.866025403784439,1.,0.866025403784439,1.,0.866025403784439,1.))
REPRESENTATION_ITEM('')
);
#4159=(
BOUNDED_CURVE()
B_SPLINE_CURVE(2,(#359237,#359238,#359239,#359240,#359241,#359242,#359243,
#359244,#359245,#359246,#359247,#359248,#359249),.UNSPECIFIED.,.F.,.F.)
B_SPLINE_CURVE_WITH_KNOTS((3,2,2,2,2,2,3),(0.257575757575758,0.262626262626263,
0.267676767676768,0.272727272727273,0.277777777777778,0.282828282828283,
0.287878787878788),.UNSPECIFIED.)
CURVE()
GEOMETRIC_REPRESENTATION_ITEM()
RATIONAL_B_SPLINE_CURVE((1.,0.866025403784439,1.,0.866025403784439,1.,0.866025403784439,
1.,0.866025403784439,1.,0.866025403784439,1.,0.866025403784439,1.))
REPRESENTATION_ITEM('')
);
#4160=(
BOUNDED_CURVE()
B_SPLINE_CURVE(2,(#359254,#359255,#359256,#359257,#359258,#359259,#359260,
#359261,#359262,#359263,#359264,#359265,#359266),.UNSPECIFIED.,.F.,.F.)
B_SPLINE_CURVE_WITH_KNOTS((3,2,2,2,2,2,3),(0.227272727272727,0.232323232323232,
0.237373737373737,0.242424242424242,0.247474747474747,0.252525252525253,
0.257575757575758),.UNSPECIFIED.)
CURVE()
GEOMETRIC_REPRESENTATION_ITEM()
RATIONAL_B_SPLINE_CURVE((1.,0.866025403784439,1.,0.866025403784439,1.,0.866025403784439,
1.,0.866025403784439,1.,0.866025403784439,1.,0.866025403784439,1.))
REPRESENTATION_ITEM('')
);
#4161=(
BOUNDED_CURVE()
B_SPLINE_CURVE(2,(#359267,#359268,#359269,#359270,#359271,#359272,#359273,
#359274,#359275,#359276,#359277,#359278,#359279),.UNSPECIFIED.,.F.,.F.)
B_SPLINE_CURVE_WITH_KNOTS((3,2,2,2,2,2,3),(0.227272727272727,0.232323232323232,
0.237373737373737,0.242424242424242,0.247474747474747,0.252525252525253,
0.257575757575758),.UNSPECIFIED.)
CURVE()
GEOMETRIC_REPRESENTATION_ITEM()
RATIONAL_B_SPLINE_CURVE((1.,0.866025403784439,1.,0.866025403784439,1.,0.866025403784439,
1.,0.866025403784439,1.,0.866025403784439,1.,0.866025403784439,1.))
REPRESENTATION_ITEM('')
);
#4162=(
BOUNDED_CURVE()
B_SPLINE_CURVE(2,(#359284,#359285,#359286,#359287,#359288,#359289,#359290,
#359291,#359292,#359293,#359294,#359295,#359296),.UNSPECIFIED.,.F.,.F.)
B_SPLINE_CURVE_WITH_KNOTS((3,2,2,2,2,2,3),(0.196969696969697,0.202020202020202,
0.207070707070707,0.212121212121212,0.217171717171717,0.222222222222222,
0.227272727272727),.UNSPECIFIED.)
CURVE()
GEOMETRIC_REPRESENTATION_ITEM()
RATIONAL_B_SPLINE_CURVE((1.,0.866025403784439,1.,0.866025403784439,1.,0.866025403784439,
1.,0.866025403784439,1.,0.866025403784439,1.,0.866025403784439,1.))
REPRESENTATION_ITEM('')
);
#4163=(
BOUNDED_CURVE()
B_SPLINE_CURVE(2,(#359297,#359298,#359299,#359300,#359301,#359302,#359303,
#359304,#359305,#359306,#359307,#359308,#359309),.UNSPECIFIED.,.F.,.F.)
B_SPLINE_CURVE_WITH_KNOTS((3,2,2,2,2,2,3),(0.196969696969697,0.202020202020202,
0.207070707070707,0.212121212121212,0.217171717171717,0.222222222222222,
0.227272727272727),.UNSPECIFIED.)
CURVE()
GEOMETRIC_REPRESENTATION_ITEM()
RATIONAL_B_SPLINE_CURVE((1.,0.866025403784439,1.,0.866025403784439,1.,0.866025403784439,
1.,0.866025403784439,1.,0.866025403784439,1.,0.866025403784439,1.))
REPRESENTATION_ITEM('')
);
#4164=(
BOUNDED_CURVE()
B_SPLINE_CURVE(2,(#359314,#359315,#359316,#359317,#359318,#359319,#359320,
#359321,#359322,#359323,#359324,#359325,#359326),.UNSPECIFIED.,.F.,.F.)
B_SPLINE_CURVE_WITH_KNOTS((3,2,2,2,2,2,3),(0.166666666666667,0.171717171717172,
0.176767676767677,0.181818181818182,0.186868686868687,0.191919191919192,
0.196969696969697),.UNSPECIFIED.)
CURVE()
GEOMETRIC_REPRESENTATION_ITEM()
RATIONAL_B_SPLINE_CURVE((1.,0.866025403784439,1.,0.866025403784439,1.,0.866025403784439,
1.,0.866025403784439,1.,0.866025403784439,1.,0.866025403784439,1.))
REPRESENTATION_ITEM('')
);
#4165=(
BOUNDED_CURVE()
B_SPLINE_CURVE(2,(#359327,#359328,#359329,#359330,#359331,#359332,#359333,
#359334,#359335,#359336,#359337,#359338,#359339),.UNSPECIFIED.,.F.,.F.)
B_SPLINE_CURVE_WITH_KNOTS((3,2,2,2,2,2,3),(0.166666666666667,0.171717171717172,
0.176767676767677,0.181818181818182,0.186868686868687,0.191919191919192,
0.196969696969697),.UNSPECIFIED.)
CURVE()
GEOMETRIC_REPRESENTATION_ITEM()
RATIONAL_B_SPLINE_CURVE((1.,0.866025403784439,1.,0.866025403784439,1.,0.866025403784439,
1.,0.866025403784439,1.,0.866025403784439,1.,0.866025403784439,1.))
REPRESENTATION_ITEM('')
);
#4166=(
BOUNDED_CURVE()
B_SPLINE_CURVE(2,(#359344,#359345,#359346,#359347,#359348,#359349,#359350,
#359351,#359352,#359353,#359354,#359355,#359356),.UNSPECIFIED.,.F.,.F.)
B_SPLINE_CURVE_WITH_KNOTS((3,2,2,2,2,2,3),(0.136363636363636,0.141414141414141,
0.146464646464646,0.151515151515151,0.156565656565657,0.161616161616162,
0.166666666666667),.UNSPECIFIED.)
CURVE()
GEOMETRIC_REPRESENTATION_ITEM()
RATIONAL_B_SPLINE_CURVE((1.,0.866025403784439,1.,0.866025403784439,1.,0.866025403784439,
1.,0.866025403784439,1.,0.866025403784439,1.,0.866025403784439,1.))
REPRESENTATION_ITEM('')
);
#4167=(
BOUNDED_CURVE()
B_SPLINE_CURVE(2,(#359357,#359358,#359359,#359360,#359361,#359362,#359363,
#359364,#359365,#359366,#359367,#359368,#359369),.UNSPECIFIED.,.F.,.F.)
B_SPLINE_CURVE_WITH_KNOTS((3,2,2,2,2,2,3),(0.136363636363636,0.141414141414141,
0.146464646464646,0.151515151515152,0.156565656565657,0.161616161616162,
0.166666666666667),.UNSPECIFIED.)
CURVE()
GEOMETRIC_REPRESENTATION_ITEM()
RATIONAL_B_SPLINE_CURVE((1.,0.866025403784439,1.,0.866025403784439,1.,0.866025403784439,
1.,0.866025403784439,1.,0.866025403784439,1.,0.866025403784439,1.))
REPRESENTATION_ITEM('')
);
#4168=(
BOUNDED_CURVE()
B_SPLINE_CURVE(2,(#359374,#359375,#359376,#359377,#359378,#359379,#359380,
#359381,#359382,#359383,#359384,#359385,#359386),.UNSPECIFIED.,.F.,.F.)
B_SPLINE_CURVE_WITH_KNOTS((3,2,2,2,2,2,3),(0.106060606060606,0.111111111111111,
0.116161616161616,0.121212121212121,0.126262626262626,0.131313131313131,
0.136363636363636),.UNSPECIFIED.)
CURVE()
GEOMETRIC_REPRESENTATION_ITEM()
RATIONAL_B_SPLINE_CURVE((1.,0.866025403784439,1.,0.866025403784439,1.,0.866025403784439,
1.,0.866025403784439,1.,0.866025403784439,1.,0.866025403784439,1.))
REPRESENTATION_ITEM('')
);
#4169=(
BOUNDED_CURVE()
B_SPLINE_CURVE(2,(#359387,#359388,#359389,#359390,#359391,#359392,#359393,
#359394,#359395,#359396,#359397,#359398,#359399),.UNSPECIFIED.,.F.,.F.)
B_SPLINE_CURVE_WITH_KNOTS((3,2,2,2,2,2,3),(0.106060606060606,0.111111111111111,
0.116161616161616,0.121212121212121,0.126262626262626,0.131313131313131,
0.136363636363636),.UNSPECIFIED.)
CURVE()
GEOMETRIC_REPRESENTATION_ITEM()
RATIONAL_B_SPLINE_CURVE((1.,0.866025403784439,1.,0.866025403784439,1.,0.866025403784439,
1.,0.866025403784439,1.,0.866025403784439,1.,0.866025403784439,1.))
REPRESENTATION_ITEM('')
);
#4170=(
BOUNDED_CURVE()
B_SPLINE_CURVE(2,(#359404,#359405,#359406,#359407,#359408,#359409,#359410,
#359411,#359412,#359413,#359414,#359415,#359416),.UNSPECIFIED.,.F.,.F.)
B_SPLINE_CURVE_WITH_KNOTS((3,2,2,2,2,2,3),(0.0757575757575758,0.0808080808080808,
0.0858585858585859,0.0909090909090909,0.095959595959596,0.101010101010101,
0.106060606060606),.UNSPECIFIED.)
CURVE()
GEOMETRIC_REPRESENTATION_ITEM()
RATIONAL_B_SPLINE_CURVE((1.,0.866025403784439,1.,0.866025403784439,1.,0.866025403784439,
1.,0.866025403784439,1.,0.866025403784439,1.,0.866025403784439,1.))
REPRESENTATION_ITEM('')
);
#4171=(
BOUNDED_CURVE()
B_SPLINE_CURVE(2,(#359417,#359418,#359419,#359420,#359421,#359422,#359423,
#359424,#359425,#359426,#359427,#359428,#359429),.UNSPECIFIED.,.F.,.F.)
B_SPLINE_CURVE_WITH_KNOTS((3,2,2,2,2,2,3),(0.0757575757575758,0.0808080808080808,
0.0858585858585859,0.0909090909090909,0.095959595959596,0.101010101010101,
0.106060606060606),.UNSPECIFIED.)
CURVE()
GEOMETRIC_REPRESENTATION_ITEM()
RATIONAL_B_SPLINE_CURVE((1.,0.866025403784439,1.,0.866025403784439,1.,0.866025403784439,
1.,0.866025403784439,1.,0.866025403784439,1.,0.866025403784439,1.))
REPRESENTATION_ITEM('')
);
#4172=(
BOUNDED_CURVE()
B_SPLINE_CURVE(2,(#359434,#359435,#359436,#359437,#359438,#359439,#359440,
#359441,#359442,#359443,#359444,#359445,#359446),.UNSPECIFIED.,.F.,.F.)
B_SPLINE_CURVE_WITH_KNOTS((3,2,2,2,2,2,3),(0.0454545454545455,0.0505050505050505,
0.0555555555555556,0.0606060606060606,0.0656565656565657,0.0707070707070707,
0.0757575757575758),.UNSPECIFIED.)
CURVE()
GEOMETRIC_REPRESENTATION_ITEM()
RATIONAL_B_SPLINE_CURVE((1.,0.866025403784439,1.,0.866025403784439,1.,0.866025403784439,
1.,0.866025403784439,1.,0.866025403784439,1.,0.866025403784439,1.))
REPRESENTATION_ITEM('')
);
#4173=(
BOUNDED_CURVE()
B_SPLINE_CURVE(2,(#359447,#359448,#359449,#359450,#359451,#359452,#359453,
#359454,#359455,#359456,#359457,#359458,#359459),.UNSPECIFIED.,.F.,.F.)
B_SPLINE_CURVE_WITH_KNOTS((3,2,2,2,2,2,3),(0.0454545454545455,0.0505050505050505,
0.0555555555555556,0.0606060606060606,0.0656565656565657,0.0707070707070707,
0.0757575757575758),.UNSPECIFIED.)
CURVE()
GEOMETRIC_REPRESENTATION_ITEM()
RATIONAL_B_SPLINE_CURVE((1.,0.866025403784439,1.,0.866025403784439,1.,0.866025403784439,
1.,0.866025403784439,1.,0.866025403784439,1.,0.866025403784439,1.))
REPRESENTATION_ITEM('')
);
#4174=(
BOUNDED_CURVE()
B_SPLINE_CURVE(2,(#359466,#359467,#359468,#359469,#359470,#359471,#359472,
#359473,#359474,#359475,#359476,#359477,#359478),.UNSPECIFIED.,.F.,.F.)
B_SPLINE_CURVE_WITH_KNOTS((3,2,2,2,2,2,3),(0.0181628739236012,0.0202020202020202,
0.0252525252525253,0.0303030303030303,0.0353535353535354,0.0404040404040404,
0.0454545454545455),.UNSPECIFIED.)
CURVE()
GEOMETRIC_REPRESENTATION_ITEM()
RATIONAL_B_SPLINE_CURVE((0.935494950279675,0.945907627743422,1.,0.866025403784439,
1.,0.866025403784439,1.,0.866025403784439,1.,0.866025403784439,1.,0.866025403784439,
1.))
REPRESENTATION_ITEM('')
);
#4175=(
BOUNDED_CURVE()
B_SPLINE_CURVE(2,(#359479,#359480,#359481,#359482,#359483,#359484,#359485,
#359486,#359487,#359488,#359489,#359490,#359491),.UNSPECIFIED.,.F.,.F.)
B_SPLINE_CURVE_WITH_KNOTS((3,2,2,2,2,2,3),(0.0151515151515152,0.0202020202020202,
0.0252525252525253,0.0303030303030303,0.0353535353535354,0.0404040404040404,
0.0454545454545455),.UNSPECIFIED.)
CURVE()
GEOMETRIC_REPRESENTATION_ITEM()
RATIONAL_B_SPLINE_CURVE((1.,0.866025403784439,1.,0.866025403784439,1.,0.866025403784439,
1.,0.866025403784439,1.,0.866025403784439,1.,0.866025403784439,1.))
REPRESENTATION_ITEM('')
);
#4176=(
BOUNDED_CURVE()
B_SPLINE_CURVE(2,(#359497,#359498,#359499,#359500,#359501,#359502,#359503),
 .UNSPECIFIED.,.F.,.F.)
B_SPLINE_CURVE_WITH_KNOTS((3,2,2,3),(0.954545454545455,0.95959595959596,
0.964646464646465,0.96969696969697),.UNSPECIFIED.)
CURVE()
GEOMETRIC_REPRESENTATION_ITEM()
RATIONAL_B_SPLINE_CURVE((1.,0.866025403784439,1.,0.866025403784439,1.,0.866025403784439,
1.))
REPRESENTATION_ITEM('')
);
#4177=(
BOUNDED_CURVE()
B_SPLINE_CURVE(2,(#361825,#361826,#361827),.UNSPECIFIED.,.F.,.F.)
B_SPLINE_CURVE_WITH_KNOTS((3,3),(0.124274873543865,0.321867155116299),
 .UNSPECIFIED.)
CURVE()
GEOMETRIC_REPRESENTATION_ITEM()
RATIONAL_B_SPLINE_CURVE((1.46410161513778,1.69059892324148,1.46410161513778))
REPRESENTATION_ITEM('')
);
#4178=(
BOUNDED_CURVE()
B_SPLINE_CURVE(2,(#361924,#361925,#361926,#361927,#361928,#361929,#361930),
 .UNSPECIFIED.,.F.,.F.)
B_SPLINE_CURVE_WITH_KNOTS((3,2,2,3),(0.0491768500135387,0.0505050505050505,
0.0555555555555556,0.0606060606060607),.UNSPECIFIED.)
CURVE()
GEOMETRIC_REPRESENTATION_ITEM()
RATIONAL_B_SPLINE_CURVE((0.948065210722613,0.964766865340365,1.,0.866025403784439,
1.,0.866025403784437,1.))
REPRESENTATION_ITEM('')
);
#4179=(
BOUNDED_CURVE()
B_SPLINE_CURVE(2,(#362007,#362008,#362009),.UNSPECIFIED.,.F.,.F.)
B_SPLINE_CURVE_WITH_KNOTS((3,3),(-0.3218671551163,-0.124274873543866),
 .UNSPECIFIED.)
CURVE()
GEOMETRIC_REPRESENTATION_ITEM()
RATIONAL_B_SPLINE_CURVE((1.46410161513778,1.69059892324148,1.46410161513778))
REPRESENTATION_ITEM('')
);
#4180=(
BOUNDED_CURVE()
B_SPLINE_CURVE(2,(#362011,#362012,#362013),.UNSPECIFIED.,.F.,.F.)
B_SPLINE_CURVE_WITH_KNOTS((3,3),(-0.321867155116299,-0.124274873543865),
 .UNSPECIFIED.)
CURVE()
GEOMETRIC_REPRESENTATION_ITEM()
RATIONAL_B_SPLINE_CURVE((1.46410161513778,1.69059892324148,1.46410161513778))
REPRESENTATION_ITEM('')
);
#4181=(
BOUNDED_CURVE()
B_SPLINE_CURVE(2,(#362015,#362016,#362017),.UNSPECIFIED.,.F.,.F.)
B_SPLINE_CURVE_WITH_KNOTS((3,3),(-0.321867155116299,-0.124274873543865),
 .UNSPECIFIED.)
CURVE()
GEOMETRIC_REPRESENTATION_ITEM()
RATIONAL_B_SPLINE_CURVE((1.46410161513778,1.69059892324148,1.46410161513778))
REPRESENTATION_ITEM('')
);
#4182=(
BOUNDED_CURVE()
B_SPLINE_CURVE(2,(#362019,#362020,#362021),.UNSPECIFIED.,.F.,.F.)
B_SPLINE_CURVE_WITH_KNOTS((3,3),(-0.321867155116299,-0.124274873543865),
 .UNSPECIFIED.)
CURVE()
GEOMETRIC_REPRESENTATION_ITEM()
RATIONAL_B_SPLINE_CURVE((1.46410161513778,1.69059892324148,1.46410161513778))
REPRESENTATION_ITEM('')
);
#4183=(
BOUNDED_CURVE()
B_SPLINE_CURVE(2,(#362023,#362024,#362025),.UNSPECIFIED.,.F.,.F.)
B_SPLINE_CURVE_WITH_KNOTS((3,3),(-0.321867155116299,-0.124274873543865),
 .UNSPECIFIED.)
CURVE()
GEOMETRIC_REPRESENTATION_ITEM()
RATIONAL_B_SPLINE_CURVE((1.46410161513778,1.69059892324148,1.46410161513778))
REPRESENTATION_ITEM('')
);
#4184=(
BOUNDED_CURVE()
B_SPLINE_CURVE(2,(#362846,#362847,#362848),.UNSPECIFIED.,.F.,.F.)
B_SPLINE_CURVE_WITH_KNOTS((3,3),(0.0143443920644589,0.0151515151515152),
 .UNSPECIFIED.)
CURVE()
GEOMETRIC_REPRESENTATION_ITEM()
RATIONAL_B_SPLINE_CURVE((0.964022189566691,0.978589470042445,1.))
REPRESENTATION_ITEM('')
);
#4414=SHAPE_REPRESENTATION_RELATIONSHIP('SRR','None',#459340,#4435);
#4435=ADVANCED_BREP_SHAPE_REPRESENTATION('',(#4467),#459229);
#4467=MANIFOLD_SOLID_BREP('Body1',#94645);
#4587=STYLED_ITEM('',(#459533),#4467);
#4877=CONICAL_SURFACE('',#99119,1.15470053837925,0.78539816339745);
#4878=CONICAL_SURFACE('',#99127,1.125,0.785398163397447);
#4879=CONICAL_SURFACE('',#99141,1.15470053837925,0.78539816339745);
#4880=CONICAL_SURFACE('',#99142,1.15470053837925,0.78539816339745);
#4881=CONICAL_SURFACE('',#99143,1.15470053837925,0.78539816339745);
#4882=CONICAL_SURFACE('',#99144,1.15470053837925,0.78539816339745);
#4883=CONICAL_SURFACE('',#99145,1.15470053837925,0.78539816339745);
#5209=FACE_BOUND('',#14282,.T.);
#5210=FACE_BOUND('',#14288,.T.);
#5211=FACE_BOUND('',#14290,.T.);
#5212=FACE_BOUND('',#14292,.T.);
#5684=PLANE('',#99132);
#5685=PLANE('',#99133);
#5686=PLANE('',#99134);
#5687=PLANE('',#99135);
#5688=PLANE('',#99146);
#5689=PLANE('',#99147);
#5690=PLANE('',#99148);
#5691=PLANE('',#99149);
#5692=PLANE('',#99150);
#5693=PLANE('',#99151);
#5694=PLANE('',#99152);
#8313=FACE_OUTER_BOUND('',#14217,.T.);
#8314=FACE_OUTER_BOUND('',#14218,.T.);
#8315=FACE_OUTER_BOUND('',#14219,.T.);
#8316=FACE_OUTER_BOUND('',#14220,.T.);
#8317=FACE_OUTER_BOUND('',#14221,.T.);
#8318=FACE_OUTER_BOUND('',#14222,.T.);
#8319=FACE_OUTER_BOUND('',#14223,.T.);
#8320=FACE_OUTER_BOUND('',#14224,.T.);
#8321=FACE_OUTER_BOUND('',#14225,.T.);
#8322=FACE_OUTER_BOUND('',#14226,.T.);
#8323=FACE_OUTER_BOUND('',#14227,.T.);
#8324=FACE_OUTER_BOUND('',#14228,.T.);
#8325=FACE_OUTER_BOUND('',#14229,.T.);
#8326=FACE_OUTER_BOUND('',#14230,.T.);
#8327=FACE_OUTER_BOUND('',#14231,.T.);
#8328=FACE_OUTER_BOUND('',#14232,.T.);
#8329=FACE_OUTER_BOUND('',#14233,.T.);
#8330=FACE_OUTER_BOUND('',#14234,.T.);
#8331=FACE_OUTER_BOUND('',#14235,.T.);
#8332=FACE_OUTER_BOUND('',#14236,.T.);
#8333=FACE_OUTER_BOUND('',#14237,.T.);
#8334=FACE_OUTER_BOUND('',#14238,.T.);
#8335=FACE_OUTER_BOUND('',#14239,.T.);
#8336=FACE_OUTER_BOUND('',#14240,.T.);
#8337=FACE_OUTER_BOUND('',#14241,.T.);
#8338=FACE_OUTER_BOUND('',#14242,.T.);
#8339=FACE_OUTER_BOUND('',#14243,.T.);
#8340=FACE_OUTER_BOUND('',#14244,.T.);
#8341=FACE_OUTER_BOUND('',#14245,.T.);
#8342=FACE_OUTER_BOUND('',#14246,.T.);
#8343=FACE_OUTER_BOUND('',#14247,.T.);
#8344=FACE_OUTER_BOUND('',#14248,.T.);
#8345=FACE_OUTER_BOUND('',#14249,.T.);
#8346=FACE_OUTER_BOUND('',#14250,.T.);
#8347=FACE_OUTER_BOUND('',#14251,.T.);
#8348=FACE_OUTER_BOUND('',#14252,.T.);
#8349=FACE_OUTER_BOUND('',#14253,.T.);
#8350=FACE_OUTER_BOUND('',#14254,.T.);
#8351=FACE_OUTER_BOUND('',#14255,.T.);
#8352=FACE_OUTER_BOUND('',#14256,.T.);
#8353=FACE_OUTER_BOUND('',#14257,.T.);
#8354=FACE_OUTER_BOUND('',#14258,.T.);
#8355=FACE_OUTER_BOUND('',#14259,.T.);
#8356=FACE_OUTER_BOUND('',#14260,.T.);
#8357=FACE_OUTER_BOUND('',#14261,.T.);
#8358=FACE_OUTER_BOUND('',#14262,.T.);
#8359=FACE_OUTER_BOUND('',#14263,.T.);
#8360=FACE_OUTER_BOUND('',#14264,.T.);
#8361=FACE_OUTER_BOUND('',#14265,.T.);
#8362=FACE_OUTER_BOUND('',#14266,.T.);
#8363=FACE_OUTER_BOUND('',#14267,.T.);
#8364=FACE_OUTER_BOUND('',#14268,.T.);
#8365=FACE_OUTER_BOUND('',#14269,.T.);
#8366=FACE_OUTER_BOUND('',#14270,.T.);
#8367=FACE_OUTER_BOUND('',#14271,.T.);
#8368=FACE_OUTER_BOUND('',#14272,.T.);
#8369=FACE_OUTER_BOUND('',#14273,.T.);
#8370=FACE_OUTER_BOUND('',#14274,.T.);
#8371=FACE_OUTER_BOUND('',#14275,.T.);
#8372=FACE_OUTER_BOUND('',#14276,.T.);
#8373=FACE_OUTER_BOUND('',#14277,.T.);
#8374=FACE_OUTER_BOUND('',#14278,.T.);
#8375=FACE_OUTER_BOUND('',#14279,.T.);
#8376=FACE_OUTER_BOUND('',#14280,.T.);
#8377=FACE_OUTER_BOUND('',#14281,.T.);
#8378=FACE_OUTER_BOUND('',#14283,.T.);
#8379=FACE_OUTER_BOUND('',#14284,.T.);
#8380=FACE_OUTER_BOUND('',#14285,.T.);
#8381=FACE_OUTER_BOUND('',#14286,.T.);
#8382=FACE_OUTER_BOUND('',#14287,.T.);
#8383=FACE_OUTER_BOUND('',#14289,.T.);
#8384=FACE_OUTER_BOUND('',#14291,.T.);
#8385=FACE_OUTER_BOUND('',#14293,.T.);
#8386=FACE_OUTER_BOUND('',#14294,.T.);
#8387=FACE_OUTER_BOUND('',#14295,.T.);
#8388=FACE_OUTER_BOUND('',#14296,.T.);
#8389=FACE_OUTER_BOUND('',#14297,.T.);
#8390=FACE_OUTER_BOUND('',#14298,.T.);
#8391=FACE_OUTER_BOUND('',#14299,.T.);
#8392=FACE_OUTER_BOUND('',#14300,.T.);
#8393=FACE_OUTER_BOUND('',#14301,.T.);
#8394=FACE_OUTER_BOUND('',#14302,.T.);
#8395=FACE_OUTER_BOUND('',#14303,.T.);
#8396=FACE_OUTER_BOUND('',#14304,.T.);
#8397=FACE_OUTER_BOUND('',#14305,.T.);
#8398=FACE_OUTER_BOUND('',#14306,.T.);
#8399=FACE_OUTER_BOUND('',#14307,.T.);
#14217=EDGE_LOOP('',(#68770,#68771,#68772,#68773));
#14218=EDGE_LOOP('',(#68774,#68775,#68776,#68777));
#14219=EDGE_LOOP('',(#68778,#68779,#68780,#68781));
#14220=EDGE_LOOP('',(#68782,#68783,#68784,#68785));
#14221=EDGE_LOOP('',(#68786,#68787,#68788,#68789));
#14222=EDGE_LOOP('',(#68790,#68791,#68792,#68793));
#14223=EDGE_LOOP('',(#68794,#68795,#68796,#68797));
#14224=EDGE_LOOP('',(#68798,#68799,#68800,#68801));
#14225=EDGE_LOOP('',(#68802,#68803,#68804,#68805));
#14226=EDGE_LOOP('',(#68806,#68807,#68808,#68809));
#14227=EDGE_LOOP('',(#68810,#68811,#68812,#68813));
#14228=EDGE_LOOP('',(#68814,#68815,#68816,#68817));
#14229=EDGE_LOOP('',(#68818,#68819,#68820,#68821));
#14230=EDGE_LOOP('',(#68822,#68823,#68824,#68825));
#14231=EDGE_LOOP('',(#68826,#68827,#68828,#68829));
#14232=EDGE_LOOP('',(#68830,#68831,#68832,#68833));
#14233=EDGE_LOOP('',(#68834,#68835,#68836,#68837));
#14234=EDGE_LOOP('',(#68838,#68839,#68840,#68841));
#14235=EDGE_LOOP('',(#68842,#68843,#68844,#68845));
#14236=EDGE_LOOP('',(#68846,#68847,#68848,#68849));
#14237=EDGE_LOOP('',(#68850,#68851,#68852,#68853));
#14238=EDGE_LOOP('',(#68854,#68855,#68856,#68857));
#14239=EDGE_LOOP('',(#68858,#68859,#68860,#68861));
#14240=EDGE_LOOP('',(#68862,#68863,#68864,#68865));
#14241=EDGE_LOOP('',(#68866,#68867,#68868,#68869));
#14242=EDGE_LOOP('',(#68870,#68871,#68872,#68873));
#14243=EDGE_LOOP('',(#68874,#68875,#68876,#68877));
#14244=EDGE_LOOP('',(#68878,#68879,#68880,#68881));
#14245=EDGE_LOOP('',(#68882,#68883,#68884,#68885));
#14246=EDGE_LOOP('',(#68886,#68887,#68888,#68889));
#14247=EDGE_LOOP('',(#68890,#68891,#68892,#68893));
#14248=EDGE_LOOP('',(#68894,#68895,#68896,#68897,#68898));
#14249=EDGE_LOOP('',(#68899,#68900,#68901,#68902));
#14250=EDGE_LOOP('',(#68903,#68904,#68905,#68906));
#14251=EDGE_LOOP('',(#68907,#68908,#68909,#68910));
#14252=EDGE_LOOP('',(#68911,#68912,#68913,#68914));
#14253=EDGE_LOOP('',(#68915,#68916,#68917,#68918));
#14254=EDGE_LOOP('',(#68919,#68920,#68921,#68922));
#14255=EDGE_LOOP('',(#68923,#68924,#68925,#68926));
#14256=EDGE_LOOP('',(#68927,#68928,#68929,#68930));
#14257=EDGE_LOOP('',(#68931,#68932,#68933,#68934));
#14258=EDGE_LOOP('',(#68935,#68936,#68937,#68938));
#14259=EDGE_LOOP('',(#68939,#68940,#68941,#68942));
#14260=EDGE_LOOP('',(#68943,#68944,#68945,#68946));
#14261=EDGE_LOOP('',(#68947,#68948,#68949,#68950));
#14262=EDGE_LOOP('',(#68951,#68952,#68953,#68954));
#14263=EDGE_LOOP('',(#68955,#68956,#68957,#68958));
#14264=EDGE_LOOP('',(#68959,#68960,#68961,#68962));
#14265=EDGE_LOOP('',(#68963,#68964,#68965,#68966));
#14266=EDGE_LOOP('',(#68967,#68968,#68969,#68970));
#14267=EDGE_LOOP('',(#68971,#68972,#68973,#68974));
#14268=EDGE_LOOP('',(#68975,#68976,#68977,#68978));
#14269=EDGE_LOOP('',(#68979,#68980,#68981,#68982));
#14270=EDGE_LOOP('',(#68983,#68984,#68985,#68986));
#14271=EDGE_LOOP('',(#68987,#68988,#68989,#68990));
#14272=EDGE_LOOP('',(#68991,#68992,#68993,#68994));
#14273=EDGE_LOOP('',(#68995,#68996,#68997,#68998));
#14274=EDGE_LOOP('',(#68999,#69000,#69001,#69002));
#14275=EDGE_LOOP('',(#69003,#69004,#69005,#69006));
#14276=EDGE_LOOP('',(#69007,#69008,#69009,#69010));
#14277=EDGE_LOOP('',(#69011,#69012,#69013,#69014));
#14278=EDGE_LOOP('',(#69015,#69016,#69017,#69018));
#14279=EDGE_LOOP('',(#69019,#69020,#69021,#69022));
#14280=EDGE_LOOP('',(#69023,#69024));
#14281=EDGE_LOOP('',(#69025));
#14282=EDGE_LOOP('',(#69026));
#14283=EDGE_LOOP('',(#69027,#69028,#69029,#69030));
#14284=EDGE_LOOP('',(#69031,#69032,#69033,#69034,#69035,#69036,#69037,#69038,
#69039));
#14285=EDGE_LOOP('',(#69040,#69041,#69042,#69043,#69044));
#14286=EDGE_LOOP('',(#69045));
#14287=EDGE_LOOP('',(#69046));
#14288=EDGE_LOOP('',(#69047,#69048,#69049,#69050));
#14289=EDGE_LOOP('',(#69051));
#14290=EDGE_LOOP('',(#69052));
#14291=EDGE_LOOP('',(#69053));
#14292=EDGE_LOOP('',(#69054,#69055,#69056,#69057,#69058,#69059));
#14293=EDGE_LOOP('',(#69060,#69061));
#14294=EDGE_LOOP('',(#69062,#69063));
#14295=EDGE_LOOP('',(#69064,#69065));
#14296=EDGE_LOOP('',(#69066,#69067));
#14297=EDGE_LOOP('',(#69068,#69069));
#14298=EDGE_LOOP('',(#69070,#69071,#69072,#69073,#69074,#69075));
#14299=EDGE_LOOP('',(#69076,#69077,#69078,#69079));
#14300=EDGE_LOOP('',(#69080,#69081,#69082,#69083));
#14301=EDGE_LOOP('',(#69084,#69085,#69086,#69087));
#14302=EDGE_LOOP('',(#69088,#69089,#69090,#69091));
#14303=EDGE_LOOP('',(#69092,#69093,#69094,#69095));
#14304=EDGE_LOOP('',(#69096,#69097,#69098,#69099));
#14305=EDGE_LOOP('',(#69100,#69101,#69102,#69103,#69104,#69105,#69106,#69107,
#69108,#69109,#69110,#69111,#69112,#69113,#69114,#69115,#69116,#69117,#69118,
#69119,#69120,#69121,#69122,#69123,#69124,#69125,#69126,#69127,#69128,#69129,
#69130,#69131,#69132,#69133,#69134,#69135,#69136,#69137,#69138,#69139,#69140,
#69141,#69142,#69143,#69144,#69145,#69146,#69147,#69148,#69149,#69150,#69151,
#69152,#69153,#69154,#69155,#69156,#69157,#69158,#69159,#69160,#69161,#69162,
#69163,#69164,#69165,#69166,#69167));
#14306=EDGE_LOOP('',(#69168,#69169,#69170));
#14307=EDGE_LOOP('',(#69171,#69172,#69173,#69174,#69175,#69176,#69177,#69178,
#69179,#69180,#69181,#69182,#69183,#69184,#69185,#69186,#69187,#69188,#69189,
#69190,#69191,#69192,#69193,#69194,#69195,#69196,#69197,#69198,#69199,#69200,
#69201,#69202,#69203,#69204,#69205,#69206,#69207,#69208,#69209,#69210,#69211,
#69212,#69213,#69214,#69215,#69216,#69217,#69218,#69219,#69220,#69221,#69222,
#69223,#69224,#69225,#69226,#69227,#69228,#69229,#69230,#69231,#69232,#69233,
#69234,#69235,#69236,#69237));
#20518=CIRCLE('',#99054,1.17524047358083);
#20519=CIRCLE('',#99086,1.17524047357586);
#20520=CIRCLE('',#99088,1.5);
#20521=CIRCLE('',#99120,1.15470053837925);
#20522=CIRCLE('',#99122,2.75);
#20523=CIRCLE('',#99123,1.5);
#20524=CIRCLE('',#99125,3.5);
#20525=CIRCLE('',#99126,3.5);
#20526=CIRCLE('',#99128,1.17524047357586);
#20527=CIRCLE('',#99129,1.5);
#20528=CIRCLE('',#99130,1.125);
#20529=CIRCLE('',#99136,1.15470053837925);
#20530=CIRCLE('',#99137,1.15470053837925);
#20531=CIRCLE('',#99138,1.15470053837925);
#20532=CIRCLE('',#99139,1.15470053837925);
#20533=CIRCLE('',#99140,1.15470053837925);
#24563=B_SPLINE_CURVE_WITH_KNOTS('',3,(#359506,#359507,#359508,#359509,
#359510,#359511,#359512,#359513,#359514,#359515,#359516,#359517,#359518,
#359519,#359520,#359521),.UNSPECIFIED.,.F.,.F.,(4,2,2,2,2,2,2,4),(-29.2770358934888,
-29.2362857521938,-29.1955119506722,-29.1366692553965,-29.0768920699773,
-29.0195042768758,-28.9598835040274,-28.9203929548343),.UNSPECIFIED.);
#24564=B_SPLINE_CURVE_WITH_KNOTS('',3,(#359526,#359527,#359528,#359529,
#359530,#359531,#359532,#359533,#359534,#359535,#359536,#359537,#359538,
#359539,#359540,#359541,#359542,#359543,#359544,#359545,#359546,#359547,
#359548,#359549,#359550,#359551,#359552,#359553,#359554,#359555,#359556,
#359557,#359558,#359559,#359560,#359561),.UNSPECIFIED.,.F.,.F.,(4,2,2,2,
2,2,2,2,2,2,2,2,2,2,2,2,2,4),(-0.94601066902327,-0.905572650935517,-0.846069453129944,
-0.78879284938284,-0.729101573772443,-0.670375555962728,-0.613287938392507,
-0.553575227518369,-0.495501327642977,-0.437451545284286,-0.377809327518591,
-0.320409512233013,-0.260253652075058,-0.201407883721806,-0.144421016431325,
-0.0847464676700296,-0.0416443989073922,-1.00000010494483E-6),
 .UNSPECIFIED.);
#24565=B_SPLINE_CURVE_WITH_KNOTS('',3,(#359562,#359563,#359564,#359565,
#359566,#359567,#359568,#359569,#359570,#359571,#359572,#359573,#359574,
#359575,#359576,#359577,#359578,#359579,#359580,#359581,#359582,#359583,
#359584,#359585,#359586,#359587,#359588,#359589,#359590,#359591,#359592,
#359593,#359594,#359595,#359596,#359597),.UNSPECIFIED.,.F.,.F.,(4,2,2,2,
2,2,2,2,2,2,2,2,2,2,2,2,2,4),(-28.9203929548343,-28.9013438219494,-28.8432744956346,
-28.7828952739219,-28.7255724465968,-28.6668280638283,-28.6070165834198,
-28.5498007229944,-28.4904108948662,-28.4314603756214,-28.3735947373694,
-28.3134411876362,-28.2559721336729,-28.1974344995555,-28.137651101191,
-28.080550994228,-28.0213654657236,-27.9725898263478),.UNSPECIFIED.);
#24566=B_SPLINE_CURVE_WITH_KNOTS('',3,(#359602,#359603,#359604,#359605,
#359606,#359607,#359608,#359609,#359610,#359611,#359612,#359613,#359614,
#359615,#359616,#359617,#359618,#359619,#359620,#359621,#359622,#359623,
#359624,#359625,#359626,#359627,#359628,#359629,#359630,#359631,#359632,
#359633,#359634,#359635,#359636,#359637),.UNSPECIFIED.,.F.,.F.,(4,2,2,2,
2,2,2,2,2,2,2,2,2,2,2,2,2,4),(-1.8926695413163,-1.84291005897148,-1.78382950075986,
-1.72680324523774,-1.66708657324484,-1.60865369543663,-1.55120091496044,
-1.49115806194456,-1.43339609076476,-1.37440371886069,-1.31512569084528,
-1.25800575207285,-1.19826779235354,-1.13963510223288,-1.08235073620415,
-1.02208914923483,-0.964129934552806,-0.94601066902327),.UNSPECIFIED.);
#24567=B_SPLINE_CURVE_WITH_KNOTS('',3,(#359638,#359639,#359640,#359641,
#359642,#359643,#359644,#359645,#359646,#359647,#359648,#359649,#359650,
#359651,#359652,#359653,#359654,#359655,#359656,#359657,#359658,#359659,
#359660,#359661,#359662,#359663,#359664,#359665,#359666,#359667,#359668,
#359669,#359670,#359671,#359672,#359673),.UNSPECIFIED.,.F.,.F.,(4,2,2,2,
2,2,2,2,2,2,2,2,2,2,2,2,2,4),(-27.9725898263478,-27.9619006210563,-27.9042087329266,
-27.8442484956794,-27.7865362065019,-27.7281728793652,-27.6683879590505,
-27.6113049906475,-27.552291595915,-27.4922363274911,-27.4346836129977,
-27.3748790713291,-27.3168429779888,-27.2586164050606,-27.1988025070983,
-27.1416465003213,-27.0827674848282,-27.0250189260883),.UNSPECIFIED.);
#24568=B_SPLINE_CURVE_WITH_KNOTS('',3,(#359678,#359679,#359680,#359681,
#359682,#359683,#359684,#359685,#359686,#359687,#359688,#359689,#359690,
#359691,#359692,#359693,#359694,#359695,#359696,#359697,#359698,#359699,
#359700,#359701,#359702,#359703,#359704,#359705,#359706,#359707,#359708,
#359709,#359710,#359711,#359712,#359713),.UNSPECIFIED.,.F.,.F.,(4,2,2,2,
2,2,2,2,2,2,2,2,2,2,2,2,2,4),(-2.83930461628737,-2.78070942430762,-2.72191816145488,
-2.6647972069617,-2.60503799392433,-2.54689906316616,-2.48884583546765,
-2.42913478010044,-2.37166991679545,-2.3115421817861,-2.25262568519442,
-2.19559552368152,-2.13587110462393,-2.07760446420945,-2.0198890025174,
-1.96003137986963,-1.9024357257172,-1.8926695413163),.UNSPECIFIED.);
#24569=B_SPLINE_CURVE_WITH_KNOTS('',3,(#359714,#359715,#359716,#359717,
#359718,#359719,#359720,#359721,#359722,#359723,#359724,#359725,#359726,
#359727,#359728,#359729,#359730,#359731,#359732,#359733,#359734,#359735,
#359736,#359737,#359738,#359739,#359740,#359741,#359742,#359743,#359744,
#359745,#359746,#359747,#359748,#359749,#359750,#359751),.UNSPECIFIED.,
 .F.,.F.,(4,2,2,2,2,2,2,2,2,2,2,2,2,2,2,2,2,2,4),(-27.0250189260883,-27.0229709630833,
-26.9655490869138,-26.9058917673861,-26.8473869725484,-26.789284343176,
-26.7288687611185,-26.6715498658954,-26.6127715994654,-26.5529475275648,
-26.495704256368,-26.4362808054032,-26.3773789390475,-26.3194833378924,
-26.2592970104669,-26.2018442363091,-26.1432763083209,-26.0834840806869,
-26.0768560357195),.UNSPECIFIED.);
#24570=B_SPLINE_CURVE_WITH_KNOTS('',3,(#359756,#359757,#359758,#359759,
#359760,#359761,#359762,#359763,#359764,#359765,#359766,#359767,#359768,
#359769,#359770,#359771,#359772,#359773,#359774,#359775,#359776,#359777,
#359778,#359779,#359780,#359781,#359782,#359783,#359784,#359785,#359786,
#359787,#359788,#359789,#359790,#359791,#359792,#359793),.UNSPECIFIED.,
 .F.,.F.,(4,2,2,2,2,2,2,2,2,2,2,2,2,2,2,2,2,2,4),(-3.78674073016776,-3.77914273671298,
-3.71938890886991,-3.66089758697167,-3.6034363230487,-3.54333169828402,
-3.48551187697086,-3.42654362802735,-3.36720317419242,-3.31003012797249,
-3.25025122193717,-3.19155616962155,-3.13425093289176,-3.07392365536491,
-3.01590295314771,-2.95735628517826,-2.89778737068896,-2.84044861901574,
-2.83930461628737),.UNSPECIFIED.);
#24571=B_SPLINE_CURVE_WITH_KNOTS('',3,(#359794,#359795,#359796,#359797,
#359798,#359799,#359800,#359801,#359802,#359803,#359804,#359805,#359806,
#359807,#359808,#359809,#359810,#359811,#359812,#359813,#359814,#359815,
#359816,#359817,#359818,#359819,#359820,#359821,#359822,#359823,#359824,
#359825,#359826,#359827,#359828,#359829),.UNSPECIFIED.,.F.,.F.,(4,2,2,2,
2,2,2,2,2,2,2,2,2,2,2,2,2,4),(-26.0768560357195,-26.0263685270805,-25.9671528988416,
-25.9077479135651,-25.8500299500852,-25.7900411558174,-25.7323562797147,
-25.6739668845061,-25.6141765859204,-25.5570898656,-25.4980505900865,-25.4380625593129,
-25.3804882052171,-25.320659935685,-25.2626595733453,-25.2044117340995,
-25.1445956843974,-25.1292817558394),.UNSPECIFIED.);
#24572=B_SPLINE_CURVE_WITH_KNOTS('',3,(#359834,#359835,#359836,#359837,
#359838,#359839,#359840,#359841,#359842,#359843,#359844,#359845,#359846,
#359847,#359848,#359849,#359850,#359851,#359852,#359853,#359854,#359855,
#359856,#359857,#359858,#359859,#359860,#359861,#359862,#359863,#359864,
#359865,#359866,#359867,#359868,#359869),.UNSPECIFIED.,.F.,.F.,(4,2,2,2,
2,2,2,2,2,2,2,2,2,2,2,2,2,4),(-4.73379937711506,-4.71760993607862,-4.65782029343659,
-4.59963256224015,-4.54158930230178,-4.48182617663283,-4.42431237784908,
-4.36422553346581,-4.30525502901722,-4.24819587084784,-4.18843777163506,
-4.13011723963591,-4.07240407682471,-4.01248924293099,-3.95483993189503,
-3.89534884352174,-3.8362097215891,-3.78674073016776),.UNSPECIFIED.);
#24573=B_SPLINE_CURVE_WITH_KNOTS('',3,(#359870,#359871,#359872,#359873,
#359874,#359875,#359876,#359877,#359878,#359879,#359880,#359881,#359882,
#359883,#359884,#359885,#359886,#359887,#359888,#359889,#359890,#359891,
#359892,#359893,#359894,#359895,#359896,#359897,#359898,#359899,#359900,
#359901,#359902,#359903,#359904,#359905),.UNSPECIFIED.,.F.,.F.,(4,2,2,2,
2,2,2,2,2,2,2,2,2,2,2,2,2,4),(-25.1292817558394,-25.0874460424636,-25.0285459963092,
-24.9687457625083,-24.9113046781623,-24.851626239461,-24.7931712161292,
-24.7350502895988,-24.6746139124586,-24.6173132140707,-24.5585162222061,
-24.4986952887874,-24.4414384282637,-24.3819967053851,-24.3231589306908,
-24.2652483109868,-24.205044695016,-24.181124288547),.UNSPECIFIED.);
#24574=B_SPLINE_CURVE_WITH_KNOTS('',3,(#359910,#359911,#359912,#359913,
#359914,#359915,#359916,#359917,#359918,#359919,#359920,#359921,#359922,
#359923,#359924,#359925,#359926,#359927,#359928,#359929,#359930,#359931,
#359932,#359933,#359934,#359935,#359936,#359937,#359938,#359939,#359940,
#359941,#359942,#359943,#359944,#359945),.UNSPECIFIED.,.F.,.F.,(4,2,2,2,
2,2,2,2,2,2,2,2,2,2,2,2,2,4),(-5.68164266866445,-5.65672900808728,-5.59657896987309,
-5.53871701905266,-5.47978603931155,-5.42039942184852,-5.36318772406343,
-5.30338370045807,-5.24464237047255,-5.18732994589727,-5.1269535569688,
-5.06888728475205,-5.01036436220717,-4.95074625365402,-4.89336124156495,
-4.83359016895416,-4.77475004818097,-4.73379937711506),.UNSPECIFIED.);
#24575=B_SPLINE_CURVE_WITH_KNOTS('',3,(#359946,#359947,#359948,#359949,
#359950,#359951,#359952,#359953,#359954,#359955,#359956,#359957,#359958,
#359959,#359960,#359961,#359962,#359963,#359964,#359965,#359966,#359967,
#359968,#359969,#359970,#359971,#359972,#359973,#359974,#359975,#359976,
#359977,#359978,#359979,#359980,#359981),.UNSPECIFIED.,.F.,.F.,(4,2,2,2,
2,2,2,2,2,2,2,2,2,2,2,2,2,4),(-24.181124288547,-24.1476227904716,-24.089039655252,
-24.0292544286749,-23.9721373554774,-23.9129069011809,-23.8535779480638,
-23.7958488025427,-23.7358468798957,-23.6782043827208,-23.6198039524279,
-23.5600241998517,-23.5029479631018,-23.4438980195044,-23.3839942080211,
-23.3264130818869,-23.2665764840907,-23.2336871318211),.UNSPECIFIED.);
#24576=B_SPLINE_CURVE_WITH_KNOTS('',3,(#359986,#359987,#359988,#359989,
#359990,#359991,#359992,#359993,#359994,#359995,#359996,#359997,#359998,
#359999,#360000,#360001,#360002,#360003,#360004,#360005,#360006,#360007,
#360008,#360009,#360010,#360011,#360012,#360013,#360014,#360015,#360016,
#360017,#360018,#360019,#360020,#360021),.UNSPECIFIED.,.F.,.F.,(4,2,2,2,
2,2,2,2,2,2,2,2,2,2,2,2,2,4),(-6.6289785836689,-6.59514941924382,-6.53535013671941,
-6.47780271809717,-6.4177707840938,-6.35876208546021,-6.30168794247145,
-6.24191189860981,-6.18355312246758,-6.12585592843799,-6.06590001355162,
-6.00821256016226,-5.94876952995814,-5.88958788307532,-5.83249429561485,
-5.7727190919009,-5.71418519391065,-5.68164266866445),.UNSPECIFIED.);
#24577=B_SPLINE_CURVE_WITH_KNOTS('',3,(#360022,#360023,#360024,#360025,
#360026,#360027,#360028,#360029,#360030,#360031,#360032,#360033,#360034,
#360035,#360036,#360037,#360038,#360039,#360040,#360041,#360042,#360043,
#360044,#360045,#360046,#360047,#360048,#360049,#360050,#360051,#360052,
#360053,#360054,#360055,#360056,#360057),.UNSPECIFIED.,.F.,.F.,(4,2,2,2,
2,2,2,2,2,2,2,2,2,2,2,2,2,4),(-23.2336871318211,-23.2086275557579,-23.1503734650017,
-23.0905712748626,-23.033442679821,-22.9745367926783,-22.9147487560726,
-22.8573032676543,-22.797619037379,-22.7392300501316,-22.6811057829897,
-22.6206640846457,-22.5633965282484,-22.5045959144076,-22.4447942837391,
-22.3875376301589,-22.3280929476983,-22.2857741951284),.UNSPECIFIED.);
#24578=B_SPLINE_CURVE_WITH_KNOTS('',3,(#360062,#360063,#360064,#360065,
#360066,#360067,#360068,#360069,#360070,#360071,#360072,#360073,#360074,
#360075,#360076,#360077,#360078,#360079,#360080,#360081,#360082,#360083,
#360084,#360085,#360086,#360087,#360088,#360089,#360090,#360091,#360092,
#360093,#360094,#360095,#360096,#360097),.UNSPECIFIED.,.F.,.F.,(4,2,2,2,
2,2,2,2,2,2,2,2,2,2,2,2,2,4),(-7.57699195719593,-7.5336040360614,-7.47418686850509,
-7.41695052210019,-7.35713701526706,-7.29836483713746,-7.24105913548731,
-7.18064950623535,-7.1225529356128,-7.06406775513403,-7.00441619331711,
-6.94700007863283,-6.88721276951991,-6.8283393945683,-6.77119421074264,
-6.71138983189206,-6.65316874394789,-6.6289785836689),.UNSPECIFIED.);
#24579=B_SPLINE_CURVE_WITH_KNOTS('',3,(#360098,#360099,#360100,#360101,
#360102,#360103,#360104,#360105,#360106,#360107,#360108,#360109,#360110,
#360111,#360112,#360113,#360114,#360115,#360116,#360117,#360118,#360119,
#360120,#360121,#360122,#360123,#360124,#360125,#360126,#360127,#360128,
#360129,#360130,#360131,#360132,#360133),.UNSPECIFIED.,.F.,.F.,(4,2,2,2,
2,2,2,2,2,2,2,2,2,2,2,2,2,4),(-22.2857741951284,-22.2693364072178,-22.2114257342202,
-22.1512203014804,-22.0938448119875,-22.0352615756877,-21.9754997082272,
-21.9183952653275,-21.859165292854,-21.7999305404075,-21.7422052085182,
-21.6822056562023,-21.6246217930565,-21.5662254676702,-21.5064727995311,
-21.449421768801,-21.3903764906121,-21.3386984476615),.UNSPECIFIED.);
#24580=B_SPLINE_CURVE_WITH_KNOTS('',3,(#360138,#360139,#360140,#360141,
#360142,#360143,#360144,#360145,#360146,#360147,#360148,#360149,#360150,
#360151,#360152,#360153,#360154,#360155,#360156,#360157,#360158,#360159,
#360160,#360161,#360162,#360163,#360164,#360165,#360166,#360167,#360168,
#360169,#360170,#360171,#360172,#360173),.UNSPECIFIED.,.F.,.F.,(4,2,2,2,
2,2,2,2,2,2,2,2,2,2,2,2,2,4),(-8.52439085180131,-8.47165190932738,-8.41262036103156,
-8.3555452676041,-8.29576697778077,-8.23738512988965,-8.17971826146527,
-8.11973686813537,-8.06202630831729,-8.00264619984432,-7.94343750413151,
-7.88633123192098,-7.82655031957626,-7.76798914240985,-7.71055206906101,
-7.65037235147109,-7.59248342397278,-7.57699195719593),.UNSPECIFIED.);
#24581=B_SPLINE_CURVE_WITH_KNOTS('',3,(#360174,#360175,#360176,#360177,
#360178,#360179,#360180,#360181,#360182,#360183,#360184,#360185,#360186,
#360187,#360188,#360189,#360190,#360191,#360192,#360193,#360194,#360195,
#360196,#360197,#360198,#360199,#360200,#360201,#360202,#360203,#360204,
#360205,#360206,#360207,#360208,#360209,#360210,#360211),.UNSPECIFIED.,
 .F.,.F.,(4,2,2,2,2,2,2,2,2,2,2,2,2,2,2,2,2,2,4),(-21.3386984476615,-21.3305761052758,
-21.273003270418,-21.213173915207,-21.1552935809097,-21.0970484612882,-21.0372768361306,
-20.9801847091942,-20.9212883924184,-20.8615291182862,-20.8040942717974,
-20.7444197976042,-20.6861149111606,-20.6280025247625,-20.5675712071319,
-20.5103527388457,-20.4515638671961,-20.3917985314428,-20.3912808464162),
 .UNSPECIFIED.);
#24582=B_SPLINE_CURVE_WITH_KNOTS('',3,(#360216,#360217,#360218,#360219,
#360220,#360221,#360222,#360223,#360224,#360225,#360226,#360227,#360228,
#360229,#360230,#360231,#360232,#360233,#360234,#360235,#360236,#360237,
#360238,#360239,#360240,#360241,#360242,#360243,#360244,#360245,#360246,
#360247,#360248,#360249,#360250,#360251,#360252,#360253),.UNSPECIFIED.,
 .F.,.F.,(4,2,2,2,2,2,2,2,2,2,2,2,2,2,2,2,2,2,4),(-9.47234169396005,-9.47079131440874,
-9.41098410876783,-9.35219620204647,-9.2949115979019,-9.23448424708455,
-9.1763723465148,-9.11794003645549,-9.0582704006571,-9.00083801663931,-8.94105012120809,
-8.88215873334131,-8.82502278464254,-8.76521939714966,-8.70698002683787,
-8.64899944808623,-8.58917950168627,-8.53161339913665,-8.52439085180131),
 .UNSPECIFIED.);
#24583=B_SPLINE_CURVE_WITH_KNOTS('',3,(#360254,#360255,#360256,#360257,
#360258,#360259,#360260,#360261,#360262,#360263,#360264,#360265,#360266,
#360267,#360268,#360269,#360270,#360271,#360272,#360273,#360274,#360275,
#360276,#360277,#360278,#360279,#360280,#360281,#360282,#360283,#360284,
#360285,#360286,#360287,#360288,#360289),.UNSPECIFIED.,.F.,.F.,(4,2,2,2,
2,2,2,2,2,2,2,2,2,2,2,2,2,4),(-20.3912808464162,-20.334556071801,-20.2751240267045,
-20.2164680585815,-20.1585726374241,-20.0983811658138,-20.041068963067,
-19.9825010710361,-19.9227798618537,-19.8657026684406,-19.8064888467141,
-19.7473690371157,-19.6896629420058,-19.6296816582903,-19.5721744062189,
-19.5137977586576,-19.4540897591255,-19.4447457737501),.UNSPECIFIED.);
#24584=B_SPLINE_CURVE_WITH_KNOTS('',3,(#360294,#360295,#360296,#360297,
#360298,#360299,#360300,#360301,#360302,#360303,#360304,#360305,#360306,
#360307,#360308,#360309,#360310,#360311,#360312,#360313,#360314,#360315,
#360316,#360317,#360318,#360319,#360320,#360321,#360322,#360323,#360324,
#360325,#360326,#360327,#360328,#360329),.UNSPECIFIED.,.F.,.F.,(4,2,2,2,
2,2,2,2,2,2,2,2,2,2,2,2,2,4),(-10.4196492469242,-10.4092374309108,-10.3494729075107,
-10.2910830142037,-10.233461608822,-10.1734701511741,-10.1157513707506,
-10.0564507135166,-9.99723022113808,-9.9401252138231,-9.88035449510157,
-9.82178110147787,-9.76437789214267,-9.70418395253122,-9.64628296916424,
-9.58747091595993,-9.52803851322082,-9.47234169396005),.UNSPECIFIED.);
#24585=B_SPLINE_CURVE_WITH_KNOTS('',3,(#360330,#360331,#360332,#360333,
#360334,#360335,#360336,#360337,#360338,#360339,#360340,#360341,#360342,
#360343,#360344,#360345,#360346,#360347,#360348,#360349,#360350,#360351,
#360352,#360353,#360354,#360355,#360356,#360357,#360358,#360359,#360360,
#360361,#360362,#360363,#360364,#360365),.UNSPECIFIED.,.F.,.F.,(4,2,2,2,
2,2,2,2,2,2,2,2,2,2,2,2,2,4),(-19.4447457737501,-19.3970794408228,-19.3380546146096,
-19.2783797548411,-19.2208308040997,-19.161024772293,-19.1032321601674,
-19.0450117778471,-18.9852885651626,-18.9282494273001,-18.869378655352,
-18.8090891815156,-18.7516607032691,-18.6919900130941,-18.6338439477108,
-18.5757401634432,-18.5159751173138,-18.4982475217245),.UNSPECIFIED.);
#24586=B_SPLINE_CURVE_WITH_KNOTS('',3,(#360370,#360371,#360372,#360373,
#360374,#360375,#360376,#360377,#360378,#360379,#360380,#360381,#360382,
#360383,#360384,#360385,#360386,#360387,#360388,#360389,#360390,#360391,
#360392,#360393,#360394,#360395,#360396,#360397,#360398,#360399,#360400,
#360401,#360402,#360403,#360404,#360405),.UNSPECIFIED.,.F.,.F.,(4,2,2,2,
2,2,2,2,2,2,2,2,2,2,2,2,2,4),(-11.3671613030629,-11.3483513921095,-11.2879218103826,
-11.2298095608741,-11.171446702329,-11.1117743353272,-11.0543405061875,
-10.9945680299796,-10.9356738342456,-10.8785619212499,-10.8187756395274,
-10.7605330146923,-10.7026071376232,-10.6427819322376,-10.5852120241117,
-10.5253383567006,-10.4662991670699,-10.4196492469242),.UNSPECIFIED.);
#24587=B_SPLINE_CURVE_WITH_KNOTS('',3,(#360406,#360407,#360408,#360409,
#360410,#360411,#360412,#360413,#360414,#360415,#360416,#360417,#360418,
#360419,#360420,#360421,#360422,#360423,#360424,#360425,#360426,#360427,
#360428,#360429,#360430,#360431,#360432,#360433,#360434,#360435,#360436,
#360437,#360438,#360439,#360440,#360441),.UNSPECIFIED.,.F.,.F.,(4,2,2,2,
2,2,2,2,2,2,2,2,2,2,2,2,2,4),(-18.4982475217245,-18.4588246892297,-18.4000678912934,
-18.3403257329831,-18.2830174724236,-18.223482590589,-18.1648133289671,
-18.1068206532574,-18.0465261169426,-17.9891653866314,-17.9304989893709,
-17.8707028571648,-17.8135408598337,-17.7542281137836,-17.6951092021336,
-17.6373101990686,-17.5772305525968,-17.5506080199207),.UNSPECIFIED.);
#24588=B_SPLINE_CURVE_WITH_KNOTS('',3,(#360446,#360447,#360448,#360449,
#360450,#360451,#360452,#360453,#360454,#360455,#360456,#360457,#360458,
#360459,#360460,#360461,#360462,#360463,#360464,#360465,#360466,#360467,
#360468,#360469,#360470,#360471,#360472,#360473,#360474,#360475,#360476,
#360477,#360478,#360479,#360480,#360481),.UNSPECIFIED.,.F.,.F.,(4,2,2,2,
2,2,2,2,2,2,2,2,2,2,2,2,2,4),(-12.314277429601,-12.2865423449001,-12.2265563711873,
-12.1688444212435,-12.1096418385269,-12.0504248995809,-11.9933353775088,
-11.9335913590392,-11.8750208936681,-11.817667321657,-11.7574746635353,
-11.6995766283184,-11.6408494403391,-11.5814171422987,-11.5241729057154,
-11.4643882936125,-11.4055997852911,-11.3671613030629),.UNSPECIFIED.);
#24589=B_SPLINE_CURVE_WITH_KNOTS('',3,(#360482,#360483,#360484,#360485,
#360486,#360487,#360488,#360489,#360490,#360491,#360492,#360493,#360494,
#360495,#360496,#360497,#360498,#360499,#360500,#360501,#360502,#360503,
#360504,#360505,#360506,#360507,#360508,#360509,#360510,#360511,#360512,
#360513,#360514,#360515,#360516,#360517),.UNSPECIFIED.,.F.,.F.,(4,2,2,2,
2,2,2,2,2,2,2,2,2,2,2,2,2,4),(-17.5506080199207,-17.5196882325723,-17.4612177719407,
-17.401439017662,-17.3443578226861,-17.285238717623,-17.2255751036821,-17.1679382057827,
-17.1080392136975,-17.0502227508961,-16.99191393138,-16.9321237907676,-16.8750265151245,
-16.8160668605451,-16.7557941095397,-16.698283187946,-16.638525529114,-16.6031179891744),
 .UNSPECIFIED.);
#24590=B_SPLINE_CURVE_WITH_KNOTS('',3,(#360522,#360523,#360524,#360525,
#360526,#360527,#360528,#360529,#360530,#360531,#360532,#360533,#360534,
#360535,#360536,#360537,#360538,#360539,#360540,#360541,#360542,#360543,
#360544,#360545,#360546,#360547,#360548,#360549,#360550,#360551,#360552,
#360553,#360554,#360555,#360556,#360557),.UNSPECIFIED.,.F.,.F.,(4,2,2,2,
2,2,2,2,2,2,2,2,2,2,2,2,2,4),(-13.2611275241497,-13.2240332453506,-13.1643737747774,
-13.1069536302929,-13.0472133148037,-12.9883318031598,-12.9312595314886,
-12.8715072459355,-12.8132766664862,-12.7554229928843,-12.6956081697718,
-12.6380495940693,-12.5782834655373,-12.519252027863,-12.4622184993239,
-12.4024844482838,-12.3441017059567,-12.314277429601),.UNSPECIFIED.);
#24591=B_SPLINE_CURVE_WITH_KNOTS('',3,(#360558,#360559,#360560,#360561,
#360562,#360563,#360564,#360565,#360566,#360567,#360568,#360569,#360570,
#360571,#360572,#360573,#360574,#360575,#360576,#360577,#360578,#360579,
#360580,#360581,#360582,#360583,#360584,#360585,#360586,#360587,#360588,
#360589,#360590,#360591,#360592,#360593),.UNSPECIFIED.,.F.,.F.,(4,2,2,2,
2,2,2,2,2,2,2,2,2,2,2,2,2,4),(-16.6031179891744,-16.5803630906363,-16.5221767759143,
-16.462348383425,-16.4051501161605,-16.3463104187655,-16.2865035095385,
-16.2291160249035,-16.1694976410878,-16.1108266704695,-16.0527553084712,
-15.9923771273555,-15.9349817326151,-15.876235592733,-15.8163819401178,
-15.7591514407899,-15.6997587114897,-15.654611343672),.UNSPECIFIED.);
#24592=B_SPLINE_CURVE_WITH_KNOTS('',3,(#360598,#360599,#360600,#360601,
#360602,#360603,#360604,#360605,#360606,#360607,#360608,#360609,#360610,
#360611,#360612,#360613,#360614,#360615,#360616,#360617,#360618,#360619,
#360620,#360621,#360622,#360623,#360624,#360625,#360626,#360627,#360628,
#360629,#360630,#360631,#360632,#360633),.UNSPECIFIED.,.F.,.F.,(4,2,2,2,
2,2,2,2,2,2,2,2,2,2,2,2,2,4),(-14.2078226042407,-14.1616527561318,-14.102455149493,
-14.0453958531341,-13.9856960744249,-13.9271440872338,-13.8698573378326,
-13.8096818371734,-13.7518021599383,-13.6931796831918,-13.6337631805218,
-13.5765359534962,-13.5167911415227,-13.4580174836316,-13.4008214879835,
-13.340405458723,-13.2823081702298,-13.2611275241497),.UNSPECIFIED.);
#24593=B_SPLINE_CURVE_WITH_KNOTS('',3,(#360634,#360635,#360636,#360637,
#360638,#360639,#360640,#360641,#360642,#360643,#360644,#360645,#360646,
#360647,#360648,#360649,#360650,#360651,#360652,#360653,#360654,#360655,
#360656,#360657,#360658,#360659,#360660,#360661,#360662,#360663,#360664,
#360665,#360666,#360667,#360668,#360669),.UNSPECIFIED.,.F.,.F.,(4,2,2,2,
2,2,2,2,2,2,2,2,2,2,2,2,2,4),(-15.654611343672,-15.6406517898237,-15.5827780369757,
-15.5226189958196,-15.4650548029905,-15.4065088447247,-15.3466765037092,
-15.2895398121176,-15.2303449176205,-15.170703619353,-15.1129964866102,
-15.0530230138708,-14.99519558114,-14.9368161615171,-14.8769760423813,-14.8177008154817,
-14.7583766231312,-14.7063679063436),.UNSPECIFIED.);
#24594=B_SPLINE_CURVE_WITH_KNOTS('',3,(#360674,#360675,#360676,#360677,
#360678,#360679,#360680,#360681,#360682,#360683,#360684,#360685,#360686,
#360687,#360688,#360689,#360690,#360691,#360692,#360693,#360694,#360695,
#360696,#360697,#360698,#360699,#360700,#360701,#360702,#360703,#360704,
#360705,#360706,#360707,#360708,#360709),.UNSPECIFIED.,.F.,.F.,(4,2,2,2,
2,2,2,2,2,2,2,2,2,2,2,2,2,4),(-15.1537653436456,-15.1002345835303,-15.0409821852976,
-14.9820358340952,-14.9242995477987,-14.8642830082815,-14.8068674757668,
-14.7470792575717,-14.6895477527618,-14.6299119365804,-14.5709041670138,
-14.5139145448345,-14.4542288146403,-14.3958689208766,-14.3383899716655,
-14.278425498234,-14.2207359254435,-14.2078226042407),.UNSPECIFIED.);
#24595=B_SPLINE_CURVE_WITH_KNOTS('',3,(#360710,#360711,#360712,#360713,
#360714,#360715,#360716,#360717,#360718,#360719,#360720,#360721,#360722,
#360723,#360724,#360725,#360726,#360727,#360728,#360729,#360730,#360731,
#360732,#360733,#360734,#360735,#360736,#360737,#360738,#360739,#360740,
#360741,#360742,#360743,#360744,#360745,#360746,#360747),.UNSPECIFIED.,
 .F.,.F.,(4,2,2,2,2,2,2,2,2,2,2,2,2,2,2,2,2,2,4),(-14.7063679063436,-14.7011878444491,
-14.6413441342094,-14.5826673668123,-14.5252266321471,-14.4649240950712,
-14.4069210059505,-14.3481170771853,-14.2885758826815,-14.2312275238881,
-14.1713416201138,-14.1124451307885,-14.0551048133669,-13.9945636453226,
-13.9363447517743,-13.8779000977309,-13.8181173661783,-13.76057775001,-13.7572072092418),
 .UNSPECIFIED.);
#24596=B_SPLINE_CURVE_WITH_KNOTS('',3,(#360752,#360753,#360754,#360755,
#360756,#360757,#360758,#360759,#360760,#360761,#360762,#360763,#360764,
#360765,#360766,#360767,#360768,#360769,#360770,#360771,#360772,#360773,
#360774,#360775,#360776,#360777,#360778,#360779,#360780,#360781,#360782,
#360783,#360784,#360785,#360786,#360787,#360788,#360789),.UNSPECIFIED.,
 .F.,.F.,(4,2,2,2,2,2,2,2,2,2,2,2,2,2,2,2,2,2,4),(-16.0998751798599,-16.0944661699573,
-16.0370900178806,-15.9774720925845,-15.9194611350742,-15.8614113663036,
-15.8017283017216,-15.7446717478584,-15.6859702556362,-15.6263082822782,
-15.5690559565789,-15.5095777085928,-15.4510629443817,-15.3931286818612,
-15.3328926225813,-15.2756424697563,-15.2170349859268,-15.1573280589623,
-15.1537653436456),.UNSPECIFIED.);
#24597=B_SPLINE_CURVE_WITH_KNOTS('',3,(#360790,#360791,#360792,#360793,
#360794,#360795,#360796,#360797,#360798,#360799,#360800,#360801,#360802,
#360803,#360804,#360805,#360806,#360807,#360808,#360809,#360810,#360811,
#360812,#360813,#360814,#360815,#360816,#360817,#360818,#360819,#360820,
#360821,#360822,#360823,#360824,#360825),.UNSPECIFIED.,.F.,.F.,(4,2,2,2,
2,2,2,2,2,2,2,2,2,2,2,2,2,4),(-13.7572072092418,-13.7007013703789,-13.6416982254372,
-13.5844902227664,-13.524600640322,-13.4662500986182,-13.4082378308948,
-13.348301084172,-13.2906243016887,-13.2306727337995,-13.1715225948561,
-13.1143609273779,-13.0544919256689,-12.995992124977,-12.93828143513,-12.8781764070513,
-12.8203488950124,-12.8083351637663),.UNSPECIFIED.);
#24598=B_SPLINE_CURVE_WITH_KNOTS('',3,(#360830,#360831,#360832,#360833,
#360834,#360835,#360836,#360837,#360838,#360839,#360840,#360841,#360842,
#360843,#360844,#360845,#360846,#360847,#360848,#360849,#360850,#360851,
#360852,#360853,#360854,#360855,#360856,#360857,#360858,#360859,#360860,
#360861,#360862,#360863,#360864,#360865),.UNSPECIFIED.,.F.,.F.,(4,2,2,2,
2,2,2,2,2,2,2,2,2,2,2,2,2,4),(-17.0450106813388,-17.0315098527715,-16.9738440378701,
-16.9139024253291,-16.8565055613141,-16.7981698690676,-16.7385346215828,
-16.6815895160318,-16.6226068061299,-16.5631048921601,-16.5056018619694,
-16.4458416325847,-16.3881739594714,-16.3300006825261,-16.2703549519301,
-16.2133967316551,-16.1545742555269,-16.0998751798599),.UNSPECIFIED.);
#24599=B_SPLINE_CURVE_WITH_KNOTS('',3,(#360866,#360867,#360868,#360869,
#360870,#360871,#360872,#360873,#360874,#360875,#360876,#360877,#360878,
#360879,#360880,#360881,#360882,#360883,#360884,#360885,#360886,#360887,
#360888,#360889,#360890,#360891,#360892,#360893,#360894,#360895,#360896,
#360897,#360898,#360899,#360900,#360901),.UNSPECIFIED.,.F.,.F.,(4,2,2,2,
2,2,2,2,2,2,2,2,2,2,2,2,2,4),(-12.8083351637663,-12.7609682207284,-12.7016349620055,
-12.6444255352263,-12.5845490220204,-12.5258638923139,-12.4683675412153,
-12.4080581728529,-12.3500467510207,-12.2911510845023,-12.2316043006535,
-12.1742480499109,-12.1143335601395,-12.0554322699415,-11.9980500980351,
-11.9375056408414,-11.8792817438646,-11.8589296630317),.UNSPECIFIED.);
#24600=B_SPLINE_CURVE_WITH_KNOTS('',3,(#360906,#360907,#360908,#360909,
#360910,#360911,#360912,#360913,#360914,#360915,#360916,#360917,#360918,
#360919,#360920,#360921,#360922,#360923,#360924,#360925,#360926,#360927,
#360928,#360929,#360930,#360931,#360932,#360933,#360934,#360935,#360936,
#360937,#360938,#360939,#360940,#360941),.UNSPECIFIED.,.F.,.F.,(4,2,2,2,
2,2,2,2,2,2,2,2,2,2,2,2,2,4),(-17.9903076061228,-17.9680233235286,-17.9100516126546,
-17.8504276638631,-17.7934153544959,-17.7347922515903,-17.6751907972335,
-17.6180133387519,-17.5586140507017,-17.5000981285757,-17.4422381848549,
-17.3820812044448,-17.3248623632732,-17.2663302079828,-17.2066766767308,
-17.1496478221714,-17.0904709505879,-17.0450106813388),.UNSPECIFIED.);
#24601=B_SPLINE_CURVE_WITH_KNOTS('',3,(#360942,#360943,#360944,#360945,
#360946,#360947,#360948,#360949,#360950,#360951,#360952,#360953,#360954,
#360955,#360956,#360957,#360958,#360959,#360960,#360961,#360962,#360963,
#360964,#360965,#360966,#360967,#360968,#360969,#360970,#360971,#360972,
#360973,#360974,#360975,#360976,#360977),.UNSPECIFIED.,.F.,.F.,(4,2,2,2,
2,2,2,2,2,2,2,2,2,2,2,2,2,4),(-11.8589296630317,-11.8207612239523,-11.7609757586343,
-11.7034322981271,-11.6435346624504,-11.584528908831,-11.5272914226937,
-11.4673788469843,-11.4090262099659,-11.3509531564106,-11.2910161981842,
-11.2333379281589,-11.1732917062938,-11.1141438241308,-11.0569636057153,
-10.9970750114197,-10.938577939892,-10.909574098799),.UNSPECIFIED.);
#24602=B_SPLINE_CURVE_WITH_KNOTS('',3,(#360982,#360983,#360984,#360985,
#360986,#360987,#360988,#360989,#360990,#360991,#360992,#360993,#360994,
#360995,#360996,#360997,#360998,#360999,#361000,#361001,#361002,#361003,
#361004,#361005,#361006,#361007,#361008,#361009,#361010,#361011,#361012,
#361013,#361014,#361015,#361016,#361017),.UNSPECIFIED.,.F.,.F.,(4,2,2,2,
2,2,2,2,2,2,2,2,2,2,2,2,2,4),(-18.9344980393133,-18.9041379145137,-18.8458912748405,
-18.7863224126782,-18.7294442575711,-18.670551023092,-18.6110353760674,
-18.553615705937,-18.4939436450504,-18.4362967240132,-18.3782072667762,
-18.3186241661682,-18.2617203663546,-18.2029821150101,-18.1428547423791,
-18.0855565847922,-18.0260209865782,-17.9903076061228),.UNSPECIFIED.);
#24603=B_SPLINE_CURVE_WITH_KNOTS('',3,(#361018,#361019,#361020,#361021,
#361022,#361023,#361024,#361025,#361026,#361027,#361028,#361029,#361030,
#361031,#361032,#361033,#361034,#361035,#361036,#361037,#361038,#361039,
#361040,#361041,#361042,#361043,#361044,#361045,#361046,#361047,#361048,
#361049,#361050,#361051,#361052,#361053),.UNSPECIFIED.,.F.,.F.,(4,2,2,2,
2,2,2,2,2,2,2,2,2,2,2,2,2,4),(-10.909574098799,-10.8808160295316,-10.8207156251837,
-10.7628910685625,-10.7034244813183,-10.6440976476971,-10.5868819744247,
-10.5269895075939,-10.4683112939554,-10.4107755782778,-10.3504750047583,
-10.2924703878915,-10.2335012948907,-10.173964376334,-10.1166141325046,
-10.0566876526939,-9.99779679495118,-9.9601521371041),.UNSPECIFIED.);
#24604=B_SPLINE_CURVE_WITH_KNOTS('',3,(#361058,#361059,#361060,#361061,
#361062,#361063,#361064,#361065,#361066,#361067,#361068,#361069,#361070,
#361071,#361072,#361073,#361074,#361075,#361076,#361077,#361078,#361079,
#361080,#361081,#361082,#361083,#361084,#361085,#361086,#361087,#361088,
#361089,#361090,#361091,#361092,#361093),.UNSPECIFIED.,.F.,.F.,(4,2,2,2,
2,2,2,2,2,2,2,2,2,2,2,2,2,4),(-19.8790955780054,-19.8401576940368,-19.7814977581655,
-19.7218695712742,-19.6647531524489,-19.6054516486236,-19.5469463032725,
-19.4891787722589,-19.4291197855388,-19.3719460257536,-19.3135074828106,
-19.2539244283835,-19.1969761629465,-19.1378932788518,-19.0789287482696,
-19.0213511210655,-18.9615029338211,-18.9344980393133),.UNSPECIFIED.);
#24605=B_SPLINE_CURVE_WITH_KNOTS('',3,(#361094,#361095,#361096,#361097,
#361098,#361099,#361100,#361101,#361102,#361103,#361104,#361105,#361106,
#361107,#361108,#361109,#361110,#361111,#361112,#361113,#361114,#361115,
#361116,#361117,#361118,#361119,#361120,#361121,#361122,#361123,#361124,
#361125,#361126,#361127,#361128,#361129),.UNSPECIFIED.,.F.,.F.,(4,2,2,2,
2,2,2,2,2,2,2,2,2,2,2,2,2,4),(-9.9601521371041,-9.94038824764174,-9.87985608738636,
-9.82164227553691,-9.76306311461492,-9.70329035061682,-9.64575796925551,
-9.58585532697708,-9.52686226224796,-9.46961036732748,-9.40969116987352,
-9.3513515529105,-9.29323419349764,-9.2333125037998,-9.17564770763484,-9.11552500244563,
-9.05639464257743,-9.01053220002199),.UNSPECIFIED.);
#24606=B_SPLINE_CURVE_WITH_KNOTS('',3,(#361134,#361135,#361136,#361137,
#361138,#361139,#361140,#361141,#361142,#361143,#361144,#361145,#361146,
#361147,#361148,#361149,#361150,#361151,#361152,#361153,#361154,#361155,
#361156,#361157,#361158,#361159,#361160,#361161,#361162,#361163,#361164,
#361165,#361166,#361167,#361168,#361169),.UNSPECIFIED.,.F.,.F.,(4,2,2,2,
2,2,2,2,2,2,2,2,2,2,2,2,2,4),(-20.8242710457994,-20.7765261092298,-20.7175778727164,
-20.6580053703026,-20.6005320267931,-20.540804205626,-20.4831026281961,
-20.4249588649431,-20.3653197791477,-20.3083624391667,-20.2495692688034,
-20.1899400450114,-20.1326074527045,-20.0730374502272,-20.0149326855893,
-19.9569251490987,-19.8972414747414,-19.8790955780054),.UNSPECIFIED.);
#24607=B_SPLINE_CURVE_WITH_KNOTS('',3,(#361170,#361171,#361172,#361173,
#361174,#361175,#361176,#361177,#361178,#361179,#361180,#361181,#361182,
#361183,#361184,#361185,#361186,#361187,#361188,#361189,#361190,#361191,
#361192,#361193,#361194,#361195,#361196,#361197,#361198,#361199,#361200,
#361201,#361202,#361203,#361204,#361205),.UNSPECIFIED.,.F.,.F.,(4,2,2,2,
2,2,2,2,2,2,2,2,2,2,2,2,2,4),(-9.01053220002199,-8.99921036745133,-8.9393184222242,
-8.88083915842011,-8.82304162701373,-8.76296130024007,-8.70515463521909,
-8.64561937780934,-8.58631424828878,-8.52910637261322,-8.46921405362235,
-8.41055784034516,-8.35299786190215,-8.29272154966623,-8.2347386804068,
-8.17571251580717,-8.11620077877754,-8.06130686846712),.UNSPECIFIED.);
#24608=B_SPLINE_CURVE_WITH_KNOTS('',3,(#361210,#361211,#361212,#361213,
#361214,#361215,#361216,#361217,#361218,#361219,#361220,#361221,#361222,
#361223,#361224,#361225,#361226,#361227,#361228,#361229,#361230,#361231,
#361232,#361233,#361234,#361235,#361236,#361237,#361238,#361239,#361240,
#361241,#361242,#361243,#361244,#361245),.UNSPECIFIED.,.F.,.F.,(4,2,2,2,
2,2,2,2,2,2,2,2,2,2,2,2,2,4),(-21.7695040114687,-21.712712284324,-21.6533554921043,
-21.5947945436566,-21.5369731193153,-21.4768581247202,-21.4196304517696,
-21.3611373908272,-21.3014984463427,-21.244496915496,-21.1853589043874,
-21.1263381651216,-21.0687067734505,-21.008802722821,-20.951383448243,-20.8930824171696,
-20.8334576289181,-20.8242710457994),.UNSPECIFIED.);
#24609=B_SPLINE_CURVE_WITH_KNOTS('',3,(#361246,#361247,#361248,#361249,
#361250,#361251,#361252,#361253,#361254,#361255,#361256,#361257,#361258,
#361259,#361260,#361261,#361262,#361263,#361264,#361265,#361266,#361267,
#361268,#361269,#361270,#361271,#361272,#361273,#361274,#361275,#361276,
#361277,#361278,#361279,#361280,#361281,#361282,#361283),.UNSPECIFIED.,
 .F.,.F.,(4,2,2,2,2,2,2,2,2,2,2,2,2,2,2,2,2,2,4),(-8.06130686846712,-8.05887034571654,
-7.99894782700157,-7.94008251681837,-7.88266222291039,-7.82215786151287,
-7.76396910049182,-7.70534692624004,-7.64560222270824,-7.58809574321899,
-7.52820385905816,-7.469238704033,-7.41198687597557,-7.35207690934848,-7.29376536285336,
-7.23561890186185,-7.17572793492865,-7.11809152052509,-7.11163898392485),
 .UNSPECIFIED.);
#24610=B_SPLINE_CURVE_WITH_KNOTS('',3,(#361288,#361289,#361290,#361291,
#361292,#361293,#361294,#361295,#361296,#361297,#361298,#361299,#361300,
#361301,#361302,#361303,#361304,#361305,#361306,#361307,#361308,#361309,
#361310,#361311,#361312,#361313,#361314,#361315,#361316,#361317,#361318,
#361319,#361320,#361321,#361322,#361323,#361324,#361325),.UNSPECIFIED.,
 .F.,.F.,(4,2,2,2,2,2,2,2,2,2,2,2,2,2,2,2,2,2,4),(-22.7156509715054,-22.7074186159329,
-22.6499177691702,-22.5901628966359,-22.5323690215547,-22.4741968613821,
-22.4145051589581,-22.3574909491047,-22.2986685245253,-22.238988725518,
-22.1816262395564,-22.1220266368737,-22.0638123939024,-22.0057734757511,
-21.9454180869479,-21.888280649569,-21.8295660328567,-21.7698819675377,
-21.7695040114687),.UNSPECIFIED.);
#24611=B_SPLINE_CURVE_WITH_KNOTS('',3,(#361326,#361327,#361328,#361329,
#361330,#361331,#361332,#361333,#361334,#361335,#361336,#361337,#361338,
#361339,#361340,#361341,#361342,#361343,#361344,#361345,#361346,#361347,
#361348,#361349,#361350,#361351,#361352,#361353,#361354,#361355,#361356,
#361357,#361358,#361359,#361360,#361361),.UNSPECIFIED.,.F.,.F.,(4,2,2,2,
2,2,2,2,2,2,2,2,2,2,2,2,2,4),(-7.11163898392485,-7.05790850141027,-6.99881095248213,
-6.94163674888716,-6.88175725112074,-6.82331090824414,-6.76549239782104,
-6.70544767686958,-6.64767387857181,-6.58808539206054,-6.52881735557916,
-6.47163120579824,-6.41175477442895,-6.353135767859,-6.29556581029132,-6.23532938765596,
-6.17738332888142,-6.16270708252577),.UNSPECIFIED.);
#24612=B_SPLINE_CURVE_WITH_KNOTS('',3,(#361366,#361367,#361368,#361369,
#361370,#361371,#361372,#361373,#361374,#361375,#361376,#361377,#361378,
#361379,#361380,#361381,#361382,#361383,#361384,#361385,#361386,#361387,
#361388,#361389,#361390,#361391,#361392,#361393,#361394,#361395,#361396,
#361397,#361398,#361399,#361400,#361401),.UNSPECIFIED.,.F.,.F.,(4,2,2,2,
2,2,2,2,2,2,2,2,2,2,2,2,2,4),(-23.6614844833627,-23.6449424473843,-23.5871022365362,
-23.5269696420123,-23.4696746996857,-23.4111627281875,-23.3514790699787,
-23.2944469148207,-23.2352891329381,-23.1761484454631,-23.1184942467699,
-23.0585682521832,-23.0010680928138,-22.9427437794047,-22.8830701897237,
-22.8260943458677,-22.7671220016819,-22.7156509715054),.UNSPECIFIED.);
#24613=B_SPLINE_CURVE_WITH_KNOTS('',3,(#361402,#361403,#361404,#361405,
#361406,#361407,#361408,#361409,#361410,#361411,#361412,#361413,#361414,
#361415,#361416,#361417,#361418,#361419,#361420,#361421,#361422,#361423,
#361424,#361425,#361426,#361427,#361428,#361429,#361430,#361431,#361432,
#361433,#361434,#361435,#361436,#361437),.UNSPECIFIED.,.F.,.F.,(4,2,2,2,
2,2,2,2,2,2,2,2,2,2,2,2,2,4),(-6.16270708252577,-6.11831491034659,-6.05884385447613,
-6.0015471618534,-5.94164428182563,-5.88281983108641,-5.82540186288241,
-5.76494103865069,-5.70679248475467,-5.64814168995376,-5.58844065129154,
-5.53097510832359,-5.47110961753744,-5.41218783882286,-5.35495023861937,
-5.29506519854675,-5.23679702670757,-5.21335483239024),.UNSPECIFIED.);
#24614=B_SPLINE_CURVE_WITH_KNOTS('',3,(#361442,#361443,#361444,#361445,
#361446,#361447,#361448,#361449,#361450,#361451,#361452,#361453,#361454,
#361455,#361456,#361457,#361458,#361459,#361460,#361461,#361462,#361463,
#361464,#361465,#361466,#361467,#361468,#361469,#361470,#361471,#361472,
#361473,#361474,#361475,#361476,#361477),.UNSPECIFIED.,.F.,.F.,(4,2,2,2,
2,2,2,2,2,2,2,2,2,2,2,2,2,4),(-24.6081837710824,-24.5830421019898,-24.5248574668377,
-24.4651313068841,-24.4080770368428,-24.3492414934905,-24.2895290755028,
-24.2321524812782,-24.1725395439001,-24.11423689657,-24.0561825895792,-23.9958132061658,
-23.9386229442598,-23.8798930451998,-23.8201687128849,-23.7629816327952,
-23.7036086069725,-23.6614844833627),.UNSPECIFIED.);
#24615=B_SPLINE_CURVE_WITH_KNOTS('',3,(#361478,#361479,#361480,#361481,
#361482,#361483,#361484,#361485,#361486,#361487,#361488,#361489,#361490,
#361491,#361492,#361493,#361494,#361495,#361496,#361497,#361498,#361499,
#361500,#361501,#361502,#361503,#361504,#361505,#361506,#361507,#361508,
#361509,#361510,#361511,#361512,#361513),.UNSPECIFIED.,.F.,.F.,(4,2,2,2,
2,2,2,2,2,2,2,2,2,2,2,2,2,4),(-5.21335483239024,-5.17863572644285,-5.11879123767709,
-5.06119837726108,-5.00096959629774,-4.94192049622973,-4.88477038234289,
-4.82491904471437,-4.7665210924622,-4.70869551497814,-4.64870233321989,
-4.59097673694955,-4.53134899118521,-4.47213387698101,-4.41498350464237,
-4.35513869118441,-4.29657254663883,-4.26486323252877),.UNSPECIFIED.);
#24616=B_SPLINE_CURVE_WITH_KNOTS('',3,(#361518,#361519,#361520,#361521,
#361522,#361523,#361524,#361525,#361526,#361527,#361528,#361529,#361530,
#361531,#361532,#361533,#361534,#361535,#361536,#361537,#361538,#361539,
#361540,#361541,#361542,#361543,#361544,#361545,#361546,#361547,#361548,
#361549,#361550,#361551,#361552,#361553),.UNSPECIFIED.,.F.,.F.,(4,2,2,2,
2,2,2,2,2,2,2,2,2,2,2,2,2,4),(-25.5544342108731,-25.5208509453158,-25.4623356142421,
-25.4026248008999,-25.3455767658485,-25.2864149936997,-25.2271757643632,
-25.1695143091372,-25.1095823895211,-25.0520197529052,-24.9936878585783,
-24.933983338271,-24.8769788824494,-24.8179983510985,-24.7581869330707,
-24.7006743283785,-24.6409086331248,-24.6081837710824),.UNSPECIFIED.);
#24617=B_SPLINE_CURVE_WITH_KNOTS('',3,(#361554,#361555,#361556,#361557,
#361558,#361559,#361560,#361561,#361562,#361563,#361564,#361565,#361566,
#361567,#361568,#361569,#361570,#361571,#361572,#361573,#361574,#361575,
#361576,#361577,#361578,#361579,#361580,#361581,#361582,#361583,#361584,
#361585,#361586,#361587,#361588,#361589),.UNSPECIFIED.,.F.,.F.,(4,2,2,2,
2,2,2,2,2,2,2,2,2,2,2,2,2,4),(-4.26486323252877,-4.23900633934104,-4.17882593258559,
-4.12093219325187,-4.06183508651317,-4.00242073272712,-3.94517207381186,
-3.88530458267638,-3.82653683258786,-3.76913495426055,-3.70873398371094,
-3.65064131432519,-3.59197531230959,-3.53233413127258,-3.47492510292252,
-3.4151018542262,-3.35623950860372,-3.31605621561602),.UNSPECIFIED.);
#24618=B_SPLINE_CURVE_WITH_KNOTS('',3,(#361594,#361595,#361596,#361597,
#361598,#361599,#361600,#361601,#361602,#361603,#361604,#361605,#361606,
#361607,#361608,#361609,#361610,#361611,#361612,#361613,#361614,#361615,
#361616,#361617,#361618,#361619,#361620,#361621,#361622,#361623,#361624,
#361625,#361626,#361627,#361628,#361629),.UNSPECIFIED.,.F.,.F.,(4,2,2,2,
2,2,2,2,2,2,2,2,2,2,2,2,2,4),(-26.5014317973833,-26.4595354955269,-26.4007023230101,
-26.3409740379703,-26.2835984636918,-26.2239878166713,-26.1656152908853,
-26.1075609039662,-26.0471933067983,-25.9899664269833,-25.9312366963228,
-25.8714893191867,-25.8142988852649,-25.754925315871,-25.6961738469028,
-25.6383302605847,-25.5781959419109,-25.5544342108731),.UNSPECIFIED.);
#24619=B_SPLINE_CURVE_WITH_KNOTS('',3,(#361630,#361631,#361632,#361633,
#361634,#361635,#361636,#361637,#361638,#361639,#361640,#361641,#361642,
#361643,#361644,#361645,#361646,#361647,#361648,#361649,#361650,#361651,
#361652,#361653,#361654,#361655,#361656,#361657,#361658,#361659,#361660,
#361661,#361662,#361663,#361664,#361665),.UNSPECIFIED.,.F.,.F.,(4,2,2,2,
2,2,2,2,2,2,2,2,2,2,2,2,2,4),(-3.31605621561602,-3.29903024172096,-3.23918601511716,
-3.18097711727524,-3.12281455031644,-3.0630329501645,-3.00549942169575,
-2.94523805588053,-2.88625374908926,-2.82914188076935,-2.76933468040783,
-2.71100129868167,-2.65318201778556,-2.5932570807603,-2.53559573555263,
-2.47594142993198,-2.41679587971833,-2.36822369355669),.UNSPECIFIED.);
#24620=B_SPLINE_CURVE_WITH_KNOTS('',3,(#361670,#361671,#361672,#361673,
#361674,#361675,#361676,#361677,#361678,#361679,#361680,#361681,#361682,
#361683,#361684,#361685,#361686,#361687,#361688,#361689,#361690,#361691,
#361692,#361693,#361694,#361695,#361696,#361697,#361698,#361699,#361700,
#361701,#361702,#361703,#361704,#361705),.UNSPECIFIED.,.F.,.F.,(4,2,2,2,
2,2,2,2,2,2,2,2,2,2,2,2,2,4),(-27.4478726632988,-27.3973197261978,-27.3381693061291,
-27.2788502071366,-27.2211965408828,-27.1612742376035,-27.1036657370775,
-27.0453414526527,-26.985622716861,-26.9286045043193,-26.8696311738349,
-26.8097314960196,-26.7522222685197,-26.6924613878446,-26.6345397360654,
-26.5763579231836,-26.5166142076797,-26.5014317973833),.UNSPECIFIED.);
#24621=B_SPLINE_CURVE_WITH_KNOTS('',3,(#361706,#361707,#361708,#361709,
#361710,#361711,#361712,#361713,#361714,#361715,#361716,#361717,#361718,
#361719,#361720,#361721,#361722,#361723,#361724,#361725,#361726,#361727,
#361728,#361729,#361730,#361731,#361732,#361733,#361734,#361735,#361736,
#361737,#361738,#361739,#361740,#361741,#361742,#361743),.UNSPECIFIED.,
 .F.,.F.,(4,2,2,2,2,2,2,2,2,2,2,2,2,2,2,2,2,2,4),(-2.36822369355669,-2.35969570935163,
-2.29989858662437,-2.24140177574115,-2.18385270788337,-2.12374532233508,
-2.06592022370505,-2.00680691534119,-1.94746619110531,-1.89028049072034,
-1.8304645649493,-1.77177026671126,-1.71439815249335,-1.65407432487789,
-1.59605411659167,-1.53738550579103,-1.47782136059953,-1.42048534994002,
-1.42021042679425),.UNSPECIFIED.);
#24622=B_SPLINE_CURVE_WITH_KNOTS('',3,(#361748,#361749,#361750,#361751,
#361752,#361753,#361754,#361755,#361756,#361757,#361758,#361759,#361760,
#361761,#361762,#361763,#361764,#361765,#361766,#361767,#361768,#361769,
#361770,#361771,#361772,#361773,#361774,#361775,#361776,#361777,#361778,
#361779,#361780,#361781,#361782,#361783,#361784,#361785),.UNSPECIFIED.,
 .F.,.F.,(4,2,2,2,2,2,2,2,2,2,2,2,2,2,2,2,2,2,4),(-28.394928409372,-28.3927695114757,
-28.335409770902,-28.2758167453806,-28.2173909528416,-28.1593514570261,
-28.0990011252068,-28.0417527514382,-27.9830383059222,-27.9232841801495,
-27.8661041969916,-27.8067454140552,-27.7479262063714,-27.6900942406652,
-27.6299736919414,-27.5725944329335,-27.5140908788942,-27.4543694236753,
-27.4478726632988),.UNSPECIFIED.);
#24623=B_SPLINE_CURVE_WITH_KNOTS('',3,(#361786,#361787,#361788,#361789,
#361790,#361791,#361792,#361793,#361794,#361795,#361796,#361797,#361798,
#361799,#361800,#361801,#361802,#361803,#361804,#361805,#361806,#361807,
#361808,#361809,#361810,#361811,#361812,#361813,#361814,#361815,#361816,
#361817,#361818,#361819,#361820,#361821),.UNSPECIFIED.,.F.,.F.,(4,2,2,2,
2,2,2,2,2,2,2,2,2,2,2,2,2,4),(-1.42021042679425,-1.36072076805539,-1.30193490150738,
-1.24476826914458,-1.18498130105108,-1.12684856833088,-1.06869780383765,
-1.00899657270127,-0.951539157864885,-0.891257122095936,-0.832355083013897,
-0.77529600850504,-0.715549563214565,-0.657298062625355,-0.599498063457814,
-0.539659288862095,-0.482079378649015,-0.473202703359355),.UNSPECIFIED.);
#24624=B_SPLINE_CURVE_WITH_KNOTS('',3,(#361844,#361845,#361846,#361847,
#361848,#361849,#361850,#361851,#361852,#361853,#361854,#361855),
 .UNSPECIFIED.,.F.,.F.,(4,2,2,2,2,4),(-0.173463023786657,-0.144399277485174,
-0.113776308502816,-0.0827143528997853,-0.0458804636919242,-1.0000001323951E-6),
 .UNSPECIFIED.);
#24625=B_SPLINE_CURVE_WITH_KNOTS('',3,(#361859,#361860,#361861,#361862,
#361863,#361864,#361865,#361866,#361867,#361868,#361869,#361870,#361871,
#361872,#361873,#361874,#361875,#361876,#361877,#361878,#361879,#361880,
#361881,#361882),.UNSPECIFIED.,.F.,.F.,(4,2,2,2,2,2,2,2,2,2,2,4),(-0.791270207765327,
-0.749036169028397,-0.706407085981735,-0.662154327887133,-0.624122080956691,
-0.588829396109561,-0.540761862599491,-0.472209855066893,-0.406689863879307,
-0.338868299808933,-0.273977253007298,-0.246317319594991),.UNSPECIFIED.);
#24626=B_SPLINE_CURVE_WITH_KNOTS('',3,(#361886,#361887,#361888,#361889,
#361890,#361891,#361892,#361893,#361894,#361895,#361896,#361897,#361898,
#361899,#361900,#361901),.UNSPECIFIED.,.F.,.F.,(4,2,2,2,2,2,2,4),(-0.246317319594991,
-0.226472527001757,-0.19198199334467,-0.155250487805907,-0.119808408672289,
-0.0860490564446136,-0.045855268046708,0.),.UNSPECIFIED.);
#24627=B_SPLINE_CURVE_WITH_KNOTS('',3,(#361904,#361905,#361906,#361907,
#361908,#361909,#361910,#361911,#361912,#361913,#361914,#361915,#361916,
#361917,#361918,#361919,#361920,#361921,#361922,#361923),.UNSPECIFIED.,
 .F.,.F.,(4,2,2,2,2,2,2,2,2,4),(-0.473202703359355,-0.422410017693474,-0.363351937608626,
-0.306317042413269,-0.246584411472418,-0.188174667531023,-0.130655960205244,
-0.0706399456385561,-0.0347067012271464,0.),.UNSPECIFIED.);
#24628=B_SPLINE_CURVE_WITH_KNOTS('',3,(#361931,#361932,#361933,#361934,
#361935,#361936,#361937,#361938,#361939,#361940,#361941,#361942,#361943,
#361944,#361945,#361946,#361947,#361948,#361949,#361950,#361951,#361952,
#361953,#361954,#361955,#361956,#361957,#361958),.UNSPECIFIED.,.F.,.F.,
(4,2,2,2,2,2,2,2,2,2,2,2,2,4),(-29.1046910466764,-29.0706370137762,-29.0374414130779,
-28.9804238291734,-28.9214729766087,-28.8615025430861,-28.8040116402705,
-28.7442710501027,-28.6863103369922,-28.628146444495,-28.568401372388,-28.5113131027202,
-28.4524975774518,-28.394928409372),.UNSPECIFIED.);
#24629=B_SPLINE_CURVE_WITH_KNOTS('',3,(#361961,#361962,#361963,#361964,
#361965,#361966,#361967,#361968,#361969,#361970,#361971,#361972,#361973,
#361974,#361975,#361976,#361977,#361978),.UNSPECIFIED.,.F.,.F.,(4,2,2,2,
2,2,2,2,4),(0.,0.0314998749400598,0.0537169728612125,0.079677450094962,
0.104184647840863,0.128403600561281,0.152338152262454,0.16487497823377,
0.178500527166238),.UNSPECIFIED.);
#24630=B_SPLINE_CURVE_WITH_KNOTS('',3,(#361979,#361980,#361981,#361982,
#361983,#361984,#361985,#361986,#361987,#361988,#361989,#361990,#361991,
#361992,#361993,#361994),.UNSPECIFIED.,.F.,.F.,(4,2,2,2,2,2,2,4),(0.,0.0490384475420047,
0.0900695236875757,0.13296300706505,0.166655888849848,0.19179904034312,
0.208292684427657,0.22546835719786),.UNSPECIFIED.);
#28898=LINE('',#358530,#32700);
#28899=LINE('',#358563,#32701);
#28900=LINE('',#358593,#32702);
#28901=LINE('',#358623,#32703);
#28902=LINE('',#358653,#32704);
#28903=LINE('',#358683,#32705);
#28904=LINE('',#358713,#32706);
#28905=LINE('',#358743,#32707);
#28906=LINE('',#358773,#32708);
#28907=LINE('',#358803,#32709);
#28908=LINE('',#358833,#32710);
#28909=LINE('',#358863,#32711);
#28910=LINE('',#358893,#32712);
#28911=LINE('',#358923,#32713);
#28912=LINE('',#358953,#32714);
#28913=LINE('',#358983,#32715);
#28914=LINE('',#359013,#32716);
#28915=LINE('',#359043,#32717);
#28916=LINE('',#359073,#32718);
#28917=LINE('',#359103,#32719);
#28918=LINE('',#359133,#32720);
#28919=LINE('',#359163,#32721);
#28920=LINE('',#359193,#32722);
#28921=LINE('',#359223,#32723);
#28922=LINE('',#359253,#32724);
#28923=LINE('',#359283,#32725);
#28924=LINE('',#359313,#32726);
#28925=LINE('',#359343,#32727);
#28926=LINE('',#359373,#32728);
#28927=LINE('',#359403,#32729);
#28928=LINE('',#359433,#32730);
#28929=LINE('',#359463,#32731);
#28930=LINE('',#359495,#32732);
#28931=LINE('',#359525,#32733);
#28932=LINE('',#359601,#32734);
#28933=LINE('',#359677,#32735);
#28934=LINE('',#359755,#32736);
#28935=LINE('',#359833,#32737);
#28936=LINE('',#359909,#32738);
#28937=LINE('',#359985,#32739);
#28938=LINE('',#360061,#32740);
#28939=LINE('',#360137,#32741);
#28940=LINE('',#360215,#32742);
#28941=LINE('',#360293,#32743);
#28942=LINE('',#360369,#32744);
#28943=LINE('',#360445,#32745);
#28944=LINE('',#360521,#32746);
#28945=LINE('',#360597,#32747);
#28946=LINE('',#360673,#32748);
#28947=LINE('',#360751,#32749);
#28948=LINE('',#360829,#32750);
#28949=LINE('',#360905,#32751);
#28950=LINE('',#360981,#32752);
#28951=LINE('',#361057,#32753);
#28952=LINE('',#361133,#32754);
#28953=LINE('',#361209,#32755);
#28954=LINE('',#361287,#32756);
#28955=LINE('',#361365,#32757);
#28956=LINE('',#361441,#32758);
#28957=LINE('',#361517,#32759);
#28958=LINE('',#361593,#32760);
#28959=LINE('',#361669,#32761);
#28960=LINE('',#361747,#32762);
#28961=LINE('',#361838,#32763);
#28962=LINE('',#361884,#32764);
#28963=LINE('',#362029,#32765);
#28964=LINE('',#362031,#32766);
#28965=LINE('',#362033,#32767);
#28966=LINE('',#362035,#32768);
#28967=LINE('',#362037,#32769);
#28968=LINE('',#362038,#32770);
#28969=LINE('',#362040,#32771);
#28970=LINE('',#362041,#32772);
#28971=LINE('',#362043,#32773);
#28972=LINE('',#362045,#32774);
#28973=LINE('',#362047,#32775);
#28974=LINE('',#362049,#32776);
#32700=VECTOR('',#115726,1.17524047358084);
#32701=VECTOR('',#115731,1.17524047358084);
#32702=VECTOR('',#115734,1.17524047358084);
#32703=VECTOR('',#115737,1.17524047358084);
#32704=VECTOR('',#115740,1.17524047358084);
#32705=VECTOR('',#115743,1.17524047358084);
#32706=VECTOR('',#115746,1.17524047358084);
#32707=VECTOR('',#115749,1.17524047358084);
#32708=VECTOR('',#115752,1.17524047358084);
#32709=VECTOR('',#115755,1.17524047358084);
#32710=VECTOR('',#115758,1.17524047358084);
#32711=VECTOR('',#115761,1.17524047358084);
#32712=VECTOR('',#115764,1.17524047358084);
#32713=VECTOR('',#115767,1.17524047358084);
#32714=VECTOR('',#115770,1.17524047358084);
#32715=VECTOR('',#115773,1.17524047358084);
#32716=VECTOR('',#115776,1.17524047358084);
#32717=VECTOR('',#115779,1.17524047358084);
#32718=VECTOR('',#115782,1.17524047358084);
#32719=VECTOR('',#115785,1.17524047358084);
#32720=VECTOR('',#115788,1.17524047358084);
#32721=VECTOR('',#115791,1.17524047358084);
#32722=VECTOR('',#115794,1.17524047358084);
#32723=VECTOR('',#115797,1.17524047358084);
#32724=VECTOR('',#115800,1.17524047358084);
#32725=VECTOR('',#115803,1.17524047358084);
#32726=VECTOR('',#115806,1.17524047358084);
#32727=VECTOR('',#115809,1.17524047358084);
#32728=VECTOR('',#115812,1.17524047358084);
#32729=VECTOR('',#115815,1.17524047358084);
#32730=VECTOR('',#115818,1.17524047358084);
#32731=VECTOR('',#115821,1.17524047358084);
#32732=VECTOR('',#115826,1.5);
#32733=VECTOR('',#115831,1.5);
#32734=VECTOR('',#115834,1.5);
#32735=VECTOR('',#115837,1.5);
#32736=VECTOR('',#115840,1.5);
#32737=VECTOR('',#115843,1.5);
#32738=VECTOR('',#115846,1.5);
#32739=VECTOR('',#115849,1.5);
#32740=VECTOR('',#115852,1.5);
#32741=VECTOR('',#115855,1.5);
#32742=VECTOR('',#115858,1.5);
#32743=VECTOR('',#115861,1.5);
#32744=VECTOR('',#115864,1.5);
#32745=VECTOR('',#115867,1.5);
#32746=VECTOR('',#115870,1.5);
#32747=VECTOR('',#115873,1.5);
#32748=VECTOR('',#115876,1.5);
#32749=VECTOR('',#115879,1.5);
#32750=VECTOR('',#115882,1.5);
#32751=VECTOR('',#115885,1.5);
#32752=VECTOR('',#115888,1.5);
#32753=VECTOR('',#115891,1.5);
#32754=VECTOR('',#115894,1.5);
#32755=VECTOR('',#115897,1.5);
#32756=VECTOR('',#115900,1.5);
#32757=VECTOR('',#115903,1.5);
#32758=VECTOR('',#115906,1.5);
#32759=VECTOR('',#115909,1.5);
#32760=VECTOR('',#115912,1.5);
#32761=VECTOR('',#115915,1.5);
#32762=VECTOR('',#115918,1.5);
#32763=VECTOR('',#115933,3.5);
#32764=VECTOR('',#115942,1.125);
#32765=VECTOR('',#115977,1000.);
#32766=VECTOR('',#115978,1000.);
#32767=VECTOR('',#115979,1000.);
#32768=VECTOR('',#115980,1000.);
#32769=VECTOR('',#115981,1000.);
#32770=VECTOR('',#115982,1000.);
#32771=VECTOR('',#115985,1000.);
#32772=VECTOR('',#115986,1000.);
#32773=VECTOR('',#115989,1000.);
#32774=VECTOR('',#115992,1000.);
#32775=VECTOR('',#115995,1000.);
#32776=VECTOR('',#115998,1000.);
#38128=VERTEX_POINT('',#358528);
#38129=VERTEX_POINT('',#358529);
#38130=VERTEX_POINT('',#358531);
#38131=VERTEX_POINT('',#358545);
#38132=VERTEX_POINT('',#358561);
#38133=VERTEX_POINT('',#358562);
#38134=VERTEX_POINT('',#358591);
#38135=VERTEX_POINT('',#358592);
#38136=VERTEX_POINT('',#358621);
#38137=VERTEX_POINT('',#358622);
#38138=VERTEX_POINT('',#358651);
#38139=VERTEX_POINT('',#358652);
#38140=VERTEX_POINT('',#358681);
#38141=VERTEX_POINT('',#358682);
#38142=VERTEX_POINT('',#358711);
#38143=VERTEX_POINT('',#358712);
#38144=VERTEX_POINT('',#358741);
#38145=VERTEX_POINT('',#358742);
#38146=VERTEX_POINT('',#358771);
#38147=VERTEX_POINT('',#358772);
#38148=VERTEX_POINT('',#358801);
#38149=VERTEX_POINT('',#358802);
#38150=VERTEX_POINT('',#358831);
#38151=VERTEX_POINT('',#358832);
#38152=VERTEX_POINT('',#358861);
#38153=VERTEX_POINT('',#358862);
#38154=VERTEX_POINT('',#358891);
#38155=VERTEX_POINT('',#358892);
#38156=VERTEX_POINT('',#358921);
#38157=VERTEX_POINT('',#358922);
#38158=VERTEX_POINT('',#358951);
#38159=VERTEX_POINT('',#358952);
#38160=VERTEX_POINT('',#358981);
#38161=VERTEX_POINT('',#358982);
#38162=VERTEX_POINT('',#359011);
#38163=VERTEX_POINT('',#359012);
#38164=VERTEX_POINT('',#359041);
#38165=VERTEX_POINT('',#359042);
#38166=VERTEX_POINT('',#359071);
#38167=VERTEX_POINT('',#359072);
#38168=VERTEX_POINT('',#359101);
#38169=VERTEX_POINT('',#359102);
#38170=VERTEX_POINT('',#359131);
#38171=VERTEX_POINT('',#359132);
#38172=VERTEX_POINT('',#359161);
#38173=VERTEX_POINT('',#359162);
#38174=VERTEX_POINT('',#359191);
#38175=VERTEX_POINT('',#359192);
#38176=VERTEX_POINT('',#359221);
#38177=VERTEX_POINT('',#359222);
#38178=VERTEX_POINT('',#359251);
#38179=VERTEX_POINT('',#359252);
#38180=VERTEX_POINT('',#359281);
#38181=VERTEX_POINT('',#359282);
#38182=VERTEX_POINT('',#359311);
#38183=VERTEX_POINT('',#359312);
#38184=VERTEX_POINT('',#359341);
#38185=VERTEX_POINT('',#359342);
#38186=VERTEX_POINT('',#359371);
#38187=VERTEX_POINT('',#359372);
#38188=VERTEX_POINT('',#359401);
#38189=VERTEX_POINT('',#359402);
#38190=VERTEX_POINT('',#359431);
#38191=VERTEX_POINT('',#359432);
#38192=VERTEX_POINT('',#359461);
#38193=VERTEX_POINT('',#359462);
#38194=VERTEX_POINT('',#359464);
#38195=VERTEX_POINT('',#359493);
#38196=VERTEX_POINT('',#359494);
#38197=VERTEX_POINT('',#359496);
#38198=VERTEX_POINT('',#359504);
#38199=VERTEX_POINT('',#359523);
#38200=VERTEX_POINT('',#359524);
#38201=VERTEX_POINT('',#359599);
#38202=VERTEX_POINT('',#359600);
#38203=VERTEX_POINT('',#359675);
#38204=VERTEX_POINT('',#359676);
#38205=VERTEX_POINT('',#359753);
#38206=VERTEX_POINT('',#359754);
#38207=VERTEX_POINT('',#359831);
#38208=VERTEX_POINT('',#359832);
#38209=VERTEX_POINT('',#359907);
#38210=VERTEX_POINT('',#359908);
#38211=VERTEX_POINT('',#359983);
#38212=VERTEX_POINT('',#359984);
#38213=VERTEX_POINT('',#360059);
#38214=VERTEX_POINT('',#360060);
#38215=VERTEX_POINT('',#360135);
#38216=VERTEX_POINT('',#360136);
#38217=VERTEX_POINT('',#360213);
#38218=VERTEX_POINT('',#360214);
#38219=VERTEX_POINT('',#360291);
#38220=VERTEX_POINT('',#360292);
#38221=VERTEX_POINT('',#360367);
#38222=VERTEX_POINT('',#360368);
#38223=VERTEX_POINT('',#360443);
#38224=VERTEX_POINT('',#360444);
#38225=VERTEX_POINT('',#360519);
#38226=VERTEX_POINT('',#360520);
#38227=VERTEX_POINT('',#360595);
#38228=VERTEX_POINT('',#360596);
#38229=VERTEX_POINT('',#360671);
#38230=VERTEX_POINT('',#360672);
#38231=VERTEX_POINT('',#360749);
#38232=VERTEX_POINT('',#360750);
#38233=VERTEX_POINT('',#360827);
#38234=VERTEX_POINT('',#360828);
#38235=VERTEX_POINT('',#360903);
#38236=VERTEX_POINT('',#360904);
#38237=VERTEX_POINT('',#360979);
#38238=VERTEX_POINT('',#360980);
#38239=VERTEX_POINT('',#361055);
#38240=VERTEX_POINT('',#361056);
#38241=VERTEX_POINT('',#361131);
#38242=VERTEX_POINT('',#361132);
#38243=VERTEX_POINT('',#361207);
#38244=VERTEX_POINT('',#361208);
#38245=VERTEX_POINT('',#361285);
#38246=VERTEX_POINT('',#361286);
#38247=VERTEX_POINT('',#361363);
#38248=VERTEX_POINT('',#361364);
#38249=VERTEX_POINT('',#361439);
#38250=VERTEX_POINT('',#361440);
#38251=VERTEX_POINT('',#361515);
#38252=VERTEX_POINT('',#361516);
#38253=VERTEX_POINT('',#361591);
#38254=VERTEX_POINT('',#361592);
#38255=VERTEX_POINT('',#361667);
#38256=VERTEX_POINT('',#361668);
#38257=VERTEX_POINT('',#361745);
#38258=VERTEX_POINT('',#361746);
#38259=VERTEX_POINT('',#361823);
#38260=VERTEX_POINT('',#361824);
#38261=VERTEX_POINT('',#361830);
#38262=VERTEX_POINT('',#361832);
#38263=VERTEX_POINT('',#361835);
#38264=VERTEX_POINT('',#361837);
#38265=VERTEX_POINT('',#361841);
#38266=VERTEX_POINT('',#361843);
#38267=VERTEX_POINT('',#361856);
#38268=VERTEX_POINT('',#361858);
#38269=VERTEX_POINT('',#361883);
#38270=VERTEX_POINT('',#361903);
#38271=VERTEX_POINT('',#361997);
#38272=VERTEX_POINT('',#361998);
#38273=VERTEX_POINT('',#362000);
#38274=VERTEX_POINT('',#362003);
#38275=VERTEX_POINT('',#362027);
#38276=VERTEX_POINT('',#362028);
#38277=VERTEX_POINT('',#362030);
#38278=VERTEX_POINT('',#362032);
#38279=VERTEX_POINT('',#362034);
#38280=VERTEX_POINT('',#362036);
#48887=EDGE_CURVE('',#38128,#38129,#28898,.T.);
#48888=EDGE_CURVE('',#38128,#38130,#4112,.T.);
#48889=EDGE_CURVE('',#38130,#38131,#20518,.T.);
#48890=EDGE_CURVE('',#38129,#38131,#4113,.T.);
#48891=EDGE_CURVE('',#38132,#38133,#28899,.T.);
#48892=EDGE_CURVE('',#38132,#38128,#4114,.T.);
#48893=EDGE_CURVE('',#38133,#38129,#4115,.T.);
#48894=EDGE_CURVE('',#38134,#38135,#28900,.T.);
#48895=EDGE_CURVE('',#38134,#38132,#4116,.T.);
#48896=EDGE_CURVE('',#38135,#38133,#4117,.T.);
#48897=EDGE_CURVE('',#38136,#38137,#28901,.T.);
#48898=EDGE_CURVE('',#38136,#38134,#4118,.T.);
#48899=EDGE_CURVE('',#38137,#38135,#4119,.T.);
#48900=EDGE_CURVE('',#38138,#38139,#28902,.T.);
#48901=EDGE_CURVE('',#38138,#38136,#4120,.T.);
#48902=EDGE_CURVE('',#38139,#38137,#4121,.T.);
#48903=EDGE_CURVE('',#38140,#38141,#28903,.T.);
#48904=EDGE_CURVE('',#38140,#38138,#4122,.T.);
#48905=EDGE_CURVE('',#38141,#38139,#4123,.T.);
#48906=EDGE_CURVE('',#38142,#38143,#28904,.T.);
#48907=EDGE_CURVE('',#38142,#38140,#4124,.T.);
#48908=EDGE_CURVE('',#38143,#38141,#4125,.T.);
#48909=EDGE_CURVE('',#38144,#38145,#28905,.T.);
#48910=EDGE_CURVE('',#38144,#38142,#4126,.T.);
#48911=EDGE_CURVE('',#38145,#38143,#4127,.T.);
#48912=EDGE_CURVE('',#38146,#38147,#28906,.T.);
#48913=EDGE_CURVE('',#38146,#38144,#4128,.T.);
#48914=EDGE_CURVE('',#38147,#38145,#4129,.T.);
#48915=EDGE_CURVE('',#38148,#38149,#28907,.T.);
#48916=EDGE_CURVE('',#38148,#38146,#4130,.T.);
#48917=EDGE_CURVE('',#38149,#38147,#4131,.T.);
#48918=EDGE_CURVE('',#38150,#38151,#28908,.T.);
#48919=EDGE_CURVE('',#38150,#38148,#4132,.T.);
#48920=EDGE_CURVE('',#38151,#38149,#4133,.T.);
#48921=EDGE_CURVE('',#38152,#38153,#28909,.T.);
#48922=EDGE_CURVE('',#38152,#38150,#4134,.T.);
#48923=EDGE_CURVE('',#38153,#38151,#4135,.T.);
#48924=EDGE_CURVE('',#38154,#38155,#28910,.T.);
#48925=EDGE_CURVE('',#38154,#38152,#4136,.T.);
#48926=EDGE_CURVE('',#38155,#38153,#4137,.T.);
#48927=EDGE_CURVE('',#38156,#38157,#28911,.T.);
#48928=EDGE_CURVE('',#38156,#38154,#4138,.T.);
#48929=EDGE_CURVE('',#38157,#38155,#4139,.T.);
#48930=EDGE_CURVE('',#38158,#38159,#28912,.T.);
#48931=EDGE_CURVE('',#38158,#38156,#4140,.T.);
#48932=EDGE_CURVE('',#38159,#38157,#4141,.T.);
#48933=EDGE_CURVE('',#38160,#38161,#28913,.T.);
#48934=EDGE_CURVE('',#38160,#38158,#4142,.T.);
#48935=EDGE_CURVE('',#38161,#38159,#4143,.T.);
#48936=EDGE_CURVE('',#38162,#38163,#28914,.T.);
#48937=EDGE_CURVE('',#38162,#38160,#4144,.T.);
#48938=EDGE_CURVE('',#38163,#38161,#4145,.T.);
#48939=EDGE_CURVE('',#38164,#38165,#28915,.T.);
#48940=EDGE_CURVE('',#38164,#38162,#4146,.T.);
#48941=EDGE_CURVE('',#38165,#38163,#4147,.T.);
#48942=EDGE_CURVE('',#38166,#38167,#28916,.T.);
#48943=EDGE_CURVE('',#38166,#38164,#4148,.T.);
#48944=EDGE_CURVE('',#38167,#38165,#4149,.T.);
#48945=EDGE_CURVE('',#38168,#38169,#28917,.T.);
#48946=EDGE_CURVE('',#38168,#38166,#4150,.T.);
#48947=EDGE_CURVE('',#38169,#38167,#4151,.T.);
#48948=EDGE_CURVE('',#38170,#38171,#28918,.T.);
#48949=EDGE_CURVE('',#38170,#38168,#4152,.T.);
#48950=EDGE_CURVE('',#38171,#38169,#4153,.T.);
#48951=EDGE_CURVE('',#38172,#38173,#28919,.T.);
#48952=EDGE_CURVE('',#38172,#38170,#4154,.T.);
#48953=EDGE_CURVE('',#38173,#38171,#4155,.T.);
#48954=EDGE_CURVE('',#38174,#38175,#28920,.T.);
#48955=EDGE_CURVE('',#38174,#38172,#4156,.T.);
#48956=EDGE_CURVE('',#38175,#38173,#4157,.T.);
#48957=EDGE_CURVE('',#38176,#38177,#28921,.T.);
#48958=EDGE_CURVE('',#38176,#38174,#4158,.T.);
#48959=EDGE_CURVE('',#38177,#38175,#4159,.T.);
#48960=EDGE_CURVE('',#38178,#38179,#28922,.T.);
#48961=EDGE_CURVE('',#38178,#38176,#4160,.T.);
#48962=EDGE_CURVE('',#38179,#38177,#4161,.T.);
#48963=EDGE_CURVE('',#38180,#38181,#28923,.T.);
#48964=EDGE_CURVE('',#38180,#38178,#4162,.T.);
#48965=EDGE_CURVE('',#38181,#38179,#4163,.T.);
#48966=EDGE_CURVE('',#38182,#38183,#28924,.T.);
#48967=EDGE_CURVE('',#38182,#38180,#4164,.T.);
#48968=EDGE_CURVE('',#38183,#38181,#4165,.T.);
#48969=EDGE_CURVE('',#38184,#38185,#28925,.T.);
#48970=EDGE_CURVE('',#38184,#38182,#4166,.T.);
#48971=EDGE_CURVE('',#38185,#38183,#4167,.T.);
#48972=EDGE_CURVE('',#38186,#38187,#28926,.T.);
#48973=EDGE_CURVE('',#38186,#38184,#4168,.T.);
#48974=EDGE_CURVE('',#38187,#38185,#4169,.T.);
#48975=EDGE_CURVE('',#38188,#38189,#28927,.T.);
#48976=EDGE_CURVE('',#38188,#38186,#4170,.T.);
#48977=EDGE_CURVE('',#38189,#38187,#4171,.T.);
#48978=EDGE_CURVE('',#38190,#38191,#28928,.T.);
#48979=EDGE_CURVE('',#38190,#38188,#4172,.T.);
#48980=EDGE_CURVE('',#38191,#38189,#4173,.T.);
#48981=EDGE_CURVE('',#38192,#38193,#28929,.T.);
#48982=EDGE_CURVE('',#38194,#38192,#20519,.T.);
#48983=EDGE_CURVE('',#38194,#38190,#4174,.T.);
#48984=EDGE_CURVE('',#38193,#38191,#4175,.T.);
#48985=EDGE_CURVE('',#38195,#38196,#28930,.T.);
#48986=EDGE_CURVE('',#38195,#38197,#4176,.T.);
#48987=EDGE_CURVE('',#38197,#38198,#20520,.T.);
#48988=EDGE_CURVE('',#38196,#38198,#24563,.F.);
#48989=EDGE_CURVE('',#38199,#38200,#28931,.T.);
#48990=EDGE_CURVE('',#38199,#38195,#24564,.T.);
#48991=EDGE_CURVE('',#38200,#38196,#24565,.F.);
#48992=EDGE_CURVE('',#38201,#38202,#28932,.T.);
#48993=EDGE_CURVE('',#38201,#38199,#24566,.T.);
#48994=EDGE_CURVE('',#38202,#38200,#24567,.F.);
#48995=EDGE_CURVE('',#38203,#38204,#28933,.T.);
#48996=EDGE_CURVE('',#38203,#38201,#24568,.T.);
#48997=EDGE_CURVE('',#38204,#38202,#24569,.F.);
#48998=EDGE_CURVE('',#38205,#38206,#28934,.T.);
#48999=EDGE_CURVE('',#38205,#38203,#24570,.T.);
#49000=EDGE_CURVE('',#38206,#38204,#24571,.F.);
#49001=EDGE_CURVE('',#38207,#38208,#28935,.T.);
#49002=EDGE_CURVE('',#38207,#38205,#24572,.T.);
#49003=EDGE_CURVE('',#38208,#38206,#24573,.F.);
#49004=EDGE_CURVE('',#38209,#38210,#28936,.T.);
#49005=EDGE_CURVE('',#38209,#38207,#24574,.T.);
#49006=EDGE_CURVE('',#38210,#38208,#24575,.F.);
#49007=EDGE_CURVE('',#38211,#38212,#28937,.T.);
#49008=EDGE_CURVE('',#38211,#38209,#24576,.T.);
#49009=EDGE_CURVE('',#38212,#38210,#24577,.F.);
#49010=EDGE_CURVE('',#38213,#38214,#28938,.T.);
#49011=EDGE_CURVE('',#38213,#38211,#24578,.T.);
#49012=EDGE_CURVE('',#38214,#38212,#24579,.F.);
#49013=EDGE_CURVE('',#38215,#38216,#28939,.T.);
#49014=EDGE_CURVE('',#38215,#38213,#24580,.T.);
#49015=EDGE_CURVE('',#38216,#38214,#24581,.F.);
#49016=EDGE_CURVE('',#38217,#38218,#28940,.T.);
#49017=EDGE_CURVE('',#38217,#38215,#24582,.T.);
#49018=EDGE_CURVE('',#38218,#38216,#24583,.F.);
#49019=EDGE_CURVE('',#38219,#38220,#28941,.T.);
#49020=EDGE_CURVE('',#38219,#38217,#24584,.T.);
#49021=EDGE_CURVE('',#38220,#38218,#24585,.F.);
#49022=EDGE_CURVE('',#38221,#38222,#28942,.T.);
#49023=EDGE_CURVE('',#38221,#38219,#24586,.T.);
#49024=EDGE_CURVE('',#38222,#38220,#24587,.F.);
#49025=EDGE_CURVE('',#38223,#38224,#28943,.T.);
#49026=EDGE_CURVE('',#38223,#38221,#24588,.T.);
#49027=EDGE_CURVE('',#38224,#38222,#24589,.F.);
#49028=EDGE_CURVE('',#38225,#38226,#28944,.T.);
#49029=EDGE_CURVE('',#38225,#38223,#24590,.T.);
#49030=EDGE_CURVE('',#38226,#38224,#24591,.F.);
#49031=EDGE_CURVE('',#38227,#38228,#28945,.T.);
#49032=EDGE_CURVE('',#38227,#38225,#24592,.T.);
#49033=EDGE_CURVE('',#38228,#38226,#24593,.F.);
#49034=EDGE_CURVE('',#38229,#38230,#28946,.T.);
#49035=EDGE_CURVE('',#38229,#38227,#24594,.T.);
#49036=EDGE_CURVE('',#38230,#38228,#24595,.F.);
#49037=EDGE_CURVE('',#38231,#38232,#28947,.T.);
#49038=EDGE_CURVE('',#38231,#38229,#24596,.T.);
#49039=EDGE_CURVE('',#38232,#38230,#24597,.F.);
#49040=EDGE_CURVE('',#38233,#38234,#28948,.T.);
#49041=EDGE_CURVE('',#38233,#38231,#24598,.T.);
#49042=EDGE_CURVE('',#38234,#38232,#24599,.F.);
#49043=EDGE_CURVE('',#38235,#38236,#28949,.T.);
#49044=EDGE_CURVE('',#38235,#38233,#24600,.T.);
#49045=EDGE_CURVE('',#38236,#38234,#24601,.F.);
#49046=EDGE_CURVE('',#38237,#38238,#28950,.T.);
#49047=EDGE_CURVE('',#38237,#38235,#24602,.T.);
#49048=EDGE_CURVE('',#38238,#38236,#24603,.F.);
#49049=EDGE_CURVE('',#38239,#38240,#28951,.T.);
#49050=EDGE_CURVE('',#38239,#38237,#24604,.T.);
#49051=EDGE_CURVE('',#38240,#38238,#24605,.F.);
#49052=EDGE_CURVE('',#38241,#38242,#28952,.T.);
#49053=EDGE_CURVE('',#38241,#38239,#24606,.T.);
#49054=EDGE_CURVE('',#38242,#38240,#24607,.F.);
#49055=EDGE_CURVE('',#38243,#38244,#28953,.T.);
#49056=EDGE_CURVE('',#38243,#38241,#24608,.T.);
#49057=EDGE_CURVE('',#38244,#38242,#24609,.F.);
#49058=EDGE_CURVE('',#38245,#38246,#28954,.T.);
#49059=EDGE_CURVE('',#38245,#38243,#24610,.T.);
#49060=EDGE_CURVE('',#38246,#38244,#24611,.F.);
#49061=EDGE_CURVE('',#38247,#38248,#28955,.T.);
#49062=EDGE_CURVE('',#38247,#38245,#24612,.T.);
#49063=EDGE_CURVE('',#38248,#38246,#24613,.F.);
#49064=EDGE_CURVE('',#38249,#38250,#28956,.T.);
#49065=EDGE_CURVE('',#38249,#38247,#24614,.T.);
#49066=EDGE_CURVE('',#38250,#38248,#24615,.F.);
#49067=EDGE_CURVE('',#38251,#38252,#28957,.T.);
#49068=EDGE_CURVE('',#38251,#38249,#24616,.T.);
#49069=EDGE_CURVE('',#38252,#38250,#24617,.F.);
#49070=EDGE_CURVE('',#38253,#38254,#28958,.T.);
#49071=EDGE_CURVE('',#38253,#38251,#24618,.T.);
#49072=EDGE_CURVE('',#38254,#38252,#24619,.F.);
#49073=EDGE_CURVE('',#38255,#38256,#28959,.T.);
#49074=EDGE_CURVE('',#38255,#38253,#24620,.T.);
#49075=EDGE_CURVE('',#38256,#38254,#24621,.F.);
#49076=EDGE_CURVE('',#38257,#38258,#28960,.T.);
#49077=EDGE_CURVE('',#38257,#38255,#24622,.T.);
#49078=EDGE_CURVE('',#38258,#38256,#24623,.F.);
#49079=EDGE_CURVE('',#38259,#38260,#4177,.F.);
#49080=EDGE_CURVE('',#38259,#38260,#20521,.T.);
#49081=EDGE_CURVE('',#38261,#38261,#20522,.T.);
#49082=EDGE_CURVE('',#38262,#38262,#20523,.T.);
#49083=EDGE_CURVE('',#38263,#38263,#20524,.T.);
#49084=EDGE_CURVE('',#38263,#38264,#28961,.T.);
#49085=EDGE_CURVE('',#38264,#38264,#20525,.T.);
#49086=EDGE_CURVE('',#38192,#38265,#20526,.T.);
#49087=EDGE_CURVE('',#38265,#38266,#24624,.T.);
#49088=EDGE_CURVE('',#38267,#38266,#20527,.T.);
#49089=EDGE_CURVE('',#38267,#38268,#24625,.T.);
#49090=EDGE_CURVE('',#38268,#38269,#28962,.T.);
#49091=EDGE_CURVE('',#38269,#38269,#20528,.T.);
#49092=EDGE_CURVE('',#38268,#38194,#24626,.T.);
#49093=EDGE_CURVE('',#38270,#38258,#24627,.F.);
#49094=EDGE_CURVE('',#38267,#38270,#4178,.T.);
#49095=EDGE_CURVE('',#38266,#38257,#24628,.T.);
#49096=EDGE_CURVE('',#38131,#38197,#24629,.T.);
#49097=EDGE_CURVE('',#38198,#38130,#24630,.T.);
#49098=EDGE_CURVE('',#38271,#38272,#20529,.T.);
#49099=EDGE_CURVE('',#38273,#38271,#20530,.T.);
#49100=EDGE_CURVE('',#38260,#38273,#20531,.T.);
#49101=EDGE_CURVE('',#38274,#38259,#20532,.T.);
#49102=EDGE_CURVE('',#38272,#38274,#20533,.T.);
#49103=EDGE_CURVE('',#38260,#38273,#4179,.T.);
#49104=EDGE_CURVE('',#38273,#38271,#4180,.T.);
#49105=EDGE_CURVE('',#38271,#38272,#4181,.T.);
#49106=EDGE_CURVE('',#38272,#38274,#4182,.T.);
#49107=EDGE_CURVE('',#38274,#38259,#4183,.T.);
#49108=EDGE_CURVE('',#38275,#38276,#28963,.T.);
#49109=EDGE_CURVE('',#38276,#38277,#28964,.T.);
#49110=EDGE_CURVE('',#38277,#38278,#28965,.T.);
#49111=EDGE_CURVE('',#38278,#38279,#28966,.T.);
#49112=EDGE_CURVE('',#38279,#38280,#28967,.T.);
#49113=EDGE_CURVE('',#38280,#38275,#28968,.T.);
#49114=EDGE_CURVE('',#38276,#38259,#28969,.T.);
#49115=EDGE_CURVE('',#38277,#38260,#28970,.T.);
#49116=EDGE_CURVE('',#38278,#38273,#28971,.T.);
#49117=EDGE_CURVE('',#38279,#38271,#28972,.T.);
#49118=EDGE_CURVE('',#38280,#38272,#28973,.T.);
#49119=EDGE_CURVE('',#38275,#38274,#28974,.T.);
#49120=EDGE_CURVE('',#38265,#38193,#4184,.T.);
#68770=ORIENTED_EDGE('',*,*,#48887,.F.);
#68771=ORIENTED_EDGE('',*,*,#48888,.T.);
#68772=ORIENTED_EDGE('',*,*,#48889,.T.);
#68773=ORIENTED_EDGE('',*,*,#48890,.F.);
#68774=ORIENTED_EDGE('',*,*,#48891,.F.);
#68775=ORIENTED_EDGE('',*,*,#48892,.T.);
#68776=ORIENTED_EDGE('',*,*,#48887,.T.);
#68777=ORIENTED_EDGE('',*,*,#48893,.F.);
#68778=ORIENTED_EDGE('',*,*,#48894,.F.);
#68779=ORIENTED_EDGE('',*,*,#48895,.T.);
#68780=ORIENTED_EDGE('',*,*,#48891,.T.);
#68781=ORIENTED_EDGE('',*,*,#48896,.F.);
#68782=ORIENTED_EDGE('',*,*,#48897,.F.);
#68783=ORIENTED_EDGE('',*,*,#48898,.T.);
#68784=ORIENTED_EDGE('',*,*,#48894,.T.);
#68785=ORIENTED_EDGE('',*,*,#48899,.F.);
#68786=ORIENTED_EDGE('',*,*,#48900,.F.);
#68787=ORIENTED_EDGE('',*,*,#48901,.T.);
#68788=ORIENTED_EDGE('',*,*,#48897,.T.);
#68789=ORIENTED_EDGE('',*,*,#48902,.F.);
#68790=ORIENTED_EDGE('',*,*,#48903,.F.);
#68791=ORIENTED_EDGE('',*,*,#48904,.T.);
#68792=ORIENTED_EDGE('',*,*,#48900,.T.);
#68793=ORIENTED_EDGE('',*,*,#48905,.F.);
#68794=ORIENTED_EDGE('',*,*,#48906,.F.);
#68795=ORIENTED_EDGE('',*,*,#48907,.T.);
#68796=ORIENTED_EDGE('',*,*,#48903,.T.);
#68797=ORIENTED_EDGE('',*,*,#48908,.F.);
#68798=ORIENTED_EDGE('',*,*,#48909,.F.);
#68799=ORIENTED_EDGE('',*,*,#48910,.T.);
#68800=ORIENTED_EDGE('',*,*,#48906,.T.);
#68801=ORIENTED_EDGE('',*,*,#48911,.F.);
#68802=ORIENTED_EDGE('',*,*,#48912,.F.);
#68803=ORIENTED_EDGE('',*,*,#48913,.T.);
#68804=ORIENTED_EDGE('',*,*,#48909,.T.);
#68805=ORIENTED_EDGE('',*,*,#48914,.F.);
#68806=ORIENTED_EDGE('',*,*,#48915,.F.);
#68807=ORIENTED_EDGE('',*,*,#48916,.T.);
#68808=ORIENTED_EDGE('',*,*,#48912,.T.);
#68809=ORIENTED_EDGE('',*,*,#48917,.F.);
#68810=ORIENTED_EDGE('',*,*,#48918,.F.);
#68811=ORIENTED_EDGE('',*,*,#48919,.T.);
#68812=ORIENTED_EDGE('',*,*,#48915,.T.);
#68813=ORIENTED_EDGE('',*,*,#48920,.F.);
#68814=ORIENTED_EDGE('',*,*,#48921,.F.);
#68815=ORIENTED_EDGE('',*,*,#48922,.T.);
#68816=ORIENTED_EDGE('',*,*,#48918,.T.);
#68817=ORIENTED_EDGE('',*,*,#48923,.F.);
#68818=ORIENTED_EDGE('',*,*,#48924,.F.);
#68819=ORIENTED_EDGE('',*,*,#48925,.T.);
#68820=ORIENTED_EDGE('',*,*,#48921,.T.);
#68821=ORIENTED_EDGE('',*,*,#48926,.F.);
#68822=ORIENTED_EDGE('',*,*,#48927,.F.);
#68823=ORIENTED_EDGE('',*,*,#48928,.T.);
#68824=ORIENTED_EDGE('',*,*,#48924,.T.);
#68825=ORIENTED_EDGE('',*,*,#48929,.F.);
#68826=ORIENTED_EDGE('',*,*,#48930,.F.);
#68827=ORIENTED_EDGE('',*,*,#48931,.T.);
#68828=ORIENTED_EDGE('',*,*,#48927,.T.);
#68829=ORIENTED_EDGE('',*,*,#48932,.F.);
#68830=ORIENTED_EDGE('',*,*,#48933,.F.);
#68831=ORIENTED_EDGE('',*,*,#48934,.T.);
#68832=ORIENTED_EDGE('',*,*,#48930,.T.);
#68833=ORIENTED_EDGE('',*,*,#48935,.F.);
#68834=ORIENTED_EDGE('',*,*,#48936,.F.);
#68835=ORIENTED_EDGE('',*,*,#48937,.T.);
#68836=ORIENTED_EDGE('',*,*,#48933,.T.);
#68837=ORIENTED_EDGE('',*,*,#48938,.F.);
#68838=ORIENTED_EDGE('',*,*,#48939,.F.);
#68839=ORIENTED_EDGE('',*,*,#48940,.T.);
#68840=ORIENTED_EDGE('',*,*,#48936,.T.);
#68841=ORIENTED_EDGE('',*,*,#48941,.F.);
#68842=ORIENTED_EDGE('',*,*,#48942,.F.);
#68843=ORIENTED_EDGE('',*,*,#48943,.T.);
#68844=ORIENTED_EDGE('',*,*,#48939,.T.);
#68845=ORIENTED_EDGE('',*,*,#48944,.F.);
#68846=ORIENTED_EDGE('',*,*,#48945,.F.);
#68847=ORIENTED_EDGE('',*,*,#48946,.T.);
#68848=ORIENTED_EDGE('',*,*,#48942,.T.);
#68849=ORIENTED_EDGE('',*,*,#48947,.F.);
#68850=ORIENTED_EDGE('',*,*,#48948,.F.);
#68851=ORIENTED_EDGE('',*,*,#48949,.T.);
#68852=ORIENTED_EDGE('',*,*,#48945,.T.);
#68853=ORIENTED_EDGE('',*,*,#48950,.F.);
#68854=ORIENTED_EDGE('',*,*,#48951,.F.);
#68855=ORIENTED_EDGE('',*,*,#48952,.T.);
#68856=ORIENTED_EDGE('',*,*,#48948,.T.);
#68857=ORIENTED_EDGE('',*,*,#48953,.F.);
#68858=ORIENTED_EDGE('',*,*,#48954,.F.);
#68859=ORIENTED_EDGE('',*,*,#48955,.T.);
#68860=ORIENTED_EDGE('',*,*,#48951,.T.);
#68861=ORIENTED_EDGE('',*,*,#48956,.F.);
#68862=ORIENTED_EDGE('',*,*,#48957,.F.);
#68863=ORIENTED_EDGE('',*,*,#48958,.T.);
#68864=ORIENTED_EDGE('',*,*,#48954,.T.);
#68865=ORIENTED_EDGE('',*,*,#48959,.F.);
#68866=ORIENTED_EDGE('',*,*,#48960,.F.);
#68867=ORIENTED_EDGE('',*,*,#48961,.T.);
#68868=ORIENTED_EDGE('',*,*,#48957,.T.);
#68869=ORIENTED_EDGE('',*,*,#48962,.F.);
#68870=ORIENTED_EDGE('',*,*,#48963,.F.);
#68871=ORIENTED_EDGE('',*,*,#48964,.T.);
#68872=ORIENTED_EDGE('',*,*,#48960,.T.);
#68873=ORIENTED_EDGE('',*,*,#48965,.F.);
#68874=ORIENTED_EDGE('',*,*,#48966,.F.);
#68875=ORIENTED_EDGE('',*,*,#48967,.T.);
#68876=ORIENTED_EDGE('',*,*,#48963,.T.);
#68877=ORIENTED_EDGE('',*,*,#48968,.F.);
#68878=ORIENTED_EDGE('',*,*,#48969,.F.);
#68879=ORIENTED_EDGE('',*,*,#48970,.T.);
#68880=ORIENTED_EDGE('',*,*,#48966,.T.);
#68881=ORIENTED_EDGE('',*,*,#48971,.F.);
#68882=ORIENTED_EDGE('',*,*,#48972,.F.);
#68883=ORIENTED_EDGE('',*,*,#48973,.T.);
#68884=ORIENTED_EDGE('',*,*,#48969,.T.);
#68885=ORIENTED_EDGE('',*,*,#48974,.F.);
#68886=ORIENTED_EDGE('',*,*,#48975,.F.);
#68887=ORIENTED_EDGE('',*,*,#48976,.T.);
#68888=ORIENTED_EDGE('',*,*,#48972,.T.);
#68889=ORIENTED_EDGE('',*,*,#48977,.F.);
#68890=ORIENTED_EDGE('',*,*,#48978,.F.);
#68891=ORIENTED_EDGE('',*,*,#48979,.T.);
#68892=ORIENTED_EDGE('',*,*,#48975,.T.);
#68893=ORIENTED_EDGE('',*,*,#48980,.F.);
#68894=ORIENTED_EDGE('',*,*,#48981,.F.);
#68895=ORIENTED_EDGE('',*,*,#48982,.F.);
#68896=ORIENTED_EDGE('',*,*,#48983,.T.);
#68897=ORIENTED_EDGE('',*,*,#48978,.T.);
#68898=ORIENTED_EDGE('',*,*,#48984,.F.);
#68899=ORIENTED_EDGE('',*,*,#48985,.F.);
#68900=ORIENTED_EDGE('',*,*,#48986,.T.);
#68901=ORIENTED_EDGE('',*,*,#48987,.T.);
#68902=ORIENTED_EDGE('',*,*,#48988,.F.);
#68903=ORIENTED_EDGE('',*,*,#48989,.F.);
#68904=ORIENTED_EDGE('',*,*,#48990,.T.);
#68905=ORIENTED_EDGE('',*,*,#48985,.T.);
#68906=ORIENTED_EDGE('',*,*,#48991,.F.);
#68907=ORIENTED_EDGE('',*,*,#48992,.F.);
#68908=ORIENTED_EDGE('',*,*,#48993,.T.);
#68909=ORIENTED_EDGE('',*,*,#48989,.T.);
#68910=ORIENTED_EDGE('',*,*,#48994,.F.);
#68911=ORIENTED_EDGE('',*,*,#48995,.F.);
#68912=ORIENTED_EDGE('',*,*,#48996,.T.);
#68913=ORIENTED_EDGE('',*,*,#48992,.T.);
#68914=ORIENTED_EDGE('',*,*,#48997,.F.);
#68915=ORIENTED_EDGE('',*,*,#48998,.F.);
#68916=ORIENTED_EDGE('',*,*,#48999,.T.);
#68917=ORIENTED_EDGE('',*,*,#48995,.T.);
#68918=ORIENTED_EDGE('',*,*,#49000,.F.);
#68919=ORIENTED_EDGE('',*,*,#49001,.F.);
#68920=ORIENTED_EDGE('',*,*,#49002,.T.);
#68921=ORIENTED_EDGE('',*,*,#48998,.T.);
#68922=ORIENTED_EDGE('',*,*,#49003,.F.);
#68923=ORIENTED_EDGE('',*,*,#49004,.F.);
#68924=ORIENTED_EDGE('',*,*,#49005,.T.);
#68925=ORIENTED_EDGE('',*,*,#49001,.T.);
#68926=ORIENTED_EDGE('',*,*,#49006,.F.);
#68927=ORIENTED_EDGE('',*,*,#49007,.F.);
#68928=ORIENTED_EDGE('',*,*,#49008,.T.);
#68929=ORIENTED_EDGE('',*,*,#49004,.T.);
#68930=ORIENTED_EDGE('',*,*,#49009,.F.);
#68931=ORIENTED_EDGE('',*,*,#49010,.F.);
#68932=ORIENTED_EDGE('',*,*,#49011,.T.);
#68933=ORIENTED_EDGE('',*,*,#49007,.T.);
#68934=ORIENTED_EDGE('',*,*,#49012,.F.);
#68935=ORIENTED_EDGE('',*,*,#49013,.F.);
#68936=ORIENTED_EDGE('',*,*,#49014,.T.);
#68937=ORIENTED_EDGE('',*,*,#49010,.T.);
#68938=ORIENTED_EDGE('',*,*,#49015,.F.);
#68939=ORIENTED_EDGE('',*,*,#49016,.F.);
#68940=ORIENTED_EDGE('',*,*,#49017,.T.);
#68941=ORIENTED_EDGE('',*,*,#49013,.T.);
#68942=ORIENTED_EDGE('',*,*,#49018,.F.);
#68943=ORIENTED_EDGE('',*,*,#49019,.F.);
#68944=ORIENTED_EDGE('',*,*,#49020,.T.);
#68945=ORIENTED_EDGE('',*,*,#49016,.T.);
#68946=ORIENTED_EDGE('',*,*,#49021,.F.);
#68947=ORIENTED_EDGE('',*,*,#49022,.F.);
#68948=ORIENTED_EDGE('',*,*,#49023,.T.);
#68949=ORIENTED_EDGE('',*,*,#49019,.T.);
#68950=ORIENTED_EDGE('',*,*,#49024,.F.);
#68951=ORIENTED_EDGE('',*,*,#49025,.F.);
#68952=ORIENTED_EDGE('',*,*,#49026,.T.);
#68953=ORIENTED_EDGE('',*,*,#49022,.T.);
#68954=ORIENTED_EDGE('',*,*,#49027,.F.);
#68955=ORIENTED_EDGE('',*,*,#49028,.F.);
#68956=ORIENTED_EDGE('',*,*,#49029,.T.);
#68957=ORIENTED_EDGE('',*,*,#49025,.T.);
#68958=ORIENTED_EDGE('',*,*,#49030,.F.);
#68959=ORIENTED_EDGE('',*,*,#49031,.F.);
#68960=ORIENTED_EDGE('',*,*,#49032,.T.);
#68961=ORIENTED_EDGE('',*,*,#49028,.T.);
#68962=ORIENTED_EDGE('',*,*,#49033,.F.);
#68963=ORIENTED_EDGE('',*,*,#49034,.F.);
#68964=ORIENTED_EDGE('',*,*,#49035,.T.);
#68965=ORIENTED_EDGE('',*,*,#49031,.T.);
#68966=ORIENTED_EDGE('',*,*,#49036,.F.);
#68967=ORIENTED_EDGE('',*,*,#49037,.F.);
#68968=ORIENTED_EDGE('',*,*,#49038,.T.);
#68969=ORIENTED_EDGE('',*,*,#49034,.T.);
#68970=ORIENTED_EDGE('',*,*,#49039,.F.);
#68971=ORIENTED_EDGE('',*,*,#49040,.F.);
#68972=ORIENTED_EDGE('',*,*,#49041,.T.);
#68973=ORIENTED_EDGE('',*,*,#49037,.T.);
#68974=ORIENTED_EDGE('',*,*,#49042,.F.);
#68975=ORIENTED_EDGE('',*,*,#49043,.F.);
#68976=ORIENTED_EDGE('',*,*,#49044,.T.);
#68977=ORIENTED_EDGE('',*,*,#49040,.T.);
#68978=ORIENTED_EDGE('',*,*,#49045,.F.);
#68979=ORIENTED_EDGE('',*,*,#49046,.F.);
#68980=ORIENTED_EDGE('',*,*,#49047,.T.);
#68981=ORIENTED_EDGE('',*,*,#49043,.T.);
#68982=ORIENTED_EDGE('',*,*,#49048,.F.);
#68983=ORIENTED_EDGE('',*,*,#49049,.F.);
#68984=ORIENTED_EDGE('',*,*,#49050,.T.);
#68985=ORIENTED_EDGE('',*,*,#49046,.T.);
#68986=ORIENTED_EDGE('',*,*,#49051,.F.);
#68987=ORIENTED_EDGE('',*,*,#49052,.F.);
#68988=ORIENTED_EDGE('',*,*,#49053,.T.);
#68989=ORIENTED_EDGE('',*,*,#49049,.T.);
#68990=ORIENTED_EDGE('',*,*,#49054,.F.);
#68991=ORIENTED_EDGE('',*,*,#49055,.F.);
#68992=ORIENTED_EDGE('',*,*,#49056,.T.);
#68993=ORIENTED_EDGE('',*,*,#49052,.T.);
#68994=ORIENTED_EDGE('',*,*,#49057,.F.);
#68995=ORIENTED_EDGE('',*,*,#49058,.F.);
#68996=ORIENTED_EDGE('',*,*,#49059,.T.);
#68997=ORIENTED_EDGE('',*,*,#49055,.T.);
#68998=ORIENTED_EDGE('',*,*,#49060,.F.);
#68999=ORIENTED_EDGE('',*,*,#49061,.F.);
#69000=ORIENTED_EDGE('',*,*,#49062,.T.);
#69001=ORIENTED_EDGE('',*,*,#49058,.T.);
#69002=ORIENTED_EDGE('',*,*,#49063,.F.);
#69003=ORIENTED_EDGE('',*,*,#49064,.F.);
#69004=ORIENTED_EDGE('',*,*,#49065,.T.);
#69005=ORIENTED_EDGE('',*,*,#49061,.T.);
#69006=ORIENTED_EDGE('',*,*,#49066,.F.);
#69007=ORIENTED_EDGE('',*,*,#49067,.F.);
#69008=ORIENTED_EDGE('',*,*,#49068,.T.);
#69009=ORIENTED_EDGE('',*,*,#49064,.T.);
#69010=ORIENTED_EDGE('',*,*,#49069,.F.);
#69011=ORIENTED_EDGE('',*,*,#49070,.F.);
#69012=ORIENTED_EDGE('',*,*,#49071,.T.);
#69013=ORIENTED_EDGE('',*,*,#49067,.T.);
#69014=ORIENTED_EDGE('',*,*,#49072,.F.);
#69015=ORIENTED_EDGE('',*,*,#49073,.F.);
#69016=ORIENTED_EDGE('',*,*,#49074,.T.);
#69017=ORIENTED_EDGE('',*,*,#49070,.T.);
#69018=ORIENTED_EDGE('',*,*,#49075,.F.);
#69019=ORIENTED_EDGE('',*,*,#49076,.F.);
#69020=ORIENTED_EDGE('',*,*,#49077,.T.);
#69021=ORIENTED_EDGE('',*,*,#49073,.T.);
#69022=ORIENTED_EDGE('',*,*,#49078,.F.);
#69023=ORIENTED_EDGE('',*,*,#49079,.F.);
#69024=ORIENTED_EDGE('',*,*,#49080,.T.);
#69025=ORIENTED_EDGE('',*,*,#49081,.F.);
#69026=ORIENTED_EDGE('',*,*,#49082,.F.);
#69027=ORIENTED_EDGE('',*,*,#49083,.F.);
#69028=ORIENTED_EDGE('',*,*,#49084,.T.);
#69029=ORIENTED_EDGE('',*,*,#49085,.T.);
#69030=ORIENTED_EDGE('',*,*,#49084,.F.);
#69031=ORIENTED_EDGE('',*,*,#48982,.T.);
#69032=ORIENTED_EDGE('',*,*,#49086,.T.);
#69033=ORIENTED_EDGE('',*,*,#49087,.T.);
#69034=ORIENTED_EDGE('',*,*,#49088,.F.);
#69035=ORIENTED_EDGE('',*,*,#49089,.T.);
#69036=ORIENTED_EDGE('',*,*,#49090,.T.);
#69037=ORIENTED_EDGE('',*,*,#49091,.F.);
#69038=ORIENTED_EDGE('',*,*,#49090,.F.);
#69039=ORIENTED_EDGE('',*,*,#49092,.T.);
#69040=ORIENTED_EDGE('',*,*,#49076,.T.);
#69041=ORIENTED_EDGE('',*,*,#49093,.F.);
#69042=ORIENTED_EDGE('',*,*,#49094,.F.);
#69043=ORIENTED_EDGE('',*,*,#49088,.T.);
#69044=ORIENTED_EDGE('',*,*,#49095,.T.);
#69045=ORIENTED_EDGE('',*,*,#49091,.T.);
#69046=ORIENTED_EDGE('',*,*,#49083,.T.);
#69047=ORIENTED_EDGE('',*,*,#48987,.F.);
#69048=ORIENTED_EDGE('',*,*,#49096,.F.);
#69049=ORIENTED_EDGE('',*,*,#48889,.F.);
#69050=ORIENTED_EDGE('',*,*,#49097,.F.);
#69051=ORIENTED_EDGE('',*,*,#49085,.F.);
#69052=ORIENTED_EDGE('',*,*,#49081,.T.);
#69053=ORIENTED_EDGE('',*,*,#49082,.T.);
#69054=ORIENTED_EDGE('',*,*,#49098,.F.);
#69055=ORIENTED_EDGE('',*,*,#49099,.F.);
#69056=ORIENTED_EDGE('',*,*,#49100,.F.);
#69057=ORIENTED_EDGE('',*,*,#49080,.F.);
#69058=ORIENTED_EDGE('',*,*,#49101,.F.);
#69059=ORIENTED_EDGE('',*,*,#49102,.F.);
#69060=ORIENTED_EDGE('',*,*,#49100,.T.);
#69061=ORIENTED_EDGE('',*,*,#49103,.F.);
#69062=ORIENTED_EDGE('',*,*,#49099,.T.);
#69063=ORIENTED_EDGE('',*,*,#49104,.F.);
#69064=ORIENTED_EDGE('',*,*,#49098,.T.);
#69065=ORIENTED_EDGE('',*,*,#49105,.F.);
#69066=ORIENTED_EDGE('',*,*,#49102,.T.);
#69067=ORIENTED_EDGE('',*,*,#49106,.F.);
#69068=ORIENTED_EDGE('',*,*,#49101,.T.);
#69069=ORIENTED_EDGE('',*,*,#49107,.F.);
#69070=ORIENTED_EDGE('',*,*,#49108,.T.);
#69071=ORIENTED_EDGE('',*,*,#49109,.T.);
#69072=ORIENTED_EDGE('',*,*,#49110,.T.);
#69073=ORIENTED_EDGE('',*,*,#49111,.T.);
#69074=ORIENTED_EDGE('',*,*,#49112,.T.);
#69075=ORIENTED_EDGE('',*,*,#49113,.T.);
#69076=ORIENTED_EDGE('',*,*,#49114,.T.);
#69077=ORIENTED_EDGE('',*,*,#49079,.T.);
#69078=ORIENTED_EDGE('',*,*,#49115,.F.);
#69079=ORIENTED_EDGE('',*,*,#49109,.F.);
#69080=ORIENTED_EDGE('',*,*,#49115,.T.);
#69081=ORIENTED_EDGE('',*,*,#49103,.T.);
#69082=ORIENTED_EDGE('',*,*,#49116,.F.);
#69083=ORIENTED_EDGE('',*,*,#49110,.F.);
#69084=ORIENTED_EDGE('',*,*,#49116,.T.);
#69085=ORIENTED_EDGE('',*,*,#49104,.T.);
#69086=ORIENTED_EDGE('',*,*,#49117,.F.);
#69087=ORIENTED_EDGE('',*,*,#49111,.F.);
#69088=ORIENTED_EDGE('',*,*,#49117,.T.);
#69089=ORIENTED_EDGE('',*,*,#49105,.T.);
#69090=ORIENTED_EDGE('',*,*,#49118,.F.);
#69091=ORIENTED_EDGE('',*,*,#49112,.F.);
#69092=ORIENTED_EDGE('',*,*,#49118,.T.);
#69093=ORIENTED_EDGE('',*,*,#49106,.T.);
#69094=ORIENTED_EDGE('',*,*,#49119,.F.);
#69095=ORIENTED_EDGE('',*,*,#49113,.F.);
#69096=ORIENTED_EDGE('',*,*,#49119,.T.);
#69097=ORIENTED_EDGE('',*,*,#49107,.T.);
#69098=ORIENTED_EDGE('',*,*,#49114,.F.);
#69099=ORIENTED_EDGE('',*,*,#49108,.F.);
#69100=ORIENTED_EDGE('',*,*,#49097,.T.);
#69101=ORIENTED_EDGE('',*,*,#48888,.F.);
#69102=ORIENTED_EDGE('',*,*,#48892,.F.);
#69103=ORIENTED_EDGE('',*,*,#48895,.F.);
#69104=ORIENTED_EDGE('',*,*,#48898,.F.);
#69105=ORIENTED_EDGE('',*,*,#48901,.F.);
#69106=ORIENTED_EDGE('',*,*,#48904,.F.);
#69107=ORIENTED_EDGE('',*,*,#48907,.F.);
#69108=ORIENTED_EDGE('',*,*,#48910,.F.);
#69109=ORIENTED_EDGE('',*,*,#48913,.F.);
#69110=ORIENTED_EDGE('',*,*,#48916,.F.);
#69111=ORIENTED_EDGE('',*,*,#48919,.F.);
#69112=ORIENTED_EDGE('',*,*,#48922,.F.);
#69113=ORIENTED_EDGE('',*,*,#48925,.F.);
#69114=ORIENTED_EDGE('',*,*,#48928,.F.);
#69115=ORIENTED_EDGE('',*,*,#48931,.F.);
#69116=ORIENTED_EDGE('',*,*,#48934,.F.);
#69117=ORIENTED_EDGE('',*,*,#48937,.F.);
#69118=ORIENTED_EDGE('',*,*,#48940,.F.);
#69119=ORIENTED_EDGE('',*,*,#48943,.F.);
#69120=ORIENTED_EDGE('',*,*,#48946,.F.);
#69121=ORIENTED_EDGE('',*,*,#48949,.F.);
#69122=ORIENTED_EDGE('',*,*,#48952,.F.);
#69123=ORIENTED_EDGE('',*,*,#48955,.F.);
#69124=ORIENTED_EDGE('',*,*,#48958,.F.);
#69125=ORIENTED_EDGE('',*,*,#48961,.F.);
#69126=ORIENTED_EDGE('',*,*,#48964,.F.);
#69127=ORIENTED_EDGE('',*,*,#48967,.F.);
#69128=ORIENTED_EDGE('',*,*,#48970,.F.);
#69129=ORIENTED_EDGE('',*,*,#48973,.F.);
#69130=ORIENTED_EDGE('',*,*,#48976,.F.);
#69131=ORIENTED_EDGE('',*,*,#48979,.F.);
#69132=ORIENTED_EDGE('',*,*,#48983,.F.);
#69133=ORIENTED_EDGE('',*,*,#49092,.F.);
#69134=ORIENTED_EDGE('',*,*,#49089,.F.);
#69135=ORIENTED_EDGE('',*,*,#49094,.T.);
#69136=ORIENTED_EDGE('',*,*,#49093,.T.);
#69137=ORIENTED_EDGE('',*,*,#49078,.T.);
#69138=ORIENTED_EDGE('',*,*,#49075,.T.);
#69139=ORIENTED_EDGE('',*,*,#49072,.T.);
#69140=ORIENTED_EDGE('',*,*,#49069,.T.);
#69141=ORIENTED_EDGE('',*,*,#49066,.T.);
#69142=ORIENTED_EDGE('',*,*,#49063,.T.);
#69143=ORIENTED_EDGE('',*,*,#49060,.T.);
#69144=ORIENTED_EDGE('',*,*,#49057,.T.);
#69145=ORIENTED_EDGE('',*,*,#49054,.T.);
#69146=ORIENTED_EDGE('',*,*,#49051,.T.);
#69147=ORIENTED_EDGE('',*,*,#49048,.T.);
#69148=ORIENTED_EDGE('',*,*,#49045,.T.);
#69149=ORIENTED_EDGE('',*,*,#49042,.T.);
#69150=ORIENTED_EDGE('',*,*,#49039,.T.);
#69151=ORIENTED_EDGE('',*,*,#49036,.T.);
#69152=ORIENTED_EDGE('',*,*,#49033,.T.);
#69153=ORIENTED_EDGE('',*,*,#49030,.T.);
#69154=ORIENTED_EDGE('',*,*,#49027,.T.);
#69155=ORIENTED_EDGE('',*,*,#49024,.T.);
#69156=ORIENTED_EDGE('',*,*,#49021,.T.);
#69157=ORIENTED_EDGE('',*,*,#49018,.T.);
#69158=ORIENTED_EDGE('',*,*,#49015,.T.);
#69159=ORIENTED_EDGE('',*,*,#49012,.T.);
#69160=ORIENTED_EDGE('',*,*,#49009,.T.);
#69161=ORIENTED_EDGE('',*,*,#49006,.T.);
#69162=ORIENTED_EDGE('',*,*,#49003,.T.);
#69163=ORIENTED_EDGE('',*,*,#49000,.T.);
#69164=ORIENTED_EDGE('',*,*,#48997,.T.);
#69165=ORIENTED_EDGE('',*,*,#48994,.T.);
#69166=ORIENTED_EDGE('',*,*,#48991,.T.);
#69167=ORIENTED_EDGE('',*,*,#48988,.T.);
#69168=ORIENTED_EDGE('',*,*,#48981,.T.);
#69169=ORIENTED_EDGE('',*,*,#49120,.F.);
#69170=ORIENTED_EDGE('',*,*,#49086,.F.);
#69171=ORIENTED_EDGE('',*,*,#49096,.T.);
#69172=ORIENTED_EDGE('',*,*,#48986,.F.);
#69173=ORIENTED_EDGE('',*,*,#48990,.F.);
#69174=ORIENTED_EDGE('',*,*,#48993,.F.);
#69175=ORIENTED_EDGE('',*,*,#48996,.F.);
#69176=ORIENTED_EDGE('',*,*,#48999,.F.);
#69177=ORIENTED_EDGE('',*,*,#49002,.F.);
#69178=ORIENTED_EDGE('',*,*,#49005,.F.);
#69179=ORIENTED_EDGE('',*,*,#49008,.F.);
#69180=ORIENTED_EDGE('',*,*,#49011,.F.);
#69181=ORIENTED_EDGE('',*,*,#49014,.F.);
#69182=ORIENTED_EDGE('',*,*,#49017,.F.);
#69183=ORIENTED_EDGE('',*,*,#49020,.F.);
#69184=ORIENTED_EDGE('',*,*,#49023,.F.);
#69185=ORIENTED_EDGE('',*,*,#49026,.F.);
#69186=ORIENTED_EDGE('',*,*,#49029,.F.);
#69187=ORIENTED_EDGE('',*,*,#49032,.F.);
#69188=ORIENTED_EDGE('',*,*,#49035,.F.);
#69189=ORIENTED_EDGE('',*,*,#49038,.F.);
#69190=ORIENTED_EDGE('',*,*,#49041,.F.);
#69191=ORIENTED_EDGE('',*,*,#49044,.F.);
#69192=ORIENTED_EDGE('',*,*,#49047,.F.);
#69193=ORIENTED_EDGE('',*,*,#49050,.F.);
#69194=ORIENTED_EDGE('',*,*,#49053,.F.);
#69195=ORIENTED_EDGE('',*,*,#49056,.F.);
#69196=ORIENTED_EDGE('',*,*,#49059,.F.);
#69197=ORIENTED_EDGE('',*,*,#49062,.F.);
#69198=ORIENTED_EDGE('',*,*,#49065,.F.);
#69199=ORIENTED_EDGE('',*,*,#49068,.F.);
#69200=ORIENTED_EDGE('',*,*,#49071,.F.);
#69201=ORIENTED_EDGE('',*,*,#49074,.F.);
#69202=ORIENTED_EDGE('',*,*,#49077,.F.);
#69203=ORIENTED_EDGE('',*,*,#49095,.F.);
#69204=ORIENTED_EDGE('',*,*,#49087,.F.);
#69205=ORIENTED_EDGE('',*,*,#49120,.T.);
#69206=ORIENTED_EDGE('',*,*,#48984,.T.);
#69207=ORIENTED_EDGE('',*,*,#48980,.T.);
#69208=ORIENTED_EDGE('',*,*,#48977,.T.);
#69209=ORIENTED_EDGE('',*,*,#48974,.T.);
#69210=ORIENTED_EDGE('',*,*,#48971,.T.);
#69211=ORIENTED_EDGE('',*,*,#48968,.T.);
#69212=ORIENTED_EDGE('',*,*,#48965,.T.);
#69213=ORIENTED_EDGE('',*,*,#48962,.T.);
#69214=ORIENTED_EDGE('',*,*,#48959,.T.);
#69215=ORIENTED_EDGE('',*,*,#48956,.T.);
#69216=ORIENTED_EDGE('',*,*,#48953,.T.);
#69217=ORIENTED_EDGE('',*,*,#48950,.T.);
#69218=ORIENTED_EDGE('',*,*,#48947,.T.);
#69219=ORIENTED_EDGE('',*,*,#48944,.T.);
#69220=ORIENTED_EDGE('',*,*,#48941,.T.);
#69221=ORIENTED_EDGE('',*,*,#48938,.T.);
#69222=ORIENTED_EDGE('',*,*,#48935,.T.);
#69223=ORIENTED_EDGE('',*,*,#48932,.T.);
#69224=ORIENTED_EDGE('',*,*,#48929,.T.);
#69225=ORIENTED_EDGE('',*,*,#48926,.T.);
#69226=ORIENTED_EDGE('',*,*,#48923,.T.);
#69227=ORIENTED_EDGE('',*,*,#48920,.T.);
#69228=ORIENTED_EDGE('',*,*,#48917,.T.);
#69229=ORIENTED_EDGE('',*,*,#48914,.T.);
#69230=ORIENTED_EDGE('',*,*,#48911,.T.);
#69231=ORIENTED_EDGE('',*,*,#48908,.T.);
#69232=ORIENTED_EDGE('',*,*,#48905,.T.);
#69233=ORIENTED_EDGE('',*,*,#48902,.T.);
#69234=ORIENTED_EDGE('',*,*,#48899,.T.);
#69235=ORIENTED_EDGE('',*,*,#48896,.T.);
#69236=ORIENTED_EDGE('',*,*,#48893,.T.);
#69237=ORIENTED_EDGE('',*,*,#48890,.T.);
#87855=CYLINDRICAL_SURFACE('',#99053,1.17524047358084);
#87856=CYLINDRICAL_SURFACE('',#99055,1.17524047358084);
#87857=CYLINDRICAL_SURFACE('',#99056,1.17524047358084);
#87858=CYLINDRICAL_SURFACE('',#99057,1.17524047358084);
#87859=CYLINDRICAL_SURFACE('',#99058,1.17524047358084);
#87860=CYLINDRICAL_SURFACE('',#99059,1.17524047358084);
#87861=CYLINDRICAL_SURFACE('',#99060,1.17524047358084);
#87862=CYLINDRICAL_SURFACE('',#99061,1.17524047358084);
#87863=CYLINDRICAL_SURFACE('',#99062,1.17524047358084);
#87864=CYLINDRICAL_SURFACE('',#99063,1.17524047358084);
#87865=CYLINDRICAL_SURFACE('',#99064,1.17524047358084);
#87866=CYLINDRICAL_SURFACE('',#99065,1.17524047358084);
#87867=CYLINDRICAL_SURFACE('',#99066,1.17524047358084);
#87868=CYLINDRICAL_SURFACE('',#99067,1.17524047358084);
#87869=CYLINDRICAL_SURFACE('',#99068,1.17524047358084);
#87870=CYLINDRICAL_SURFACE('',#99069,1.17524047358084);
#87871=CYLINDRICAL_SURFACE('',#99070,1.17524047358084);
#87872=CYLINDRICAL_SURFACE('',#99071,1.17524047358084);
#87873=CYLINDRICAL_SURFACE('',#99072,1.17524047358084);
#87874=CYLINDRICAL_SURFACE('',#99073,1.17524047358084);
#87875=CYLINDRICAL_SURFACE('',#99074,1.17524047358084);
#87876=CYLINDRICAL_SURFACE('',#99075,1.17524047358084);
#87877=CYLINDRICAL_SURFACE('',#99076,1.17524047358084);
#87878=CYLINDRICAL_SURFACE('',#99077,1.17524047358084);
#87879=CYLINDRICAL_SURFACE('',#99078,1.17524047358084);
#87880=CYLINDRICAL_SURFACE('',#99079,1.17524047358084);
#87881=CYLINDRICAL_SURFACE('',#99080,1.17524047358084);
#87882=CYLINDRICAL_SURFACE('',#99081,1.17524047358084);
#87883=CYLINDRICAL_SURFACE('',#99082,1.17524047358084);
#87884=CYLINDRICAL_SURFACE('',#99083,1.17524047358084);
#87885=CYLINDRICAL_SURFACE('',#99084,1.17524047358084);
#87886=CYLINDRICAL_SURFACE('',#99085,1.17524047358084);
#87887=CYLINDRICAL_SURFACE('',#99087,1.5);
#87888=CYLINDRICAL_SURFACE('',#99089,1.5);
#87889=CYLINDRICAL_SURFACE('',#99090,1.5);
#87890=CYLINDRICAL_SURFACE('',#99091,1.5);
#87891=CYLINDRICAL_SURFACE('',#99092,1.5);
#87892=CYLINDRICAL_SURFACE('',#99093,1.5);
#87893=CYLINDRICAL_SURFACE('',#99094,1.5);
#87894=CYLINDRICAL_SURFACE('',#99095,1.5);
#87895=CYLINDRICAL_SURFACE('',#99096,1.5);
#87896=CYLINDRICAL_SURFACE('',#99097,1.5);
#87897=CYLINDRICAL_SURFACE('',#99098,1.5);
#87898=CYLINDRICAL_SURFACE('',#99099,1.5);
#87899=CYLINDRICAL_SURFACE('',#99100,1.5);
#87900=CYLINDRICAL_SURFACE('',#99101,1.5);
#87901=CYLINDRICAL_SURFACE('',#99102,1.5);
#87902=CYLINDRICAL_SURFACE('',#99103,1.5);
#87903=CYLINDRICAL_SURFACE('',#99104,1.5);
#87904=CYLINDRICAL_SURFACE('',#99105,1.5);
#87905=CYLINDRICAL_SURFACE('',#99106,1.5);
#87906=CYLINDRICAL_SURFACE('',#99107,1.5);
#87907=CYLINDRICAL_SURFACE('',#99108,1.5);
#87908=CYLINDRICAL_SURFACE('',#99109,1.5);
#87909=CYLINDRICAL_SURFACE('',#99110,1.5);
#87910=CYLINDRICAL_SURFACE('',#99111,1.5);
#87911=CYLINDRICAL_SURFACE('',#99112,1.5);
#87912=CYLINDRICAL_SURFACE('',#99113,1.5);
#87913=CYLINDRICAL_SURFACE('',#99114,1.5);
#87914=CYLINDRICAL_SURFACE('',#99115,1.5);
#87915=CYLINDRICAL_SURFACE('',#99116,1.5);
#87916=CYLINDRICAL_SURFACE('',#99117,1.5);
#87917=CYLINDRICAL_SURFACE('',#99118,1.5);
#87918=CYLINDRICAL_SURFACE('',#99124,3.5);
#87919=CYLINDRICAL_SURFACE('',#99131,1.5);
#87920=CYLINDRICAL_SURFACE('',#99153,1.17524047358084);
#90777=ADVANCED_FACE('',(#8313),#87855,.T.);
#90778=ADVANCED_FACE('',(#8314),#87856,.T.);
#90779=ADVANCED_FACE('',(#8315),#87857,.T.);
#90780=ADVANCED_FACE('',(#8316),#87858,.T.);
#90781=ADVANCED_FACE('',(#8317),#87859,.T.);
#90782=ADVANCED_FACE('',(#8318),#87860,.T.);
#90783=ADVANCED_FACE('',(#8319),#87861,.T.);
#90784=ADVANCED_FACE('',(#8320),#87862,.T.);
#90785=ADVANCED_FACE('',(#8321),#87863,.T.);
#90786=ADVANCED_FACE('',(#8322),#87864,.T.);
#90787=ADVANCED_FACE('',(#8323),#87865,.T.);
#90788=ADVANCED_FACE('',(#8324),#87866,.T.);
#90789=ADVANCED_FACE('',(#8325),#87867,.T.);
#90790=ADVANCED_FACE('',(#8326),#87868,.T.);
#90791=ADVANCED_FACE('',(#8327),#87869,.T.);
#90792=ADVANCED_FACE('',(#8328),#87870,.T.);
#90793=ADVANCED_FACE('',(#8329),#87871,.T.);
#90794=ADVANCED_FACE('',(#8330),#87872,.T.);
#90795=ADVANCED_FACE('',(#8331),#87873,.T.);
#90796=ADVANCED_FACE('',(#8332),#87874,.T.);
#90797=ADVANCED_FACE('',(#8333),#87875,.T.);
#90798=ADVANCED_FACE('',(#8334),#87876,.T.);
#90799=ADVANCED_FACE('',(#8335),#87877,.T.);
#90800=ADVANCED_FACE('',(#8336),#87878,.T.);
#90801=ADVANCED_FACE('',(#8337),#87879,.T.);
#90802=ADVANCED_FACE('',(#8338),#87880,.T.);
#90803=ADVANCED_FACE('',(#8339),#87881,.T.);
#90804=ADVANCED_FACE('',(#8340),#87882,.T.);
#90805=ADVANCED_FACE('',(#8341),#87883,.T.);
#90806=ADVANCED_FACE('',(#8342),#87884,.T.);
#90807=ADVANCED_FACE('',(#8343),#87885,.T.);
#90808=ADVANCED_FACE('',(#8344),#87886,.T.);
#90809=ADVANCED_FACE('',(#8345),#87887,.T.);
#90810=ADVANCED_FACE('',(#8346),#87888,.T.);
#90811=ADVANCED_FACE('',(#8347),#87889,.T.);
#90812=ADVANCED_FACE('',(#8348),#87890,.T.);
#90813=ADVANCED_FACE('',(#8349),#87891,.T.);
#90814=ADVANCED_FACE('',(#8350),#87892,.T.);
#90815=ADVANCED_FACE('',(#8351),#87893,.T.);
#90816=ADVANCED_FACE('',(#8352),#87894,.T.);
#90817=ADVANCED_FACE('',(#8353),#87895,.T.);
#90818=ADVANCED_FACE('',(#8354),#87896,.T.);
#90819=ADVANCED_FACE('',(#8355),#87897,.T.);
#90820=ADVANCED_FACE('',(#8356),#87898,.T.);
#90821=ADVANCED_FACE('',(#8357),#87899,.T.);
#90822=ADVANCED_FACE('',(#8358),#87900,.T.);
#90823=ADVANCED_FACE('',(#8359),#87901,.T.);
#90824=ADVANCED_FACE('',(#8360),#87902,.T.);
#90825=ADVANCED_FACE('',(#8361),#87903,.T.);
#90826=ADVANCED_FACE('',(#8362),#87904,.T.);
#90827=ADVANCED_FACE('',(#8363),#87905,.T.);
#90828=ADVANCED_FACE('',(#8364),#87906,.T.);
#90829=ADVANCED_FACE('',(#8365),#87907,.T.);
#90830=ADVANCED_FACE('',(#8366),#87908,.T.);
#90831=ADVANCED_FACE('',(#8367),#87909,.T.);
#90832=ADVANCED_FACE('',(#8368),#87910,.T.);
#90833=ADVANCED_FACE('',(#8369),#87911,.T.);
#90834=ADVANCED_FACE('',(#8370),#87912,.T.);
#90835=ADVANCED_FACE('',(#8371),#87913,.T.);
#90836=ADVANCED_FACE('',(#8372),#87914,.T.);
#90837=ADVANCED_FACE('',(#8373),#87915,.T.);
#90838=ADVANCED_FACE('',(#8374),#87916,.T.);
#90839=ADVANCED_FACE('',(#8375),#87917,.T.);
#90840=ADVANCED_FACE('',(#8376),#4877,.F.);
#90841=ADVANCED_FACE('',(#8377,#5209),#142,.T.);
#90842=ADVANCED_FACE('',(#8378),#87918,.T.);
#90843=ADVANCED_FACE('',(#8379),#4878,.T.);
#90844=ADVANCED_FACE('',(#8380),#87919,.T.);
#90845=ADVANCED_FACE('',(#8381),#5684,.T.);
#90846=ADVANCED_FACE('',(#8382,#5210),#5685,.F.);
#90847=ADVANCED_FACE('',(#8383,#5211),#5686,.F.);
#90848=ADVANCED_FACE('',(#8384,#5212),#5687,.F.);
#90849=ADVANCED_FACE('',(#8385),#4879,.F.);
#90850=ADVANCED_FACE('',(#8386),#4880,.F.);
#90851=ADVANCED_FACE('',(#8387),#4881,.F.);
#90852=ADVANCED_FACE('',(#8388),#4882,.F.);
#90853=ADVANCED_FACE('',(#8389),#4883,.F.);
#90854=ADVANCED_FACE('',(#8390),#5688,.T.);
#90855=ADVANCED_FACE('',(#8391),#5689,.F.);
#90856=ADVANCED_FACE('',(#8392),#5690,.F.);
#90857=ADVANCED_FACE('',(#8393),#5691,.F.);
#90858=ADVANCED_FACE('',(#8394),#5692,.F.);
#90859=ADVANCED_FACE('',(#8395),#5693,.F.);
#90860=ADVANCED_FACE('',(#8396),#5694,.F.);
#90861=ADVANCED_FACE('',(#8397),#2307,.T.);
#90862=ADVANCED_FACE('',(#8398),#87920,.T.);
#90863=ADVANCED_FACE('',(#8399),#2308,.T.);
#94645=CLOSED_SHELL('',(#90777,#90778,#90779,#90780,#90781,#90782,#90783,
#90784,#90785,#90786,#90787,#90788,#90789,#90790,#90791,#90792,#90793,#90794,
#90795,#90796,#90797,#90798,#90799,#90800,#90801,#90802,#90803,#90804,#90805,
#90806,#90807,#90808,#90809,#90810,#90811,#90812,#90813,#90814,#90815,#90816,
#90817,#90818,#90819,#90820,#90821,#90822,#90823,#90824,#90825,#90826,#90827,
#90828,#90829,#90830,#90831,#90832,#90833,#90834,#90835,#90836,#90837,#90838,
#90839,#90840,#90841,#90842,#90843,#90844,#90845,#90846,#90847,#90848,#90849,
#90850,#90851,#90852,#90853,#90854,#90855,#90856,#90857,#90858,#90859,#90860,
#90861,#90862,#90863));
#99052=AXIS2_PLACEMENT_3D('',#358526,#115722,#115723);
#99053=AXIS2_PLACEMENT_3D('',#358527,#115724,#115725);
#99054=AXIS2_PLACEMENT_3D('',#358546,#115727,#115728);
#99055=AXIS2_PLACEMENT_3D('',#358560,#115729,#115730);
#99056=AXIS2_PLACEMENT_3D('',#358590,#115732,#115733);
#99057=AXIS2_PLACEMENT_3D('',#358620,#115735,#115736);
#99058=AXIS2_PLACEMENT_3D('',#358650,#115738,#115739);
#99059=AXIS2_PLACEMENT_3D('',#358680,#115741,#115742);
#99060=AXIS2_PLACEMENT_3D('',#358710,#115744,#115745);
#99061=AXIS2_PLACEMENT_3D('',#358740,#115747,#115748);
#99062=AXIS2_PLACEMENT_3D('',#358770,#115750,#115751);
#99063=AXIS2_PLACEMENT_3D('',#358800,#115753,#115754);
#99064=AXIS2_PLACEMENT_3D('',#358830,#115756,#115757);
#99065=AXIS2_PLACEMENT_3D('',#358860,#115759,#115760);
#99066=AXIS2_PLACEMENT_3D('',#358890,#115762,#115763);
#99067=AXIS2_PLACEMENT_3D('',#358920,#115765,#115766);
#99068=AXIS2_PLACEMENT_3D('',#358950,#115768,#115769);
#99069=AXIS2_PLACEMENT_3D('',#358980,#115771,#115772);
#99070=AXIS2_PLACEMENT_3D('',#359010,#115774,#115775);
#99071=AXIS2_PLACEMENT_3D('',#359040,#115777,#115778);
#99072=AXIS2_PLACEMENT_3D('',#359070,#115780,#115781);
#99073=AXIS2_PLACEMENT_3D('',#359100,#115783,#115784);
#99074=AXIS2_PLACEMENT_3D('',#359130,#115786,#115787);
#99075=AXIS2_PLACEMENT_3D('',#359160,#115789,#115790);
#99076=AXIS2_PLACEMENT_3D('',#359190,#115792,#115793);
#99077=AXIS2_PLACEMENT_3D('',#359220,#115795,#115796);
#99078=AXIS2_PLACEMENT_3D('',#359250,#115798,#115799);
#99079=AXIS2_PLACEMENT_3D('',#359280,#115801,#115802);
#99080=AXIS2_PLACEMENT_3D('',#359310,#115804,#115805);
#99081=AXIS2_PLACEMENT_3D('',#359340,#115807,#115808);
#99082=AXIS2_PLACEMENT_3D('',#359370,#115810,#115811);
#99083=AXIS2_PLACEMENT_3D('',#359400,#115813,#115814);
#99084=AXIS2_PLACEMENT_3D('',#359430,#115816,#115817);
#99085=AXIS2_PLACEMENT_3D('',#359460,#115819,#115820);
#99086=AXIS2_PLACEMENT_3D('',#359465,#115822,#115823);
#99087=AXIS2_PLACEMENT_3D('',#359492,#115824,#115825);
#99088=AXIS2_PLACEMENT_3D('',#359505,#115827,#115828);
#99089=AXIS2_PLACEMENT_3D('',#359522,#115829,#115830);
#99090=AXIS2_PLACEMENT_3D('',#359598,#115832,#115833);
#99091=AXIS2_PLACEMENT_3D('',#359674,#115835,#115836);
#99092=AXIS2_PLACEMENT_3D('',#359752,#115838,#115839);
#99093=AXIS2_PLACEMENT_3D('',#359830,#115841,#115842);
#99094=AXIS2_PLACEMENT_3D('',#359906,#115844,#115845);
#99095=AXIS2_PLACEMENT_3D('',#359982,#115847,#115848);
#99096=AXIS2_PLACEMENT_3D('',#360058,#115850,#115851);
#99097=AXIS2_PLACEMENT_3D('',#360134,#115853,#115854);
#99098=AXIS2_PLACEMENT_3D('',#360212,#115856,#115857);
#99099=AXIS2_PLACEMENT_3D('',#360290,#115859,#115860);
#99100=AXIS2_PLACEMENT_3D('',#360366,#115862,#115863);
#99101=AXIS2_PLACEMENT_3D('',#360442,#115865,#115866);
#99102=AXIS2_PLACEMENT_3D('',#360518,#115868,#115869);
#99103=AXIS2_PLACEMENT_3D('',#360594,#115871,#115872);
#99104=AXIS2_PLACEMENT_3D('',#360670,#115874,#115875);
#99105=AXIS2_PLACEMENT_3D('',#360748,#115877,#115878);
#99106=AXIS2_PLACEMENT_3D('',#360826,#115880,#115881);
#99107=AXIS2_PLACEMENT_3D('',#360902,#115883,#115884);
#99108=AXIS2_PLACEMENT_3D('',#360978,#115886,#115887);
#99109=AXIS2_PLACEMENT_3D('',#361054,#115889,#115890);
#99110=AXIS2_PLACEMENT_3D('',#361130,#115892,#115893);
#99111=AXIS2_PLACEMENT_3D('',#361206,#115895,#115896);
#99112=AXIS2_PLACEMENT_3D('',#361284,#115898,#115899);
#99113=AXIS2_PLACEMENT_3D('',#361362,#115901,#115902);
#99114=AXIS2_PLACEMENT_3D('',#361438,#115904,#115905);
#99115=AXIS2_PLACEMENT_3D('',#361514,#115907,#115908);
#99116=AXIS2_PLACEMENT_3D('',#361590,#115910,#115911);
#99117=AXIS2_PLACEMENT_3D('',#361666,#115913,#115914);
#99118=AXIS2_PLACEMENT_3D('',#361744,#115916,#115917);
#99119=AXIS2_PLACEMENT_3D('',#361822,#115919,#115920);
#99120=AXIS2_PLACEMENT_3D('',#361828,#115921,#115922);
#99121=AXIS2_PLACEMENT_3D('',#361829,#115923,#115924);
#99122=AXIS2_PLACEMENT_3D('',#361831,#115925,#115926);
#99123=AXIS2_PLACEMENT_3D('',#361833,#115927,#115928);
#99124=AXIS2_PLACEMENT_3D('',#361834,#115929,#115930);
#99125=AXIS2_PLACEMENT_3D('',#361836,#115931,#115932);
#99126=AXIS2_PLACEMENT_3D('',#361839,#115934,#115935);
#99127=AXIS2_PLACEMENT_3D('',#361840,#115936,#115937);
#99128=AXIS2_PLACEMENT_3D('',#361842,#115938,#115939);
#99129=AXIS2_PLACEMENT_3D('',#361857,#115940,#115941);
#99130=AXIS2_PLACEMENT_3D('',#361885,#115943,#115944);
#99131=AXIS2_PLACEMENT_3D('',#361902,#115945,#115946);
#99132=AXIS2_PLACEMENT_3D('',#361959,#115947,#115948);
#99133=AXIS2_PLACEMENT_3D('',#361960,#115949,#115950);
#99134=AXIS2_PLACEMENT_3D('',#361995,#115951,#115952);
#99135=AXIS2_PLACEMENT_3D('',#361996,#115953,#115954);
#99136=AXIS2_PLACEMENT_3D('',#361999,#115955,#115956);
#99137=AXIS2_PLACEMENT_3D('',#362001,#115957,#115958);
#99138=AXIS2_PLACEMENT_3D('',#362002,#115959,#115960);
#99139=AXIS2_PLACEMENT_3D('',#362004,#115961,#115962);
#99140=AXIS2_PLACEMENT_3D('',#362005,#115963,#115964);
#99141=AXIS2_PLACEMENT_3D('',#362006,#115965,#115966);
#99142=AXIS2_PLACEMENT_3D('',#362010,#115967,#115968);
#99143=AXIS2_PLACEMENT_3D('',#362014,#115969,#115970);
#99144=AXIS2_PLACEMENT_3D('',#362018,#115971,#115972);
#99145=AXIS2_PLACEMENT_3D('',#362022,#115973,#115974);
#99146=AXIS2_PLACEMENT_3D('',#362026,#115975,#115976);
#99147=AXIS2_PLACEMENT_3D('',#362039,#115983,#115984);
#99148=AXIS2_PLACEMENT_3D('',#362042,#115987,#115988);
#99149=AXIS2_PLACEMENT_3D('',#362044,#115990,#115991);
#99150=AXIS2_PLACEMENT_3D('',#362046,#115993,#115994);
#99151=AXIS2_PLACEMENT_3D('',#362048,#115996,#115997);
#99152=AXIS2_PLACEMENT_3D('',#362050,#115999,#116000);
#99153=AXIS2_PLACEMENT_3D('',#362845,#116001,#116002);
#115722=DIRECTION('axis',(0.,0.,1.));
#115723=DIRECTION('refdir',(1.,0.,0.));
#115724=DIRECTION('center_axis',(-3.15057456128877E-15,3.72034542862913E-31,
-1.));
#115725=DIRECTION('ref_axis',(1.18084665392185E-16,1.,0.));
#115726=DIRECTION('',(3.15057456128877E-15,-3.72034542862913E-31,1.));
#115727=DIRECTION('center_axis',(0.,0.,-1.));
#115728=DIRECTION('ref_axis',(-0.700629269222024,-0.713525491562434,0.));
#115729=DIRECTION('center_axis',(-3.15057456128877E-15,3.72034542862913E-31,
-1.));
#115730=DIRECTION('ref_axis',(1.18084665392185E-16,1.,0.));
#115731=DIRECTION('',(3.15057456128877E-15,-3.72034542862913E-31,1.));
#115732=DIRECTION('center_axis',(-3.15057456128877E-15,3.72034542862913E-31,
-1.));
#115733=DIRECTION('ref_axis',(1.18084665392185E-16,1.,0.));
#115734=DIRECTION('',(3.15057456128877E-15,-3.72034542862913E-31,1.));
#115735=DIRECTION('center_axis',(-3.15057456128877E-15,3.72034542862913E-31,
-1.));
#115736=DIRECTION('ref_axis',(1.18084665392185E-16,1.,0.));
#115737=DIRECTION('',(3.15057456128877E-15,-3.72034542862913E-31,1.));
#115738=DIRECTION('center_axis',(-3.15057456128877E-15,3.72034542862913E-31,
-1.));
#115739=DIRECTION('ref_axis',(1.18084665392185E-16,1.,0.));
#115740=DIRECTION('',(3.15057456128877E-15,-3.72034542862913E-31,1.));
#115741=DIRECTION('center_axis',(-3.15057456128877E-15,3.72034542862913E-31,
-1.));
#115742=DIRECTION('ref_axis',(1.18084665392185E-16,1.,0.));
#115743=DIRECTION('',(3.15057456128877E-15,-3.72034542862913E-31,1.));
#115744=DIRECTION('center_axis',(-3.15057456128877E-15,3.72034542862913E-31,
-1.));
#115745=DIRECTION('ref_axis',(1.18084665392185E-16,1.,0.));
#115746=DIRECTION('',(3.15057456128877E-15,-3.72034542862913E-31,1.));
#115747=DIRECTION('center_axis',(-3.15057456128877E-15,3.72034542862913E-31,
-1.));
#115748=DIRECTION('ref_axis',(1.18084665392185E-16,1.,0.));
#115749=DIRECTION('',(3.15057456128877E-15,-3.72034542862913E-31,1.));
#115750=DIRECTION('center_axis',(-3.15057456128877E-15,3.72034542862913E-31,
-1.));
#115751=DIRECTION('ref_axis',(1.18084665392185E-16,1.,0.));
#115752=DIRECTION('',(3.15057456128877E-15,-3.72034542862913E-31,1.));
#115753=DIRECTION('center_axis',(-3.15057456128877E-15,3.72034542862913E-31,
-1.));
#115754=DIRECTION('ref_axis',(1.18084665392185E-16,1.,0.));
#115755=DIRECTION('',(3.15057456128877E-15,-3.72034542862913E-31,1.));
#115756=DIRECTION('center_axis',(-3.15057456128877E-15,3.72034542862913E-31,
-1.));
#115757=DIRECTION('ref_axis',(1.18084665392185E-16,1.,0.));
#115758=DIRECTION('',(3.15057456128877E-15,-3.72034542862913E-31,1.));
#115759=DIRECTION('center_axis',(-3.15057456128877E-15,3.72034542862913E-31,
-1.));
#115760=DIRECTION('ref_axis',(1.18084665392185E-16,1.,0.));
#115761=DIRECTION('',(3.15057456128877E-15,-3.72034542862913E-31,1.));
#115762=DIRECTION('center_axis',(-3.15057456128877E-15,3.72034542862913E-31,
-1.));
#115763=DIRECTION('ref_axis',(1.18084665392185E-16,1.,0.));
#115764=DIRECTION('',(3.15057456128877E-15,-3.72034542862913E-31,1.));
#115765=DIRECTION('center_axis',(-3.15057456128877E-15,3.72034542862913E-31,
-1.));
#115766=DIRECTION('ref_axis',(1.18084665392185E-16,1.,0.));
#115767=DIRECTION('',(3.15057456128877E-15,-3.72034542862913E-31,1.));
#115768=DIRECTION('center_axis',(-3.15057456128877E-15,3.72034542862913E-31,
-1.));
#115769=DIRECTION('ref_axis',(1.18084665392185E-16,1.,0.));
#115770=DIRECTION('',(3.15057456128877E-15,-3.72034542862913E-31,1.));
#115771=DIRECTION('center_axis',(-3.15057456128877E-15,3.72034542862913E-31,
-1.));
#115772=DIRECTION('ref_axis',(1.18084665392185E-16,1.,0.));
#115773=DIRECTION('',(3.15057456128877E-15,-3.72034542862913E-31,1.));
#115774=DIRECTION('center_axis',(-3.15057456128877E-15,3.72034542862913E-31,
-1.));
#115775=DIRECTION('ref_axis',(1.18084665392185E-16,1.,0.));
#115776=DIRECTION('',(3.15057456128877E-15,-3.72034542862913E-31,1.));
#115777=DIRECTION('center_axis',(-3.15057456128877E-15,3.72034542862913E-31,
-1.));
#115778=DIRECTION('ref_axis',(1.18084665392185E-16,1.,0.));
#115779=DIRECTION('',(3.15057456128877E-15,-3.72034542862913E-31,1.));
#115780=DIRECTION('center_axis',(-3.15057456128877E-15,3.72034542862913E-31,
-1.));
#115781=DIRECTION('ref_axis',(1.18084665392185E-16,1.,0.));
#115782=DIRECTION('',(3.15057456128877E-15,-3.72034542862913E-31,1.));
#115783=DIRECTION('center_axis',(-3.15057456128877E-15,3.72034542862913E-31,
-1.));
#115784=DIRECTION('ref_axis',(1.18084665392185E-16,1.,0.));
#115785=DIRECTION('',(3.15057456128877E-15,-3.72034542862913E-31,1.));
#115786=DIRECTION('center_axis',(-3.15057456128877E-15,3.72034542862913E-31,
-1.));
#115787=DIRECTION('ref_axis',(1.18084665392185E-16,1.,0.));
#115788=DIRECTION('',(3.15057456128877E-15,-3.72034542862913E-31,1.));
#115789=DIRECTION('center_axis',(-3.15057456128877E-15,3.72034542862913E-31,
-1.));
#115790=DIRECTION('ref_axis',(1.18084665392185E-16,1.,0.));
#115791=DIRECTION('',(3.15057456128877E-15,-3.72034542862913E-31,1.));
#115792=DIRECTION('center_axis',(-3.15057456128877E-15,3.72034542862913E-31,
-1.));
#115793=DIRECTION('ref_axis',(1.18084665392185E-16,1.,0.));
#115794=DIRECTION('',(3.15057456128877E-15,-3.72034542862913E-31,1.));
#115795=DIRECTION('center_axis',(-3.15057456128877E-15,3.72034542862913E-31,
-1.));
#115796=DIRECTION('ref_axis',(1.18084665392185E-16,1.,0.));
#115797=DIRECTION('',(3.15057456128877E-15,-3.72034542862913E-31,1.));
#115798=DIRECTION('center_axis',(-3.15057456128877E-15,3.72034542862913E-31,
-1.));
#115799=DIRECTION('ref_axis',(1.18084665392185E-16,1.,0.));
#115800=DIRECTION('',(3.15057456128877E-15,-3.72034542862913E-31,1.));
#115801=DIRECTION('center_axis',(-3.15057456128877E-15,3.72034542862913E-31,
-1.));
#115802=DIRECTION('ref_axis',(1.18084665392185E-16,1.,0.));
#115803=DIRECTION('',(3.15057456128877E-15,-3.72034542862913E-31,1.));
#115804=DIRECTION('center_axis',(-3.15057456128877E-15,3.72034542862913E-31,
-1.));
#115805=DIRECTION('ref_axis',(1.18084665392185E-16,1.,0.));
#115806=DIRECTION('',(3.15057456128877E-15,-3.72034542862913E-31,1.));
#115807=DIRECTION('center_axis',(-3.15057456128877E-15,3.72034542862913E-31,
-1.));
#115808=DIRECTION('ref_axis',(1.18084665392185E-16,1.,0.));
#115809=DIRECTION('',(3.15057456128877E-15,-3.72034542862913E-31,1.));
#115810=DIRECTION('center_axis',(-3.15057456128877E-15,3.72034542862913E-31,
-1.));
#115811=DIRECTION('ref_axis',(1.18084665392185E-16,1.,0.));
#115812=DIRECTION('',(3.15057456128877E-15,-3.72034542862913E-31,1.));
#115813=DIRECTION('center_axis',(-3.15057456128877E-15,3.72034542862913E-31,
-1.));
#115814=DIRECTION('ref_axis',(1.18084665392185E-16,1.,0.));
#115815=DIRECTION('',(3.15057456128877E-15,-3.72034542862913E-31,1.));
#115816=DIRECTION('center_axis',(-3.15057456128877E-15,3.72034542862913E-31,
-1.));
#115817=DIRECTION('ref_axis',(1.18084665392185E-16,1.,0.));
#115818=DIRECTION('',(3.15057456128877E-15,-3.72034542862913E-31,1.));
#115819=DIRECTION('center_axis',(-3.15057456128877E-15,3.72034542862913E-31,
-1.));
#115820=DIRECTION('ref_axis',(1.18084665392185E-16,1.,0.));
#115821=DIRECTION('',(3.15057456128877E-15,-3.72034542862913E-31,1.));
#115822=DIRECTION('center_axis',(1.38133616053571E-12,-4.24340571905306E-12,
-1.));
#115823=DIRECTION('ref_axis',(-1.35431357084844E-12,-1.,4.2434905355515E-12));
#115824=DIRECTION('center_axis',(0.,8.13151629364128E-17,-1.));
#115825=DIRECTION('ref_axis',(0.,1.,8.13151629364128E-17));
#115826=DIRECTION('',(0.,-8.13151629364128E-17,1.));
#115827=DIRECTION('center_axis',(0.,0.,-1.));
#115828=DIRECTION('ref_axis',(1.,0.,0.));
#115829=DIRECTION('center_axis',(0.,8.13151629364128E-17,-1.));
#115830=DIRECTION('ref_axis',(0.,1.,8.13151629364128E-17));
#115831=DIRECTION('',(0.,-8.13151629364128E-17,1.));
#115832=DIRECTION('center_axis',(0.,8.13151629364128E-17,-1.));
#115833=DIRECTION('ref_axis',(0.,1.,8.13151629364128E-17));
#115834=DIRECTION('',(0.,-8.13151629364128E-17,1.));
#115835=DIRECTION('center_axis',(0.,8.13151629364128E-17,-1.));
#115836=DIRECTION('ref_axis',(0.,1.,8.13151629364128E-17));
#115837=DIRECTION('',(0.,-8.13151629364128E-17,1.));
#115838=DIRECTION('center_axis',(0.,8.13151629364128E-17,-1.));
#115839=DIRECTION('ref_axis',(0.,1.,8.13151629364128E-17));
#115840=DIRECTION('',(0.,-8.13151629364128E-17,1.));
#115841=DIRECTION('center_axis',(0.,8.13151629364128E-17,-1.));
#115842=DIRECTION('ref_axis',(0.,1.,8.13151629364128E-17));
#115843=DIRECTION('',(0.,-8.13151629364128E-17,1.));
#115844=DIRECTION('center_axis',(0.,8.13151629364128E-17,-1.));
#115845=DIRECTION('ref_axis',(0.,1.,8.13151629364128E-17));
#115846=DIRECTION('',(0.,-8.13151629364128E-17,1.));
#115847=DIRECTION('center_axis',(0.,8.13151629364128E-17,-1.));
#115848=DIRECTION('ref_axis',(0.,1.,8.13151629364128E-17));
#115849=DIRECTION('',(0.,-8.13151629364128E-17,1.));
#115850=DIRECTION('center_axis',(0.,8.13151629364128E-17,-1.));
#115851=DIRECTION('ref_axis',(0.,1.,8.13151629364128E-17));
#115852=DIRECTION('',(0.,-8.13151629364128E-17,1.));
#115853=DIRECTION('center_axis',(0.,8.13151629364128E-17,-1.));
#115854=DIRECTION('ref_axis',(0.,1.,8.13151629364128E-17));
#115855=DIRECTION('',(0.,-8.13151629364128E-17,1.));
#115856=DIRECTION('center_axis',(0.,8.13151629364128E-17,-1.));
#115857=DIRECTION('ref_axis',(0.,1.,8.13151629364128E-17));
#115858=DIRECTION('',(0.,-8.13151629364128E-17,1.));
#115859=DIRECTION('center_axis',(0.,8.13151629364128E-17,-1.));
#115860=DIRECTION('ref_axis',(0.,1.,8.13151629364128E-17));
#115861=DIRECTION('',(0.,-8.13151629364128E-17,1.));
#115862=DIRECTION('center_axis',(0.,8.13151629364128E-17,-1.));
#115863=DIRECTION('ref_axis',(0.,1.,8.13151629364128E-17));
#115864=DIRECTION('',(0.,-8.13151629364128E-17,1.));
#115865=DIRECTION('center_axis',(0.,8.13151629364128E-17,-1.));
#115866=DIRECTION('ref_axis',(0.,1.,8.13151629364128E-17));
#115867=DIRECTION('',(0.,-8.13151629364128E-17,1.));
#115868=DIRECTION('center_axis',(0.,8.13151629364128E-17,-1.));
#115869=DIRECTION('ref_axis',(0.,1.,8.13151629364128E-17));
#115870=DIRECTION('',(0.,-8.13151629364128E-17,1.));
#115871=DIRECTION('center_axis',(0.,8.13151629364128E-17,-1.));
#115872=DIRECTION('ref_axis',(0.,1.,8.13151629364128E-17));
#115873=DIRECTION('',(0.,-8.13151629364128E-17,1.));
#115874=DIRECTION('center_axis',(0.,8.13151629364128E-17,-1.));
#115875=DIRECTION('ref_axis',(0.,1.,8.13151629364128E-17));
#115876=DIRECTION('',(0.,-8.13151629364128E-17,1.));
#115877=DIRECTION('center_axis',(0.,8.13151629364128E-17,-1.));
#115878=DIRECTION('ref_axis',(0.,1.,8.13151629364128E-17));
#115879=DIRECTION('',(0.,-8.13151629364128E-17,1.));
#115880=DIRECTION('center_axis',(0.,8.13151629364128E-17,-1.));
#115881=DIRECTION('ref_axis',(0.,1.,8.13151629364128E-17));
#115882=DIRECTION('',(0.,-8.13151629364128E-17,1.));
#115883=DIRECTION('center_axis',(0.,8.13151629364128E-17,-1.));
#115884=DIRECTION('ref_axis',(0.,1.,8.13151629364128E-17));
#115885=DIRECTION('',(0.,-8.13151629364128E-17,1.));
#115886=DIRECTION('center_axis',(0.,8.13151629364128E-17,-1.));
#115887=DIRECTION('ref_axis',(0.,1.,8.13151629364128E-17));
#115888=DIRECTION('',(0.,-8.13151629364128E-17,1.));
#115889=DIRECTION('center_axis',(0.,8.13151629364128E-17,-1.));
#115890=DIRECTION('ref_axis',(0.,1.,8.13151629364128E-17));
#115891=DIRECTION('',(0.,-8.13151629364128E-17,1.));
#115892=DIRECTION('center_axis',(0.,8.13151629364128E-17,-1.));
#115893=DIRECTION('ref_axis',(0.,1.,8.13151629364128E-17));
#115894=DIRECTION('',(0.,-8.13151629364128E-17,1.));
#115895=DIRECTION('center_axis',(0.,8.13151629364128E-17,-1.));
#115896=DIRECTION('ref_axis',(0.,1.,8.13151629364128E-17));
#115897=DIRECTION('',(0.,-8.13151629364128E-17,1.));
#115898=DIRECTION('center_axis',(0.,8.13151629364128E-17,-1.));
#115899=DIRECTION('ref_axis',(0.,1.,8.13151629364128E-17));
#115900=DIRECTION('',(0.,-8.13151629364128E-17,1.));
#115901=DIRECTION('center_axis',(0.,8.13151629364128E-17,-1.));
#115902=DIRECTION('ref_axis',(0.,1.,8.13151629364128E-17));
#115903=DIRECTION('',(0.,-8.13151629364128E-17,1.));
#115904=DIRECTION('center_axis',(0.,8.13151629364128E-17,-1.));
#115905=DIRECTION('ref_axis',(0.,1.,8.13151629364128E-17));
#115906=DIRECTION('',(0.,-8.13151629364128E-17,1.));
#115907=DIRECTION('center_axis',(0.,8.13151629364128E-17,-1.));
#115908=DIRECTION('ref_axis',(0.,1.,8.13151629364128E-17));
#115909=DIRECTION('',(0.,-8.13151629364128E-17,1.));
#115910=DIRECTION('center_axis',(0.,8.13151629364128E-17,-1.));
#115911=DIRECTION('ref_axis',(0.,1.,8.13151629364128E-17));
#115912=DIRECTION('',(0.,-8.13151629364128E-17,1.));
#115913=DIRECTION('center_axis',(0.,8.13151629364128E-17,-1.));
#115914=DIRECTION('ref_axis',(0.,1.,8.13151629364128E-17));
#115915=DIRECTION('',(0.,-8.13151629364128E-17,1.));
#115916=DIRECTION('center_axis',(0.,8.13151629364128E-17,-1.));
#115917=DIRECTION('ref_axis',(0.,1.,8.13151629364128E-17));
#115918=DIRECTION('',(0.,-8.13151629364128E-17,1.));
#115919=DIRECTION('center_axis',(0.,0.,1.));
#115920=DIRECTION('ref_axis',(1.,0.,0.));
#115921=DIRECTION('center_axis',(0.,0.,1.));
#115922=DIRECTION('ref_axis',(1.,0.,0.));
#115923=DIRECTION('center_axis',(1.,6.9217303377289E-15,0.));
#115924=DIRECTION('ref_axis',(6.98296267768627E-15,-1.,0.));
#115925=DIRECTION('center_axis',(0.,0.,-1.));
#115926=DIRECTION('ref_axis',(-1.,0.,0.));
#115927=DIRECTION('center_axis',(0.,0.,1.));
#115928=DIRECTION('ref_axis',(1.,0.,0.));
#115929=DIRECTION('center_axis',(0.,0.,-1.));
#115930=DIRECTION('ref_axis',(-1.,0.,0.));
#115931=DIRECTION('center_axis',(0.,0.,-1.));
#115932=DIRECTION('ref_axis',(-1.,0.,0.));
#115933=DIRECTION('',(0.,0.,1.));
#115934=DIRECTION('center_axis',(0.,0.,-1.));
#115935=DIRECTION('ref_axis',(-1.,0.,0.));
#115936=DIRECTION('center_axis',(0.,-8.13151629364128E-17,1.));
#115937=DIRECTION('ref_axis',(0.,-1.,-8.13151629364128E-17));
#115938=DIRECTION('center_axis',(1.38133616053571E-12,-4.24340571905306E-12,
-1.));
#115939=DIRECTION('ref_axis',(-1.35431357084844E-12,-1.,4.2434905355515E-12));
#115940=DIRECTION('center_axis',(0.,-8.13151629364128E-17,1.));
#115941=DIRECTION('ref_axis',(0.,1.,8.13151629364128E-17));
#115942=DIRECTION('',(8.65956056235493E-17,-0.707106781186547,-0.707106781186548));
#115943=DIRECTION('center_axis',(0.,8.13151629364128E-17,-1.));
#115944=DIRECTION('ref_axis',(0.,1.,8.13151629364128E-17));
#115945=DIRECTION('center_axis',(0.,8.13151629364128E-17,-1.));
#115946=DIRECTION('ref_axis',(0.,1.,8.13151629364128E-17));
#115947=DIRECTION('center_axis',(0.,8.13151629364128E-17,-1.));
#115948=DIRECTION('ref_axis',(0.,1.,8.13151629364128E-17));
#115949=DIRECTION('center_axis',(0.,0.,1.));
#115950=DIRECTION('ref_axis',(1.,0.,0.));
#115951=DIRECTION('center_axis',(0.,0.,-1.));
#115952=DIRECTION('ref_axis',(-1.,0.,0.));
#115953=DIRECTION('center_axis',(0.,0.,-1.));
#115954=DIRECTION('ref_axis',(-1.,0.,0.));
#115955=DIRECTION('center_axis',(0.,0.,1.));
#115956=DIRECTION('ref_axis',(1.,0.,0.));
#115957=DIRECTION('center_axis',(0.,0.,1.));
#115958=DIRECTION('ref_axis',(1.,0.,0.));
#115959=DIRECTION('center_axis',(0.,0.,1.));
#115960=DIRECTION('ref_axis',(1.,0.,0.));
#115961=DIRECTION('center_axis',(0.,0.,1.));
#115962=DIRECTION('ref_axis',(1.,0.,0.));
#115963=DIRECTION('center_axis',(0.,0.,1.));
#115964=DIRECTION('ref_axis',(1.,0.,0.));
#115965=DIRECTION('center_axis',(0.,0.,1.));
#115966=DIRECTION('ref_axis',(1.,0.,0.));
#115967=DIRECTION('center_axis',(0.,0.,1.));
#115968=DIRECTION('ref_axis',(1.,0.,0.));
#115969=DIRECTION('center_axis',(0.,0.,1.));
#115970=DIRECTION('ref_axis',(-1.,-3.21624529935327E-16,0.));
#115971=DIRECTION('center_axis',(0.,0.,1.));
#115972=DIRECTION('ref_axis',(1.,0.,0.));
#115973=DIRECTION('center_axis',(0.,0.,1.));
#115974=DIRECTION('ref_axis',(1.,0.,0.));
#115975=DIRECTION('center_axis',(0.,0.,1.));
#115976=DIRECTION('ref_axis',(1.,0.,0.));
#115977=DIRECTION('',(0.866025403784438,0.5,0.));
#115978=DIRECTION('',(0.,1.,0.));
#115979=DIRECTION('',(-0.866025403784439,0.5,0.));
#115980=DIRECTION('',(-0.866025403784438,-0.5,0.));
#115981=DIRECTION('',(1.87789324842145E-16,-1.,0.));
#115982=DIRECTION('',(0.866025403784438,-0.5,0.));
#115983=DIRECTION('center_axis',(1.,0.,0.));
#115984=DIRECTION('ref_axis',(0.,0.,-1.));
#115985=DIRECTION('',(0.,0.,1.));
#115986=DIRECTION('',(0.,0.,1.));
#115987=DIRECTION('center_axis',(0.5,0.866025403784439,0.));
#115988=DIRECTION('ref_axis',(-0.866025403784439,0.5,0.));
#115989=DIRECTION('',(0.,0.,1.));
#115990=DIRECTION('center_axis',(-0.5,0.866025403784439,0.));
#115991=DIRECTION('ref_axis',(-0.866025403784439,-0.5,0.));
#115992=DIRECTION('',(0.,0.,1.));
#115993=DIRECTION('center_axis',(-1.,-1.87789324842145E-16,0.));
#115994=DIRECTION('ref_axis',(1.87789324842145E-16,-1.,0.));
#115995=DIRECTION('',(0.,0.,1.));
#115996=DIRECTION('center_axis',(-0.5,-0.866025403784439,0.));
#115997=DIRECTION('ref_axis',(0.866025403784439,-0.5,0.));
#115998=DIRECTION('',(0.,0.,1.));
#115999=DIRECTION('center_axis',(0.5,-0.866025403784438,0.));
#116000=DIRECTION('ref_axis',(0.866025403784438,0.5,0.));
#116001=DIRECTION('center_axis',(-3.15057456128877E-15,3.72034542862913E-31,
-1.));
#116002=DIRECTION('ref_axis',(1.18084665392185E-16,1.,0.));
#358526=CARTESIAN_POINT('',(0.,0.,0.));
#358527=CARTESIAN_POINT('Origin',(-1.38777878078146E-16,-5.55111512312578E-15,
-17.91875));
#358528=CARTESIAN_POINT('',(2.44788436161308E-14,-1.17524047358083,-2.2));
#358529=CARTESIAN_POINT('',(2.45772990711711E-14,-1.17524047358083,-2.1375));
#358530=CARTESIAN_POINT('',(-4.21481204576211E-16,-1.17524047358085,-17.91875));
#358531=CARTESIAN_POINT('',(-1.43925448419918E-16,-1.17524047358083,-1.7));
#358532=CARTESIAN_POINT('Ctrl Pts',(-1.43925448419918E-16,-1.17524047358083,
-2.2));
#358533=CARTESIAN_POINT('Ctrl Pts',(0.678525403784434,-1.17524047358083,
-2.15833333333333));
#358534=CARTESIAN_POINT('Ctrl Pts',(1.01778810567665,-0.587620236790415,
-2.11666666666667));
#358535=CARTESIAN_POINT('Ctrl Pts',(1.35705080756887,-1.00219152102279E-15,
-2.075));
#358536=CARTESIAN_POINT('Ctrl Pts',(1.01778810567665,0.587620236790412,
-2.03333333333333));
#358537=CARTESIAN_POINT('Ctrl Pts',(0.678525403784435,1.17524047358083,
-1.99166666666667));
#358538=CARTESIAN_POINT('Ctrl Pts',(0.,1.17524047358083,-1.95));
#358539=CARTESIAN_POINT('Ctrl Pts',(-0.678525403784434,1.17524047358083,
-1.90833333333333));
#358540=CARTESIAN_POINT('Ctrl Pts',(-1.01778810567665,0.587620236790413,
-1.86666666666667));
#358541=CARTESIAN_POINT('Ctrl Pts',(-1.35705080756887,-7.79083855215448E-16,
-1.825));
#358542=CARTESIAN_POINT('Ctrl Pts',(-1.01778810567665,-0.587620236790415,
-1.78333333333333));
#358543=CARTESIAN_POINT('Ctrl Pts',(-0.678525403784435,-1.17524047358083,
-1.74166666666667));
#358544=CARTESIAN_POINT('Ctrl Pts',(-1.43925448419918E-16,-1.17524047358083,
-1.7));
#358545=CARTESIAN_POINT('',(-0.823407874165082,-0.838564036615828,-1.7));
#358546=CARTESIAN_POINT('Origin',(-1.01413306947856E-15,-1.11022302462516E-15,
-1.7));
#358547=CARTESIAN_POINT('Ctrl Pts',(-1.43925448419918E-16,-1.17524047358083,
-2.1375));
#358548=CARTESIAN_POINT('Ctrl Pts',(0.678525403784434,-1.17524047358083,
-2.09583333333333));
#358549=CARTESIAN_POINT('Ctrl Pts',(1.01778810567665,-0.587620236790415,
-2.05416666666667));
#358550=CARTESIAN_POINT('Ctrl Pts',(1.35705080756887,-1.02951000095943E-15,
-2.0125));
#358551=CARTESIAN_POINT('Ctrl Pts',(1.01778810567665,0.587620236790413,
-1.97083333333333));
#358552=CARTESIAN_POINT('Ctrl Pts',(0.678525403784435,1.17524047358083,
-1.92916666666667));
#358553=CARTESIAN_POINT('Ctrl Pts',(0.,1.17524047358083,-1.8875));
#358554=CARTESIAN_POINT('Ctrl Pts',(-0.678525403784434,1.17524047358083,
-1.84583333333333));
#358555=CARTESIAN_POINT('Ctrl Pts',(-1.01778810567665,0.587620236790414,
-1.80416666666667));
#358556=CARTESIAN_POINT('Ctrl Pts',(-1.35705080756887,-8.0640233515209E-16,
-1.7625));
#358557=CARTESIAN_POINT('Ctrl Pts',(-1.01778810567665,-0.587620236790415,
-1.72083333333333));
#358558=CARTESIAN_POINT('Ctrl Pts',(-0.937699045799837,-0.726338557627484,
-1.71099716760418));
#358559=CARTESIAN_POINT('Ctrl Pts',(-0.823407874165082,-0.838564036615828,
-1.7));
#358560=CARTESIAN_POINT('Origin',(-1.38777878078146E-16,-5.55111512312578E-15,
-17.91875));
#358561=CARTESIAN_POINT('',(2.36911999758087E-14,-1.17524047358083,-2.7));
#358562=CARTESIAN_POINT('',(2.37896554308489E-14,-1.17524047358083,-2.6375));
#358563=CARTESIAN_POINT('',(-4.21481204576211E-16,-1.17524047358085,-17.91875));
#358564=CARTESIAN_POINT('Ctrl Pts',(-1.43925448419918E-16,-1.17524047358083,
-2.7));
#358565=CARTESIAN_POINT('Ctrl Pts',(0.678525403784434,-1.17524047358083,
-2.65833333333333));
#358566=CARTESIAN_POINT('Ctrl Pts',(1.01778810567665,-0.587620236790415,
-2.61666666666667));
#358567=CARTESIAN_POINT('Ctrl Pts',(1.35705080756887,-7.83643681529645E-16,
-2.575));
#358568=CARTESIAN_POINT('Ctrl Pts',(1.01778810567665,0.587620236790413,
-2.53333333333334));
#358569=CARTESIAN_POINT('Ctrl Pts',(0.678525403784435,1.17524047358083,
-2.49166666666667));
#358570=CARTESIAN_POINT('Ctrl Pts',(0.,1.17524047358083,-2.45));
#358571=CARTESIAN_POINT('Ctrl Pts',(-0.678525403784434,1.17524047358083,
-2.40833333333333));
#358572=CARTESIAN_POINT('Ctrl Pts',(-1.01778810567665,0.587620236790414,
-2.36666666666667));
#358573=CARTESIAN_POINT('Ctrl Pts',(-1.35705080756887,-5.60536015722306E-16,
-2.325));
#358574=CARTESIAN_POINT('Ctrl Pts',(-1.01778810567665,-0.587620236790415,
-2.28333333333333));
#358575=CARTESIAN_POINT('Ctrl Pts',(-0.678525403784435,-1.17524047358083,
-2.24166666666667));
#358576=CARTESIAN_POINT('Ctrl Pts',(-1.43925448419918E-16,-1.17524047358083,
-2.2));
#358577=CARTESIAN_POINT('Ctrl Pts',(-1.43925448419918E-16,-1.17524047358083,
-2.6375));
#358578=CARTESIAN_POINT('Ctrl Pts',(0.678525403784434,-1.17524047358083,
-2.59583333333333));
#358579=CARTESIAN_POINT('Ctrl Pts',(1.01778810567665,-0.587620236790415,
-2.55416666666667));
#358580=CARTESIAN_POINT('Ctrl Pts',(1.35705080756887,-8.10962161466288E-16,
-2.5125));
#358581=CARTESIAN_POINT('Ctrl Pts',(1.01778810567665,0.587620236790413,
-2.47083333333334));
#358582=CARTESIAN_POINT('Ctrl Pts',(0.678525403784435,1.17524047358083,
-2.42916666666667));
#358583=CARTESIAN_POINT('Ctrl Pts',(0.,1.17524047358083,-2.3875));
#358584=CARTESIAN_POINT('Ctrl Pts',(-0.678525403784434,1.17524047358083,
-2.34583333333333));
#358585=CARTESIAN_POINT('Ctrl Pts',(-1.01778810567665,0.587620236790414,
-2.30416666666667));
#358586=CARTESIAN_POINT('Ctrl Pts',(-1.35705080756887,-5.87854495658949E-16,
-2.2625));
#358587=CARTESIAN_POINT('Ctrl Pts',(-1.01778810567665,-0.587620236790415,
-2.22083333333333));
#358588=CARTESIAN_POINT('Ctrl Pts',(-0.678525403784435,-1.17524047358083,
-2.17916666666667));
#358589=CARTESIAN_POINT('Ctrl Pts',(-1.43925448419918E-16,-1.17524047358083,
-2.1375));
#358590=CARTESIAN_POINT('Origin',(-1.38777878078146E-16,-5.55111512312578E-15,
-17.91875));
#358591=CARTESIAN_POINT('',(2.29035563354865E-14,-1.17524047358083,-3.2));
#358592=CARTESIAN_POINT('',(2.30020117905267E-14,-1.17524047358083,-3.1375));
#358593=CARTESIAN_POINT('',(-4.21481204576211E-16,-1.17524047358085,-17.91875));
#358594=CARTESIAN_POINT('Ctrl Pts',(-1.43925448419918E-16,-1.17524047358083,
-3.2));
#358595=CARTESIAN_POINT('Ctrl Pts',(0.678525403784434,-1.17524047358083,
-3.15833333333333));
#358596=CARTESIAN_POINT('Ctrl Pts',(1.01778810567665,-0.587620236790415,
-3.11666666666667));
#358597=CARTESIAN_POINT('Ctrl Pts',(1.35705080756887,-5.65095842036504E-16,
-3.075));
#358598=CARTESIAN_POINT('Ctrl Pts',(1.01778810567665,0.587620236790413,
-3.03333333333333));
#358599=CARTESIAN_POINT('Ctrl Pts',(0.678525403784435,1.17524047358083,
-2.99166666666667));
#358600=CARTESIAN_POINT('Ctrl Pts',(0.,1.17524047358083,-2.95));
#358601=CARTESIAN_POINT('Ctrl Pts',(-0.678525403784434,1.17524047358083,
-2.90833333333333));
#358602=CARTESIAN_POINT('Ctrl Pts',(-1.01778810567665,0.587620236790414,
-2.86666666666667));
#358603=CARTESIAN_POINT('Ctrl Pts',(-1.35705080756887,-3.41988176229165E-16,
-2.825));
#358604=CARTESIAN_POINT('Ctrl Pts',(-1.01778810567665,-0.587620236790414,
-2.78333333333333));
#358605=CARTESIAN_POINT('Ctrl Pts',(-0.678525403784435,-1.17524047358083,
-2.74166666666667));
#358606=CARTESIAN_POINT('Ctrl Pts',(-1.43925448419918E-16,-1.17524047358083,
-2.7));
#358607=CARTESIAN_POINT('Ctrl Pts',(-1.43925448419918E-16,-1.17524047358083,
-3.1375));
#358608=CARTESIAN_POINT('Ctrl Pts',(0.678525403784434,-1.17524047358083,
-3.09583333333333));
#358609=CARTESIAN_POINT('Ctrl Pts',(1.01778810567665,-0.587620236790415,
-3.05416666666667));
#358610=CARTESIAN_POINT('Ctrl Pts',(1.35705080756887,-5.92414321973146E-16,
-3.0125));
#358611=CARTESIAN_POINT('Ctrl Pts',(1.01778810567665,0.587620236790413,
-2.97083333333333));
#358612=CARTESIAN_POINT('Ctrl Pts',(0.678525403784435,1.17524047358083,
-2.92916666666667));
#358613=CARTESIAN_POINT('Ctrl Pts',(0.,1.17524047358083,-2.8875));
#358614=CARTESIAN_POINT('Ctrl Pts',(-0.678525403784434,1.17524047358083,
-2.84583333333333));
#358615=CARTESIAN_POINT('Ctrl Pts',(-1.01778810567665,0.587620236790414,
-2.80416666666667));
#358616=CARTESIAN_POINT('Ctrl Pts',(-1.35705080756887,-3.69306656165807E-16,
-2.7625));
#358617=CARTESIAN_POINT('Ctrl Pts',(-1.01778810567665,-0.587620236790414,
-2.72083333333333));
#358618=CARTESIAN_POINT('Ctrl Pts',(-0.678525403784435,-1.17524047358083,
-2.67916666666667));
#358619=CARTESIAN_POINT('Ctrl Pts',(-1.43925448419918E-16,-1.17524047358083,
-2.6375));
#358620=CARTESIAN_POINT('Origin',(-1.38777878078146E-16,-5.55111512312578E-15,
-17.91875));
#358621=CARTESIAN_POINT('',(2.21159126951643E-14,-1.17524047358083,-3.7));
#358622=CARTESIAN_POINT('',(2.22143681502045E-14,-1.17524047358083,-3.6375));
#358623=CARTESIAN_POINT('',(-4.21481204576211E-16,-1.17524047358085,-17.91875));
#358624=CARTESIAN_POINT('Ctrl Pts',(-1.43925448419918E-16,-1.17524047358083,
-3.7));
#358625=CARTESIAN_POINT('Ctrl Pts',(0.678525403784434,-1.17524047358083,
-3.65833333333333));
#358626=CARTESIAN_POINT('Ctrl Pts',(1.01778810567665,-0.587620236790415,
-3.61666666666667));
#358627=CARTESIAN_POINT('Ctrl Pts',(1.35705080756887,-3.46548002543362E-16,
-3.575));
#358628=CARTESIAN_POINT('Ctrl Pts',(1.01778810567665,0.587620236790413,
-3.53333333333333));
#358629=CARTESIAN_POINT('Ctrl Pts',(0.678525403784435,1.17524047358083,
-3.49166666666667));
#358630=CARTESIAN_POINT('Ctrl Pts',(0.,1.17524047358083,-3.45));
#358631=CARTESIAN_POINT('Ctrl Pts',(-0.678525403784434,1.17524047358083,
-3.40833333333333));
#358632=CARTESIAN_POINT('Ctrl Pts',(-1.01778810567665,0.587620236790414,
-3.36666666666667));
#358633=CARTESIAN_POINT('Ctrl Pts',(-1.35705080756887,-1.23440336736023E-16,
-3.325));
#358634=CARTESIAN_POINT('Ctrl Pts',(-1.01778810567665,-0.587620236790414,
-3.28333333333333));
#358635=CARTESIAN_POINT('Ctrl Pts',(-0.678525403784435,-1.17524047358083,
-3.24166666666667));
#358636=CARTESIAN_POINT('Ctrl Pts',(-1.43925448419918E-16,-1.17524047358083,
-3.2));
#358637=CARTESIAN_POINT('Ctrl Pts',(-1.43925448419918E-16,-1.17524047358083,
-3.6375));
#358638=CARTESIAN_POINT('Ctrl Pts',(0.678525403784434,-1.17524047358083,
-3.59583333333333));
#358639=CARTESIAN_POINT('Ctrl Pts',(1.01778810567665,-0.587620236790415,
-3.55416666666667));
#358640=CARTESIAN_POINT('Ctrl Pts',(1.35705080756887,-3.73866482480005E-16,
-3.5125));
#358641=CARTESIAN_POINT('Ctrl Pts',(1.01778810567665,0.587620236790413,
-3.47083333333333));
#358642=CARTESIAN_POINT('Ctrl Pts',(0.678525403784435,1.17524047358083,
-3.42916666666667));
#358643=CARTESIAN_POINT('Ctrl Pts',(0.,1.17524047358083,-3.3875));
#358644=CARTESIAN_POINT('Ctrl Pts',(-0.678525403784434,1.17524047358083,
-3.34583333333333));
#358645=CARTESIAN_POINT('Ctrl Pts',(-1.01778810567665,0.587620236790414,
-3.30416666666667));
#358646=CARTESIAN_POINT('Ctrl Pts',(-1.35705080756887,-1.50758816672666E-16,
-3.2625));
#358647=CARTESIAN_POINT('Ctrl Pts',(-1.01778810567665,-0.587620236790414,
-3.22083333333333));
#358648=CARTESIAN_POINT('Ctrl Pts',(-0.678525403784435,-1.17524047358083,
-3.17916666666667));
#358649=CARTESIAN_POINT('Ctrl Pts',(-1.43925448419918E-16,-1.17524047358083,
-3.1375));
#358650=CARTESIAN_POINT('Origin',(-1.38777878078146E-16,-5.55111512312578E-15,
-17.91875));
#358651=CARTESIAN_POINT('',(2.13282690548421E-14,-1.17524047358083,-4.2));
#358652=CARTESIAN_POINT('',(2.14267245098824E-14,-1.17524047358083,-4.1375));
#358653=CARTESIAN_POINT('',(-4.21481204576211E-16,-1.17524047358085,-17.91875));
#358654=CARTESIAN_POINT('Ctrl Pts',(-1.43925448419918E-16,-1.17524047358083,
-4.2));
#358655=CARTESIAN_POINT('Ctrl Pts',(0.678525403784434,-1.17524047358083,
-4.15833333333333));
#358656=CARTESIAN_POINT('Ctrl Pts',(1.01778810567665,-0.587620236790415,
-4.11666666666667));
#358657=CARTESIAN_POINT('Ctrl Pts',(1.35705080756887,-1.28000163050222E-16,
-4.075));
#358658=CARTESIAN_POINT('Ctrl Pts',(1.01778810567665,0.587620236790413,
-4.03333333333333));
#358659=CARTESIAN_POINT('Ctrl Pts',(0.678525403784435,1.17524047358083,
-3.99166666666667));
#358660=CARTESIAN_POINT('Ctrl Pts',(0.,1.17524047358083,-3.95));
#358661=CARTESIAN_POINT('Ctrl Pts',(-0.678525403784434,1.17524047358083,
-3.90833333333334));
#358662=CARTESIAN_POINT('Ctrl Pts',(-1.01778810567665,0.587620236790414,
-3.86666666666667));
#358663=CARTESIAN_POINT('Ctrl Pts',(-1.35705080756887,9.5107502757118E-17,
-3.825));
#358664=CARTESIAN_POINT('Ctrl Pts',(-1.01778810567665,-0.587620236790414,
-3.78333333333333));
#358665=CARTESIAN_POINT('Ctrl Pts',(-0.678525403784435,-1.17524047358083,
-3.74166666666667));
#358666=CARTESIAN_POINT('Ctrl Pts',(-1.43925448419918E-16,-1.17524047358083,
-3.7));
#358667=CARTESIAN_POINT('Ctrl Pts',(-1.43925448419918E-16,-1.17524047358083,
-4.1375));
#358668=CARTESIAN_POINT('Ctrl Pts',(0.678525403784434,-1.17524047358083,
-4.09583333333333));
#358669=CARTESIAN_POINT('Ctrl Pts',(1.01778810567665,-0.587620236790415,
-4.05416666666667));
#358670=CARTESIAN_POINT('Ctrl Pts',(1.35705080756887,-1.55318642986864E-16,
-4.0125));
#358671=CARTESIAN_POINT('Ctrl Pts',(1.01778810567665,0.587620236790414,
-3.97083333333333));
#358672=CARTESIAN_POINT('Ctrl Pts',(0.678525403784435,1.17524047358083,
-3.92916666666667));
#358673=CARTESIAN_POINT('Ctrl Pts',(0.,1.17524047358083,-3.8875));
#358674=CARTESIAN_POINT('Ctrl Pts',(-0.678525403784434,1.17524047358083,
-3.84583333333333));
#358675=CARTESIAN_POINT('Ctrl Pts',(-1.01778810567665,0.587620236790414,
-3.80416666666667));
#358676=CARTESIAN_POINT('Ctrl Pts',(-1.35705080756887,6.77890228204754E-17,
-3.7625));
#358677=CARTESIAN_POINT('Ctrl Pts',(-1.01778810567665,-0.587620236790414,
-3.72083333333333));
#358678=CARTESIAN_POINT('Ctrl Pts',(-0.678525403784435,-1.17524047358083,
-3.67916666666667));
#358679=CARTESIAN_POINT('Ctrl Pts',(-1.43925448419918E-16,-1.17524047358083,
-3.6375));
#358680=CARTESIAN_POINT('Origin',(-1.38777878078146E-16,-5.55111512312578E-15,
-17.91875));
#358681=CARTESIAN_POINT('',(2.05406254145199E-14,-1.17524047358083,-4.7));
#358682=CARTESIAN_POINT('',(2.06390808695602E-14,-1.17524047358083,-4.6375));
#358683=CARTESIAN_POINT('',(-4.21481204576211E-16,-1.17524047358085,-17.91875));
#358684=CARTESIAN_POINT('Ctrl Pts',(-1.43925448419918E-16,-1.17524047358083,
-4.7));
#358685=CARTESIAN_POINT('Ctrl Pts',(0.678525403784434,-1.17524047358083,
-4.65833333333333));
#358686=CARTESIAN_POINT('Ctrl Pts',(1.01778810567665,-0.587620236790414,
-4.61666666666667));
#358687=CARTESIAN_POINT('Ctrl Pts',(1.35705080756887,9.05476764429197E-17,
-4.575));
#358688=CARTESIAN_POINT('Ctrl Pts',(1.01778810567665,0.587620236790414,
-4.53333333333333));
#358689=CARTESIAN_POINT('Ctrl Pts',(0.678525403784435,1.17524047358083,
-4.49166666666667));
#358690=CARTESIAN_POINT('Ctrl Pts',(0.,1.17524047358083,-4.45));
#358691=CARTESIAN_POINT('Ctrl Pts',(-0.678525403784434,1.17524047358083,
-4.40833333333333));
#358692=CARTESIAN_POINT('Ctrl Pts',(-1.01778810567665,0.587620236790414,
-4.36666666666667));
#358693=CARTESIAN_POINT('Ctrl Pts',(-1.35705080756887,3.13655342250259E-16,
-4.325));
#358694=CARTESIAN_POINT('Ctrl Pts',(-1.01778810567665,-0.587620236790414,
-4.28333333333333));
#358695=CARTESIAN_POINT('Ctrl Pts',(-0.678525403784435,-1.17524047358083,
-4.24166666666667));
#358696=CARTESIAN_POINT('Ctrl Pts',(-1.43925448419918E-16,-1.17524047358083,
-4.2));
#358697=CARTESIAN_POINT('Ctrl Pts',(-1.43925448419918E-16,-1.17524047358083,
-4.6375));
#358698=CARTESIAN_POINT('Ctrl Pts',(0.678525403784434,-1.17524047358083,
-4.59583333333333));
#358699=CARTESIAN_POINT('Ctrl Pts',(1.01778810567665,-0.587620236790414,
-4.55416666666667));
#358700=CARTESIAN_POINT('Ctrl Pts',(1.35705080756887,6.32291965062771E-17,
-4.5125));
#358701=CARTESIAN_POINT('Ctrl Pts',(1.01778810567665,0.587620236790414,
-4.47083333333333));
#358702=CARTESIAN_POINT('Ctrl Pts',(0.678525403784435,1.17524047358083,
-4.42916666666667));
#358703=CARTESIAN_POINT('Ctrl Pts',(0.,1.17524047358083,-4.3875));
#358704=CARTESIAN_POINT('Ctrl Pts',(-0.678525403784434,1.17524047358083,
-4.34583333333333));
#358705=CARTESIAN_POINT('Ctrl Pts',(-1.01778810567665,0.587620236790415,
-4.30416666666667));
#358706=CARTESIAN_POINT('Ctrl Pts',(-1.35705080756887,2.86336862313616E-16,
-4.2625));
#358707=CARTESIAN_POINT('Ctrl Pts',(-1.01778810567665,-0.587620236790414,
-4.22083333333333));
#358708=CARTESIAN_POINT('Ctrl Pts',(-0.678525403784435,-1.17524047358083,
-4.17916666666667));
#358709=CARTESIAN_POINT('Ctrl Pts',(-1.43925448419918E-16,-1.17524047358083,
-4.1375));
#358710=CARTESIAN_POINT('Origin',(-1.38777878078146E-16,-5.55111512312578E-15,
-17.91875));
#358711=CARTESIAN_POINT('',(1.97529817741977E-14,-1.17524047358083,-5.2));
#358712=CARTESIAN_POINT('',(1.9851437229238E-14,-1.17524047358083,-5.1375));
#358713=CARTESIAN_POINT('',(-4.21481204576211E-16,-1.17524047358085,-17.91875));
#358714=CARTESIAN_POINT('Ctrl Pts',(-1.43925448419918E-16,-1.17524047358083,
-5.2));
#358715=CARTESIAN_POINT('Ctrl Pts',(0.678525403784434,-1.17524047358083,
-5.15833333333333));
#358716=CARTESIAN_POINT('Ctrl Pts',(1.01778810567665,-0.587620236790414,
-5.11666666666667));
#358717=CARTESIAN_POINT('Ctrl Pts',(1.35705080756887,3.09095515936061E-16,
-5.075));
#358718=CARTESIAN_POINT('Ctrl Pts',(1.01778810567665,0.587620236790414,
-5.03333333333333));
#358719=CARTESIAN_POINT('Ctrl Pts',(0.678525403784435,1.17524047358083,
-4.99166666666667));
#358720=CARTESIAN_POINT('Ctrl Pts',(0.,1.17524047358083,-4.95));
#358721=CARTESIAN_POINT('Ctrl Pts',(-0.678525403784434,1.17524047358083,
-4.90833333333333));
#358722=CARTESIAN_POINT('Ctrl Pts',(-1.01778810567665,0.587620236790415,
-4.86666666666667));
#358723=CARTESIAN_POINT('Ctrl Pts',(-1.35705080756887,5.322031817434E-16,
-4.825));
#358724=CARTESIAN_POINT('Ctrl Pts',(-1.01778810567665,-0.587620236790414,
-4.78333333333333));
#358725=CARTESIAN_POINT('Ctrl Pts',(-0.678525403784435,-1.17524047358083,
-4.74166666666667));
#358726=CARTESIAN_POINT('Ctrl Pts',(-1.43925448419918E-16,-1.17524047358083,
-4.7));
#358727=CARTESIAN_POINT('Ctrl Pts',(-1.43925448419918E-16,-1.17524047358083,
-5.1375));
#358728=CARTESIAN_POINT('Ctrl Pts',(0.678525403784434,-1.17524047358083,
-5.09583333333333));
#358729=CARTESIAN_POINT('Ctrl Pts',(1.01778810567665,-0.587620236790414,
-5.05416666666667));
#358730=CARTESIAN_POINT('Ctrl Pts',(1.35705080756887,2.81777035999419E-16,
-5.0125));
#358731=CARTESIAN_POINT('Ctrl Pts',(1.01778810567665,0.587620236790414,
-4.97083333333333));
#358732=CARTESIAN_POINT('Ctrl Pts',(0.678525403784435,1.17524047358083,
-4.92916666666667));
#358733=CARTESIAN_POINT('Ctrl Pts',(0.,1.17524047358083,-4.8875));
#358734=CARTESIAN_POINT('Ctrl Pts',(-0.678525403784434,1.17524047358083,
-4.84583333333333));
#358735=CARTESIAN_POINT('Ctrl Pts',(-1.01778810567665,0.587620236790415,
-4.80416666666667));
#358736=CARTESIAN_POINT('Ctrl Pts',(-1.35705080756887,5.04884701806758E-16,
-4.7625));
#358737=CARTESIAN_POINT('Ctrl Pts',(-1.01778810567665,-0.587620236790414,
-4.72083333333333));
#358738=CARTESIAN_POINT('Ctrl Pts',(-0.678525403784435,-1.17524047358083,
-4.67916666666667));
#358739=CARTESIAN_POINT('Ctrl Pts',(-1.43925448419918E-16,-1.17524047358083,
-4.6375));
#358740=CARTESIAN_POINT('Origin',(-1.38777878078146E-16,-5.55111512312578E-15,
-17.91875));
#358741=CARTESIAN_POINT('',(1.89653381338755E-14,-1.17524047358083,-5.7));
#358742=CARTESIAN_POINT('',(1.90637935889158E-14,-1.17524047358083,-5.6375));
#358743=CARTESIAN_POINT('',(-4.21481204576211E-16,-1.17524047358085,-17.91875));
#358744=CARTESIAN_POINT('Ctrl Pts',(-1.43925448419918E-16,-1.17524047358083,
-5.7));
#358745=CARTESIAN_POINT('Ctrl Pts',(0.678525403784434,-1.17524047358083,
-5.65833333333333));
#358746=CARTESIAN_POINT('Ctrl Pts',(1.01778810567665,-0.587620236790414,
-5.61666666666667));
#358747=CARTESIAN_POINT('Ctrl Pts',(1.35705080756887,5.27643355429203E-16,
-5.575));
#358748=CARTESIAN_POINT('Ctrl Pts',(1.01778810567665,0.587620236790414,
-5.53333333333334));
#358749=CARTESIAN_POINT('Ctrl Pts',(0.678525403784435,1.17524047358083,
-5.49166666666667));
#358750=CARTESIAN_POINT('Ctrl Pts',(0.,1.17524047358083,-5.45));
#358751=CARTESIAN_POINT('Ctrl Pts',(-0.678525403784434,1.17524047358083,
-5.40833333333333));
#358752=CARTESIAN_POINT('Ctrl Pts',(-1.01778810567665,0.587620236790415,
-5.36666666666667));
#358753=CARTESIAN_POINT('Ctrl Pts',(-1.35705080756887,7.50751021236542E-16,
-5.325));
#358754=CARTESIAN_POINT('Ctrl Pts',(-1.01778810567665,-0.587620236790413,
-5.28333333333333));
#358755=CARTESIAN_POINT('Ctrl Pts',(-0.678525403784435,-1.17524047358083,
-5.24166666666667));
#358756=CARTESIAN_POINT('Ctrl Pts',(-1.43925448419918E-16,-1.17524047358083,
-5.2));
#358757=CARTESIAN_POINT('Ctrl Pts',(-1.43925448419918E-16,-1.17524047358083,
-5.6375));
#358758=CARTESIAN_POINT('Ctrl Pts',(0.678525403784434,-1.17524047358083,
-5.59583333333333));
#358759=CARTESIAN_POINT('Ctrl Pts',(1.01778810567665,-0.587620236790414,
-5.55416666666667));
#358760=CARTESIAN_POINT('Ctrl Pts',(1.35705080756887,5.0032487549256E-16,
-5.5125));
#358761=CARTESIAN_POINT('Ctrl Pts',(1.01778810567665,0.587620236790414,
-5.47083333333333));
#358762=CARTESIAN_POINT('Ctrl Pts',(0.678525403784435,1.17524047358083,
-5.42916666666667));
#358763=CARTESIAN_POINT('Ctrl Pts',(0.,1.17524047358083,-5.3875));
#358764=CARTESIAN_POINT('Ctrl Pts',(-0.678525403784434,1.17524047358083,
-5.34583333333333));
#358765=CARTESIAN_POINT('Ctrl Pts',(-1.01778810567665,0.587620236790415,
-5.30416666666667));
#358766=CARTESIAN_POINT('Ctrl Pts',(-1.35705080756887,7.23432541299899E-16,
-5.2625));
#358767=CARTESIAN_POINT('Ctrl Pts',(-1.01778810567665,-0.587620236790413,
-5.22083333333333));
#358768=CARTESIAN_POINT('Ctrl Pts',(-0.678525403784435,-1.17524047358083,
-5.17916666666667));
#358769=CARTESIAN_POINT('Ctrl Pts',(-1.43925448419918E-16,-1.17524047358083,
-5.1375));
#358770=CARTESIAN_POINT('Origin',(-1.38777878078146E-16,-5.55111512312578E-15,
-17.91875));
#358771=CARTESIAN_POINT('',(1.81776944935533E-14,-1.17524047358083,-6.2));
#358772=CARTESIAN_POINT('',(1.82761499485936E-14,-1.17524047358083,-6.1375));
#358773=CARTESIAN_POINT('',(-4.21481204576211E-16,-1.17524047358085,-17.91875));
#358774=CARTESIAN_POINT('Ctrl Pts',(-1.43925448419918E-16,-1.17524047358083,
-6.2));
#358775=CARTESIAN_POINT('Ctrl Pts',(0.678525403784434,-1.17524047358083,
-6.15833333333334));
#358776=CARTESIAN_POINT('Ctrl Pts',(1.01778810567665,-0.587620236790414,
-6.11666666666667));
#358777=CARTESIAN_POINT('Ctrl Pts',(1.35705080756887,7.46191194922343E-16,
-6.075));
#358778=CARTESIAN_POINT('Ctrl Pts',(1.01778810567665,0.587620236790414,
-6.03333333333333));
#358779=CARTESIAN_POINT('Ctrl Pts',(0.678525403784435,1.17524047358083,
-5.99166666666667));
#358780=CARTESIAN_POINT('Ctrl Pts',(0.,1.17524047358083,-5.95));
#358781=CARTESIAN_POINT('Ctrl Pts',(-0.678525403784434,1.17524047358083,
-5.90833333333333));
#358782=CARTESIAN_POINT('Ctrl Pts',(-1.01778810567665,0.587620236790415,
-5.86666666666667));
#358783=CARTESIAN_POINT('Ctrl Pts',(-1.35705080756887,9.69298860729681E-16,
-5.825));
#358784=CARTESIAN_POINT('Ctrl Pts',(-1.01778810567665,-0.587620236790413,
-5.78333333333333));
#358785=CARTESIAN_POINT('Ctrl Pts',(-0.678525403784435,-1.17524047358083,
-5.74166666666667));
#358786=CARTESIAN_POINT('Ctrl Pts',(-1.43925448419918E-16,-1.17524047358083,
-5.7));
#358787=CARTESIAN_POINT('Ctrl Pts',(-1.43925448419918E-16,-1.17524047358083,
-6.1375));
#358788=CARTESIAN_POINT('Ctrl Pts',(0.678525403784434,-1.17524047358083,
-6.09583333333334));
#358789=CARTESIAN_POINT('Ctrl Pts',(1.01778810567665,-0.587620236790414,
-6.05416666666667));
#358790=CARTESIAN_POINT('Ctrl Pts',(1.35705080756887,7.18872714985701E-16,
-6.0125));
#358791=CARTESIAN_POINT('Ctrl Pts',(1.01778810567665,0.587620236790414,
-5.97083333333333));
#358792=CARTESIAN_POINT('Ctrl Pts',(0.678525403784435,1.17524047358083,
-5.92916666666667));
#358793=CARTESIAN_POINT('Ctrl Pts',(0.,1.17524047358083,-5.8875));
#358794=CARTESIAN_POINT('Ctrl Pts',(-0.678525403784434,1.17524047358083,
-5.84583333333334));
#358795=CARTESIAN_POINT('Ctrl Pts',(-1.01778810567665,0.587620236790415,
-5.80416666666667));
#358796=CARTESIAN_POINT('Ctrl Pts',(-1.35705080756887,9.41980380793039E-16,
-5.7625));
#358797=CARTESIAN_POINT('Ctrl Pts',(-1.01778810567665,-0.587620236790413,
-5.72083333333333));
#358798=CARTESIAN_POINT('Ctrl Pts',(-0.678525403784435,-1.17524047358083,
-5.67916666666667));
#358799=CARTESIAN_POINT('Ctrl Pts',(-1.43925448419918E-16,-1.17524047358083,
-5.6375));
#358800=CARTESIAN_POINT('Origin',(-1.38777878078146E-16,-5.55111512312578E-15,
-17.91875));
#358801=CARTESIAN_POINT('',(1.73900508532311E-14,-1.17524047358083,-6.7));
#358802=CARTESIAN_POINT('',(1.74885063082714E-14,-1.17524047358083,-6.6375));
#358803=CARTESIAN_POINT('',(-4.21481204576211E-16,-1.17524047358085,-17.91875));
#358804=CARTESIAN_POINT('Ctrl Pts',(-1.43925448419918E-16,-1.17524047358083,
-6.7));
#358805=CARTESIAN_POINT('Ctrl Pts',(0.678525403784434,-1.17524047358083,
-6.65833333333333));
#358806=CARTESIAN_POINT('Ctrl Pts',(1.01778810567665,-0.587620236790414,
-6.61666666666667));
#358807=CARTESIAN_POINT('Ctrl Pts',(1.35705080756887,9.64739034415485E-16,
-6.575));
#358808=CARTESIAN_POINT('Ctrl Pts',(1.01778810567665,0.587620236790414,
-6.53333333333333));
#358809=CARTESIAN_POINT('Ctrl Pts',(0.678525403784435,1.17524047358083,
-6.49166666666667));
#358810=CARTESIAN_POINT('Ctrl Pts',(0.,1.17524047358083,-6.45));
#358811=CARTESIAN_POINT('Ctrl Pts',(-0.678525403784434,1.17524047358083,
-6.40833333333334));
#358812=CARTESIAN_POINT('Ctrl Pts',(-1.01778810567665,0.587620236790415,
-6.36666666666667));
#358813=CARTESIAN_POINT('Ctrl Pts',(-1.35705080756887,1.18784670022282E-15,
-6.325));
#358814=CARTESIAN_POINT('Ctrl Pts',(-1.01778810567665,-0.587620236790413,
-6.28333333333333));
#358815=CARTESIAN_POINT('Ctrl Pts',(-0.678525403784435,-1.17524047358083,
-6.24166666666667));
#358816=CARTESIAN_POINT('Ctrl Pts',(-1.43925448419918E-16,-1.17524047358083,
-6.2));
#358817=CARTESIAN_POINT('Ctrl Pts',(-1.43925448419918E-16,-1.17524047358083,
-6.6375));
#358818=CARTESIAN_POINT('Ctrl Pts',(0.678525403784434,-1.17524047358083,
-6.59583333333333));
#358819=CARTESIAN_POINT('Ctrl Pts',(1.01778810567665,-0.587620236790414,
-6.55416666666667));
#358820=CARTESIAN_POINT('Ctrl Pts',(1.35705080756887,9.37420554478842E-16,
-6.5125));
#358821=CARTESIAN_POINT('Ctrl Pts',(1.01778810567665,0.587620236790415,
-6.47083333333333));
#358822=CARTESIAN_POINT('Ctrl Pts',(0.678525403784435,1.17524047358083,
-6.42916666666667));
#358823=CARTESIAN_POINT('Ctrl Pts',(0.,1.17524047358083,-6.3875));
#358824=CARTESIAN_POINT('Ctrl Pts',(-0.678525403784434,1.17524047358083,
-6.34583333333333));
#358825=CARTESIAN_POINT('Ctrl Pts',(-1.01778810567665,0.587620236790415,
-6.30416666666667));
#358826=CARTESIAN_POINT('Ctrl Pts',(-1.35705080756887,1.16052822028618E-15,
-6.2625));
#358827=CARTESIAN_POINT('Ctrl Pts',(-1.01778810567665,-0.587620236790413,
-6.22083333333333));
#358828=CARTESIAN_POINT('Ctrl Pts',(-0.678525403784435,-1.17524047358083,
-6.17916666666667));
#358829=CARTESIAN_POINT('Ctrl Pts',(-1.43925448419918E-16,-1.17524047358083,
-6.1375));
#358830=CARTESIAN_POINT('Origin',(-1.38777878078146E-16,-5.55111512312578E-15,
-17.91875));
#358831=CARTESIAN_POINT('',(1.66024072129089E-14,-1.17524047358083,-7.2));
#358832=CARTESIAN_POINT('',(1.67008626679492E-14,-1.17524047358083,-7.1375));
#358833=CARTESIAN_POINT('',(-4.21481204576211E-16,-1.17524047358085,-17.91875));
#358834=CARTESIAN_POINT('Ctrl Pts',(-1.43925448419918E-16,-1.17524047358083,
-7.2));
#358835=CARTESIAN_POINT('Ctrl Pts',(0.678525403784434,-1.17524047358083,
-7.15833333333333));
#358836=CARTESIAN_POINT('Ctrl Pts',(1.01778810567665,-0.587620236790413,
-7.11666666666667));
#358837=CARTESIAN_POINT('Ctrl Pts',(1.35705080756887,1.18328687390863E-15,
-7.075));
#358838=CARTESIAN_POINT('Ctrl Pts',(1.01778810567665,0.587620236790415,
-7.03333333333333));
#358839=CARTESIAN_POINT('Ctrl Pts',(0.678525403784435,1.17524047358083,
-6.99166666666667));
#358840=CARTESIAN_POINT('Ctrl Pts',(0.,1.17524047358083,-6.95));
#358841=CARTESIAN_POINT('Ctrl Pts',(-0.678525403784434,1.17524047358083,
-6.90833333333333));
#358842=CARTESIAN_POINT('Ctrl Pts',(-1.01778810567665,0.587620236790415,
-6.86666666666667));
#358843=CARTESIAN_POINT('Ctrl Pts',(-1.35705080756887,1.40639453971596E-15,
-6.825));
#358844=CARTESIAN_POINT('Ctrl Pts',(-1.01778810567665,-0.587620236790413,
-6.78333333333333));
#358845=CARTESIAN_POINT('Ctrl Pts',(-0.678525403784435,-1.17524047358083,
-6.74166666666667));
#358846=CARTESIAN_POINT('Ctrl Pts',(-1.43925448419918E-16,-1.17524047358083,
-6.7));
#358847=CARTESIAN_POINT('Ctrl Pts',(-1.43925448419918E-16,-1.17524047358083,
-7.1375));
#358848=CARTESIAN_POINT('Ctrl Pts',(0.678525403784434,-1.17524047358083,
-7.09583333333333));
#358849=CARTESIAN_POINT('Ctrl Pts',(1.01778810567665,-0.587620236790413,
-7.05416666666667));
#358850=CARTESIAN_POINT('Ctrl Pts',(1.35705080756887,1.15596839397198E-15,
-7.0125));
#358851=CARTESIAN_POINT('Ctrl Pts',(1.01778810567665,0.587620236790415,
-6.97083333333333));
#358852=CARTESIAN_POINT('Ctrl Pts',(0.678525403784435,1.17524047358083,
-6.92916666666667));
#358853=CARTESIAN_POINT('Ctrl Pts',(0.,1.17524047358083,-6.8875));
#358854=CARTESIAN_POINT('Ctrl Pts',(-0.678525403784434,1.17524047358083,
-6.84583333333333));
#358855=CARTESIAN_POINT('Ctrl Pts',(-1.01778810567665,0.587620236790416,
-6.80416666666667));
#358856=CARTESIAN_POINT('Ctrl Pts',(-1.35705080756887,1.37907605977932E-15,
-6.7625));
#358857=CARTESIAN_POINT('Ctrl Pts',(-1.01778810567665,-0.587620236790413,
-6.72083333333333));
#358858=CARTESIAN_POINT('Ctrl Pts',(-0.678525403784435,-1.17524047358083,
-6.67916666666667));
#358859=CARTESIAN_POINT('Ctrl Pts',(-1.43925448419918E-16,-1.17524047358083,
-6.6375));
#358860=CARTESIAN_POINT('Origin',(-1.38777878078146E-16,-5.55111512312578E-15,
-17.91875));
#358861=CARTESIAN_POINT('',(1.58147635725867E-14,-1.17524047358083,-7.7));
#358862=CARTESIAN_POINT('',(1.5913219027627E-14,-1.17524047358083,-7.6375));
#358863=CARTESIAN_POINT('',(-4.21481204576211E-16,-1.17524047358085,-17.91875));
#358864=CARTESIAN_POINT('Ctrl Pts',(-1.43925448419918E-16,-1.17524047358083,
-7.7));
#358865=CARTESIAN_POINT('Ctrl Pts',(0.678525403784434,-1.17524047358083,
-7.65833333333334));
#358866=CARTESIAN_POINT('Ctrl Pts',(1.01778810567665,-0.587620236790413,
-7.61666666666667));
#358867=CARTESIAN_POINT('Ctrl Pts',(1.35705080756887,1.40183471340177E-15,
-7.575));
#358868=CARTESIAN_POINT('Ctrl Pts',(1.01778810567665,0.587620236790415,
-7.53333333333333));
#358869=CARTESIAN_POINT('Ctrl Pts',(0.678525403784435,1.17524047358083,
-7.49166666666667));
#358870=CARTESIAN_POINT('Ctrl Pts',(0.,1.17524047358083,-7.45));
#358871=CARTESIAN_POINT('Ctrl Pts',(-0.678525403784434,1.17524047358083,
-7.40833333333333));
#358872=CARTESIAN_POINT('Ctrl Pts',(-1.01778810567665,0.587620236790416,
-7.36666666666667));
#358873=CARTESIAN_POINT('Ctrl Pts',(-1.35705080756887,1.62494237920911E-15,
-7.325));
#358874=CARTESIAN_POINT('Ctrl Pts',(-1.01778810567665,-0.587620236790412,
-7.28333333333333));
#358875=CARTESIAN_POINT('Ctrl Pts',(-0.678525403784435,-1.17524047358083,
-7.24166666666667));
#358876=CARTESIAN_POINT('Ctrl Pts',(-1.43925448419918E-16,-1.17524047358083,
-7.2));
#358877=CARTESIAN_POINT('Ctrl Pts',(-1.43925448419918E-16,-1.17524047358083,
-7.6375));
#358878=CARTESIAN_POINT('Ctrl Pts',(0.678525403784434,-1.17524047358083,
-7.59583333333333));
#358879=CARTESIAN_POINT('Ctrl Pts',(1.01778810567665,-0.587620236790413,
-7.55416666666667));
#358880=CARTESIAN_POINT('Ctrl Pts',(1.35705080756887,1.37451623346513E-15,
-7.5125));
#358881=CARTESIAN_POINT('Ctrl Pts',(1.01778810567665,0.587620236790415,
-7.47083333333333));
#358882=CARTESIAN_POINT('Ctrl Pts',(0.678525403784435,1.17524047358083,
-7.42916666666667));
#358883=CARTESIAN_POINT('Ctrl Pts',(0.,1.17524047358083,-7.3875));
#358884=CARTESIAN_POINT('Ctrl Pts',(-0.678525403784434,1.17524047358083,
-7.34583333333333));
#358885=CARTESIAN_POINT('Ctrl Pts',(-1.01778810567665,0.587620236790416,
-7.30416666666667));
#358886=CARTESIAN_POINT('Ctrl Pts',(-1.35705080756887,1.59762389927246E-15,
-7.2625));
#358887=CARTESIAN_POINT('Ctrl Pts',(-1.01778810567665,-0.587620236790412,
-7.22083333333333));
#358888=CARTESIAN_POINT('Ctrl Pts',(-0.678525403784435,-1.17524047358083,
-7.17916666666667));
#358889=CARTESIAN_POINT('Ctrl Pts',(-1.43925448419918E-16,-1.17524047358083,
-7.1375));
#358890=CARTESIAN_POINT('Origin',(-1.38777878078146E-16,-5.55111512312578E-15,
-17.91875));
#358891=CARTESIAN_POINT('',(1.50271199322645E-14,-1.17524047358083,-8.2));
#358892=CARTESIAN_POINT('',(1.51255753873048E-14,-1.17524047358083,-8.1375));
#358893=CARTESIAN_POINT('',(-4.21481204576211E-16,-1.17524047358085,-17.91875));
#358894=CARTESIAN_POINT('Ctrl Pts',(-1.43925448419918E-16,-1.17524047358083,
-8.2));
#358895=CARTESIAN_POINT('Ctrl Pts',(0.678525403784434,-1.17524047358083,
-8.15833333333333));
#358896=CARTESIAN_POINT('Ctrl Pts',(1.01778810567665,-0.587620236790413,
-8.11666666666667));
#358897=CARTESIAN_POINT('Ctrl Pts',(1.35705080756887,1.62038255289491E-15,
-8.075));
#358898=CARTESIAN_POINT('Ctrl Pts',(1.01778810567665,0.587620236790415,
-8.03333333333333));
#358899=CARTESIAN_POINT('Ctrl Pts',(0.678525403784435,1.17524047358083,
-7.99166666666667));
#358900=CARTESIAN_POINT('Ctrl Pts',(0.,1.17524047358083,-7.95));
#358901=CARTESIAN_POINT('Ctrl Pts',(-0.678525403784434,1.17524047358083,
-7.90833333333333));
#358902=CARTESIAN_POINT('Ctrl Pts',(-1.01778810567665,0.587620236790416,
-7.86666666666667));
#358903=CARTESIAN_POINT('Ctrl Pts',(-1.35705080756887,1.84349021870225E-15,
-7.825));
#358904=CARTESIAN_POINT('Ctrl Pts',(-1.01778810567665,-0.587620236790412,
-7.78333333333333));
#358905=CARTESIAN_POINT('Ctrl Pts',(-0.678525403784435,-1.17524047358083,
-7.74166666666667));
#358906=CARTESIAN_POINT('Ctrl Pts',(-1.43925448419918E-16,-1.17524047358083,
-7.7));
#358907=CARTESIAN_POINT('Ctrl Pts',(-1.43925448419918E-16,-1.17524047358083,
-8.1375));
#358908=CARTESIAN_POINT('Ctrl Pts',(0.678525403784434,-1.17524047358083,
-8.09583333333333));
#358909=CARTESIAN_POINT('Ctrl Pts',(1.01778810567665,-0.587620236790413,
-8.05416666666667));
#358910=CARTESIAN_POINT('Ctrl Pts',(1.35705080756887,1.59306407295827E-15,
-8.0125));
#358911=CARTESIAN_POINT('Ctrl Pts',(1.01778810567665,0.587620236790415,
-7.97083333333334));
#358912=CARTESIAN_POINT('Ctrl Pts',(0.678525403784435,1.17524047358083,
-7.92916666666667));
#358913=CARTESIAN_POINT('Ctrl Pts',(0.,1.17524047358083,-7.8875));
#358914=CARTESIAN_POINT('Ctrl Pts',(-0.678525403784434,1.17524047358083,
-7.84583333333333));
#358915=CARTESIAN_POINT('Ctrl Pts',(-1.01778810567665,0.587620236790416,
-7.80416666666667));
#358916=CARTESIAN_POINT('Ctrl Pts',(-1.35705080756887,1.8161717387656E-15,
-7.7625));
#358917=CARTESIAN_POINT('Ctrl Pts',(-1.01778810567665,-0.587620236790412,
-7.72083333333334));
#358918=CARTESIAN_POINT('Ctrl Pts',(-0.678525403784435,-1.17524047358083,
-7.67916666666667));
#358919=CARTESIAN_POINT('Ctrl Pts',(-1.43925448419918E-16,-1.17524047358083,
-7.6375));
#358920=CARTESIAN_POINT('Origin',(-1.38777878078146E-16,-5.55111512312578E-15,
-17.91875));
#358921=CARTESIAN_POINT('',(1.42394762919424E-14,-1.17524047358083,-8.7));
#358922=CARTESIAN_POINT('',(1.43379317469826E-14,-1.17524047358083,-8.6375));
#358923=CARTESIAN_POINT('',(-4.21481204576211E-16,-1.17524047358085,-17.91875));
#358924=CARTESIAN_POINT('Ctrl Pts',(-1.43925448419918E-16,-1.17524047358083,
-8.7));
#358925=CARTESIAN_POINT('Ctrl Pts',(0.678525403784434,-1.17524047358083,
-8.65833333333333));
#358926=CARTESIAN_POINT('Ctrl Pts',(1.01778810567665,-0.587620236790413,
-8.61666666666667));
#358927=CARTESIAN_POINT('Ctrl Pts',(1.35705080756887,1.83893039238805E-15,
-8.575));
#358928=CARTESIAN_POINT('Ctrl Pts',(1.01778810567665,0.587620236790415,
-8.53333333333333));
#358929=CARTESIAN_POINT('Ctrl Pts',(0.678525403784435,1.17524047358083,
-8.49166666666667));
#358930=CARTESIAN_POINT('Ctrl Pts',(0.,1.17524047358083,-8.45));
#358931=CARTESIAN_POINT('Ctrl Pts',(-0.678525403784434,1.17524047358083,
-8.40833333333333));
#358932=CARTESIAN_POINT('Ctrl Pts',(-1.01778810567665,0.587620236790416,
-8.36666666666667));
#358933=CARTESIAN_POINT('Ctrl Pts',(-1.35705080756887,2.06203805819539E-15,
-8.325));
#358934=CARTESIAN_POINT('Ctrl Pts',(-1.01778810567665,-0.587620236790412,
-8.28333333333333));
#358935=CARTESIAN_POINT('Ctrl Pts',(-0.678525403784435,-1.17524047358083,
-8.24166666666667));
#358936=CARTESIAN_POINT('Ctrl Pts',(-1.43925448419918E-16,-1.17524047358083,
-8.2));
#358937=CARTESIAN_POINT('Ctrl Pts',(-1.43925448419918E-16,-1.17524047358083,
-8.6375));
#358938=CARTESIAN_POINT('Ctrl Pts',(0.678525403784434,-1.17524047358083,
-8.59583333333333));
#358939=CARTESIAN_POINT('Ctrl Pts',(1.01778810567665,-0.587620236790413,
-8.55416666666667));
#358940=CARTESIAN_POINT('Ctrl Pts',(1.35705080756887,1.81161191245141E-15,
-8.5125));
#358941=CARTESIAN_POINT('Ctrl Pts',(1.01778810567665,0.587620236790415,
-8.47083333333333));
#358942=CARTESIAN_POINT('Ctrl Pts',(0.678525403784435,1.17524047358083,
-8.42916666666667));
#358943=CARTESIAN_POINT('Ctrl Pts',(0.,1.17524047358083,-8.3875));
#358944=CARTESIAN_POINT('Ctrl Pts',(-0.678525403784434,1.17524047358083,
-8.34583333333333));
#358945=CARTESIAN_POINT('Ctrl Pts',(-1.01778810567665,0.587620236790416,
-8.30416666666667));
#358946=CARTESIAN_POINT('Ctrl Pts',(-1.35705080756887,2.03471957825875E-15,
-8.2625));
#358947=CARTESIAN_POINT('Ctrl Pts',(-1.01778810567665,-0.587620236790412,
-8.22083333333333));
#358948=CARTESIAN_POINT('Ctrl Pts',(-0.678525403784435,-1.17524047358083,
-8.17916666666667));
#358949=CARTESIAN_POINT('Ctrl Pts',(-1.43925448419918E-16,-1.17524047358083,
-8.1375));
#358950=CARTESIAN_POINT('Origin',(-1.38777878078146E-16,-5.55111512312578E-15,
-17.91875));
#358951=CARTESIAN_POINT('',(1.34518326516202E-14,-1.17524047358083,-9.2));
#358952=CARTESIAN_POINT('',(1.35502881066604E-14,-1.17524047358083,-9.1375));
#358953=CARTESIAN_POINT('',(-4.21481204576211E-16,-1.17524047358085,-17.91875));
#358954=CARTESIAN_POINT('Ctrl Pts',(-1.43925448419918E-16,-1.17524047358083,
-9.2));
#358955=CARTESIAN_POINT('Ctrl Pts',(0.678525403784434,-1.17524047358083,
-9.15833333333333));
#358956=CARTESIAN_POINT('Ctrl Pts',(1.01778810567665,-0.587620236790412,
-9.11666666666667));
#358957=CARTESIAN_POINT('Ctrl Pts',(1.35705080756887,2.05747823188119E-15,
-9.075));
#358958=CARTESIAN_POINT('Ctrl Pts',(1.01778810567665,0.587620236790415,
-9.03333333333333));
#358959=CARTESIAN_POINT('Ctrl Pts',(0.678525403784435,1.17524047358083,
-8.99166666666667));
#358960=CARTESIAN_POINT('Ctrl Pts',(0.,1.17524047358083,-8.95));
#358961=CARTESIAN_POINT('Ctrl Pts',(-0.678525403784434,1.17524047358083,
-8.90833333333333));
#358962=CARTESIAN_POINT('Ctrl Pts',(-1.01778810567665,0.587620236790416,
-8.86666666666667));
#358963=CARTESIAN_POINT('Ctrl Pts',(-1.35705080756887,2.28058589768853E-15,
-8.825));
#358964=CARTESIAN_POINT('Ctrl Pts',(-1.01778810567665,-0.587620236790412,
-8.78333333333333));
#358965=CARTESIAN_POINT('Ctrl Pts',(-0.678525403784435,-1.17524047358083,
-8.74166666666667));
#358966=CARTESIAN_POINT('Ctrl Pts',(-1.43925448419918E-16,-1.17524047358083,
-8.7));
#358967=CARTESIAN_POINT('Ctrl Pts',(-1.43925448419918E-16,-1.17524047358083,
-9.1375));
#358968=CARTESIAN_POINT('Ctrl Pts',(0.678525403784434,-1.17524047358083,
-9.09583333333333));
#358969=CARTESIAN_POINT('Ctrl Pts',(1.01778810567665,-0.587620236790412,
-9.05416666666667));
#358970=CARTESIAN_POINT('Ctrl Pts',(1.35705080756887,2.03015975194455E-15,
-9.0125));
#358971=CARTESIAN_POINT('Ctrl Pts',(1.01778810567665,0.587620236790416,
-8.97083333333333));
#358972=CARTESIAN_POINT('Ctrl Pts',(0.678525403784435,1.17524047358083,
-8.92916666666667));
#358973=CARTESIAN_POINT('Ctrl Pts',(0.,1.17524047358083,-8.8875));
#358974=CARTESIAN_POINT('Ctrl Pts',(-0.678525403784434,1.17524047358083,
-8.84583333333333));
#358975=CARTESIAN_POINT('Ctrl Pts',(-1.01778810567665,0.587620236790416,
-8.80416666666667));
#358976=CARTESIAN_POINT('Ctrl Pts',(-1.35705080756887,2.25326741775189E-15,
-8.7625));
#358977=CARTESIAN_POINT('Ctrl Pts',(-1.01778810567665,-0.587620236790412,
-8.72083333333333));
#358978=CARTESIAN_POINT('Ctrl Pts',(-0.678525403784435,-1.17524047358083,
-8.67916666666667));
#358979=CARTESIAN_POINT('Ctrl Pts',(-1.43925448419918E-16,-1.17524047358083,
-8.6375));
#358980=CARTESIAN_POINT('Origin',(-1.38777878078146E-16,-5.55111512312578E-15,
-17.91875));
#358981=CARTESIAN_POINT('',(1.2664189011298E-14,-1.17524047358083,-9.7));
#358982=CARTESIAN_POINT('',(1.27626444663382E-14,-1.17524047358083,-9.6375));
#358983=CARTESIAN_POINT('',(-4.21481204576211E-16,-1.17524047358085,-17.91875));
#358984=CARTESIAN_POINT('Ctrl Pts',(-1.43925448419918E-16,-1.17524047358083,
-9.7));
#358985=CARTESIAN_POINT('Ctrl Pts',(0.678525403784434,-1.17524047358083,
-9.65833333333333));
#358986=CARTESIAN_POINT('Ctrl Pts',(1.01778810567665,-0.587620236790412,
-9.61666666666667));
#358987=CARTESIAN_POINT('Ctrl Pts',(1.35705080756887,2.27602607137433E-15,
-9.575));
#358988=CARTESIAN_POINT('Ctrl Pts',(1.01778810567665,0.587620236790416,
-9.53333333333333));
#358989=CARTESIAN_POINT('Ctrl Pts',(0.678525403784435,1.17524047358083,
-9.49166666666667));
#358990=CARTESIAN_POINT('Ctrl Pts',(0.,1.17524047358083,-9.45));
#358991=CARTESIAN_POINT('Ctrl Pts',(-0.678525403784434,1.17524047358083,
-9.40833333333333));
#358992=CARTESIAN_POINT('Ctrl Pts',(-1.01778810567665,0.587620236790417,
-9.36666666666667));
#358993=CARTESIAN_POINT('Ctrl Pts',(-1.35705080756887,2.49913373718167E-15,
-9.325));
#358994=CARTESIAN_POINT('Ctrl Pts',(-1.01778810567665,-0.587620236790411,
-9.28333333333333));
#358995=CARTESIAN_POINT('Ctrl Pts',(-0.678525403784435,-1.17524047358083,
-9.24166666666667));
#358996=CARTESIAN_POINT('Ctrl Pts',(-1.43925448419918E-16,-1.17524047358083,
-9.2));
#358997=CARTESIAN_POINT('Ctrl Pts',(-1.43925448419918E-16,-1.17524047358083,
-9.6375));
#358998=CARTESIAN_POINT('Ctrl Pts',(0.678525403784434,-1.17524047358083,
-9.59583333333333));
#358999=CARTESIAN_POINT('Ctrl Pts',(1.01778810567665,-0.587620236790412,
-9.55416666666667));
#359000=CARTESIAN_POINT('Ctrl Pts',(1.35705080756887,2.24870759143769E-15,
-9.5125));
#359001=CARTESIAN_POINT('Ctrl Pts',(1.01778810567665,0.587620236790416,
-9.47083333333333));
#359002=CARTESIAN_POINT('Ctrl Pts',(0.678525403784435,1.17524047358083,
-9.42916666666667));
#359003=CARTESIAN_POINT('Ctrl Pts',(0.,1.17524047358083,-9.3875));
#359004=CARTESIAN_POINT('Ctrl Pts',(-0.678525403784434,1.17524047358083,
-9.34583333333333));
#359005=CARTESIAN_POINT('Ctrl Pts',(-1.01778810567665,0.587620236790417,
-9.30416666666667));
#359006=CARTESIAN_POINT('Ctrl Pts',(-1.35705080756887,2.47181525724503E-15,
-9.2625));
#359007=CARTESIAN_POINT('Ctrl Pts',(-1.01778810567665,-0.587620236790412,
-9.22083333333333));
#359008=CARTESIAN_POINT('Ctrl Pts',(-0.678525403784435,-1.17524047358083,
-9.17916666666667));
#359009=CARTESIAN_POINT('Ctrl Pts',(-1.43925448419918E-16,-1.17524047358083,
-9.1375));
#359010=CARTESIAN_POINT('Origin',(-1.38777878078146E-16,-5.55111512312578E-15,
-17.91875));
#359011=CARTESIAN_POINT('',(1.18765453709758E-14,-1.17524047358083,-10.2));
#359012=CARTESIAN_POINT('',(1.19750008260161E-14,-1.17524047358083,-10.1375));
#359013=CARTESIAN_POINT('',(-4.21481204576211E-16,-1.17524047358085,-17.91875));
#359014=CARTESIAN_POINT('Ctrl Pts',(-1.43925448419918E-16,-1.17524047358083,
-10.2));
#359015=CARTESIAN_POINT('Ctrl Pts',(0.678525403784434,-1.17524047358083,
-10.1583333333333));
#359016=CARTESIAN_POINT('Ctrl Pts',(1.01778810567665,-0.587620236790412,
-10.1166666666667));
#359017=CARTESIAN_POINT('Ctrl Pts',(1.35705080756887,2.49457391086747E-15,
-10.075));
#359018=CARTESIAN_POINT('Ctrl Pts',(1.01778810567665,0.587620236790416,
-10.0333333333333));
#359019=CARTESIAN_POINT('Ctrl Pts',(0.678525403784435,1.17524047358083,
-9.99166666666667));
#359020=CARTESIAN_POINT('Ctrl Pts',(0.,1.17524047358083,-9.95));
#359021=CARTESIAN_POINT('Ctrl Pts',(-0.678525403784434,1.17524047358083,
-9.90833333333333));
#359022=CARTESIAN_POINT('Ctrl Pts',(-1.01778810567665,0.587620236790417,
-9.86666666666667));
#359023=CARTESIAN_POINT('Ctrl Pts',(-1.35705080756887,2.71768157667481E-15,
-9.825));
#359024=CARTESIAN_POINT('Ctrl Pts',(-1.01778810567665,-0.587620236790411,
-9.78333333333333));
#359025=CARTESIAN_POINT('Ctrl Pts',(-0.678525403784435,-1.17524047358083,
-9.74166666666667));
#359026=CARTESIAN_POINT('Ctrl Pts',(-1.43925448419918E-16,-1.17524047358083,
-9.7));
#359027=CARTESIAN_POINT('Ctrl Pts',(-1.43925448419918E-16,-1.17524047358083,
-10.1375));
#359028=CARTESIAN_POINT('Ctrl Pts',(0.678525403784434,-1.17524047358083,
-10.0958333333333));
#359029=CARTESIAN_POINT('Ctrl Pts',(1.01778810567665,-0.587620236790412,
-10.0541666666667));
#359030=CARTESIAN_POINT('Ctrl Pts',(1.35705080756887,2.46725543093083E-15,
-10.0125));
#359031=CARTESIAN_POINT('Ctrl Pts',(1.01778810567665,0.587620236790416,
-9.97083333333333));
#359032=CARTESIAN_POINT('Ctrl Pts',(0.678525403784435,1.17524047358083,
-9.92916666666667));
#359033=CARTESIAN_POINT('Ctrl Pts',(0.,1.17524047358083,-9.8875));
#359034=CARTESIAN_POINT('Ctrl Pts',(-0.678525403784434,1.17524047358083,
-9.84583333333333));
#359035=CARTESIAN_POINT('Ctrl Pts',(-1.01778810567665,0.587620236790417,
-9.80416666666667));
#359036=CARTESIAN_POINT('Ctrl Pts',(-1.35705080756887,2.69036309673817E-15,
-9.7625));
#359037=CARTESIAN_POINT('Ctrl Pts',(-1.01778810567665,-0.587620236790411,
-9.72083333333333));
#359038=CARTESIAN_POINT('Ctrl Pts',(-0.678525403784435,-1.17524047358083,
-9.67916666666667));
#359039=CARTESIAN_POINT('Ctrl Pts',(-1.43925448419918E-16,-1.17524047358083,
-9.6375));
#359040=CARTESIAN_POINT('Origin',(-1.38777878078146E-16,-5.55111512312578E-15,
-17.91875));
#359041=CARTESIAN_POINT('',(1.10889017306536E-14,-1.17524047358083,-10.7));
#359042=CARTESIAN_POINT('',(1.11873571856939E-14,-1.17524047358083,-10.6375));
#359043=CARTESIAN_POINT('',(-4.21481204576211E-16,-1.17524047358085,-17.91875));
#359044=CARTESIAN_POINT('Ctrl Pts',(-1.43925448419918E-16,-1.17524047358083,
-10.7));
#359045=CARTESIAN_POINT('Ctrl Pts',(0.678525403784434,-1.17524047358083,
-10.6583333333333));
#359046=CARTESIAN_POINT('Ctrl Pts',(1.01778810567665,-0.587620236790412,
-10.6166666666667));
#359047=CARTESIAN_POINT('Ctrl Pts',(1.35705080756887,2.71312175036061E-15,
-10.575));
#359048=CARTESIAN_POINT('Ctrl Pts',(1.01778810567665,0.587620236790416,
-10.5333333333333));
#359049=CARTESIAN_POINT('Ctrl Pts',(0.678525403784435,1.17524047358083,
-10.4916666666667));
#359050=CARTESIAN_POINT('Ctrl Pts',(0.,1.17524047358083,-10.45));
#359051=CARTESIAN_POINT('Ctrl Pts',(-0.678525403784434,1.17524047358083,
-10.4083333333333));
#359052=CARTESIAN_POINT('Ctrl Pts',(-1.01778810567665,0.587620236790417,
-10.3666666666667));
#359053=CARTESIAN_POINT('Ctrl Pts',(-1.35705080756887,2.93622941616795E-15,
-10.325));
#359054=CARTESIAN_POINT('Ctrl Pts',(-1.01778810567665,-0.587620236790411,
-10.2833333333333));
#359055=CARTESIAN_POINT('Ctrl Pts',(-0.678525403784435,-1.17524047358083,
-10.2416666666667));
#359056=CARTESIAN_POINT('Ctrl Pts',(-1.43925448419918E-16,-1.17524047358083,
-10.2));
#359057=CARTESIAN_POINT('Ctrl Pts',(-1.43925448419918E-16,-1.17524047358083,
-10.6375));
#359058=CARTESIAN_POINT('Ctrl Pts',(0.678525403784434,-1.17524047358083,
-10.5958333333333));
#359059=CARTESIAN_POINT('Ctrl Pts',(1.01778810567665,-0.587620236790412,
-10.5541666666667));
#359060=CARTESIAN_POINT('Ctrl Pts',(1.35705080756887,2.68580327042397E-15,
-10.5125));
#359061=CARTESIAN_POINT('Ctrl Pts',(1.01778810567665,0.587620236790416,
-10.4708333333333));
#359062=CARTESIAN_POINT('Ctrl Pts',(0.678525403784435,1.17524047358083,
-10.4291666666667));
#359063=CARTESIAN_POINT('Ctrl Pts',(0.,1.17524047358083,-10.3875));
#359064=CARTESIAN_POINT('Ctrl Pts',(-0.678525403784434,1.17524047358083,
-10.3458333333333));
#359065=CARTESIAN_POINT('Ctrl Pts',(-1.01778810567665,0.587620236790417,
-10.3041666666667));
#359066=CARTESIAN_POINT('Ctrl Pts',(-1.35705080756887,2.90891093623131E-15,
-10.2625));
#359067=CARTESIAN_POINT('Ctrl Pts',(-1.01778810567665,-0.587620236790411,
-10.2208333333333));
#359068=CARTESIAN_POINT('Ctrl Pts',(-0.678525403784435,-1.17524047358083,
-10.1791666666667));
#359069=CARTESIAN_POINT('Ctrl Pts',(-1.43925448419918E-16,-1.17524047358083,
-10.1375));
#359070=CARTESIAN_POINT('Origin',(-1.38777878078146E-16,-5.55111512312578E-15,
-17.91875));
#359071=CARTESIAN_POINT('',(1.03012580903314E-14,-1.17524047358082,-11.2));
#359072=CARTESIAN_POINT('',(1.03997135453717E-14,-1.17524047358083,-11.1375));
#359073=CARTESIAN_POINT('',(-4.21481204576211E-16,-1.17524047358085,-17.91875));
#359074=CARTESIAN_POINT('Ctrl Pts',(-1.43925448419918E-16,-1.17524047358082,
-11.2));
#359075=CARTESIAN_POINT('Ctrl Pts',(0.678525403784434,-1.17524047358083,
-11.1583333333333));
#359076=CARTESIAN_POINT('Ctrl Pts',(1.01778810567665,-0.587620236790411,
-11.1166666666667));
#359077=CARTESIAN_POINT('Ctrl Pts',(1.35705080756887,2.93166958985376E-15,
-11.075));
#359078=CARTESIAN_POINT('Ctrl Pts',(1.01778810567665,0.587620236790416,
-11.0333333333333));
#359079=CARTESIAN_POINT('Ctrl Pts',(0.678525403784435,1.17524047358083,
-10.9916666666667));
#359080=CARTESIAN_POINT('Ctrl Pts',(0.,1.17524047358083,-10.95));
#359081=CARTESIAN_POINT('Ctrl Pts',(-0.678525403784434,1.17524047358083,
-10.9083333333333));
#359082=CARTESIAN_POINT('Ctrl Pts',(-1.01778810567665,0.587620236790417,
-10.8666666666667));
#359083=CARTESIAN_POINT('Ctrl Pts',(-1.35705080756887,3.15477725566109E-15,
-10.825));
#359084=CARTESIAN_POINT('Ctrl Pts',(-1.01778810567665,-0.587620236790411,
-10.7833333333333));
#359085=CARTESIAN_POINT('Ctrl Pts',(-0.678525403784435,-1.17524047358083,
-10.7416666666667));
#359086=CARTESIAN_POINT('Ctrl Pts',(-1.43925448419918E-16,-1.17524047358083,
-10.7));
#359087=CARTESIAN_POINT('Ctrl Pts',(-1.43925448419918E-16,-1.17524047358083,
-11.1375));
#359088=CARTESIAN_POINT('Ctrl Pts',(0.678525403784434,-1.17524047358083,
-11.0958333333333));
#359089=CARTESIAN_POINT('Ctrl Pts',(1.01778810567665,-0.587620236790412,
-11.0541666666667));
#359090=CARTESIAN_POINT('Ctrl Pts',(1.35705080756887,2.90435110991711E-15,
-11.0125));
#359091=CARTESIAN_POINT('Ctrl Pts',(1.01778810567665,0.587620236790416,
-10.9708333333333));
#359092=CARTESIAN_POINT('Ctrl Pts',(0.678525403784435,1.17524047358083,
-10.9291666666667));
#359093=CARTESIAN_POINT('Ctrl Pts',(0.,1.17524047358083,-10.8875));
#359094=CARTESIAN_POINT('Ctrl Pts',(-0.678525403784434,1.17524047358083,
-10.8458333333333));
#359095=CARTESIAN_POINT('Ctrl Pts',(-1.01778810567665,0.587620236790417,
-10.8041666666667));
#359096=CARTESIAN_POINT('Ctrl Pts',(-1.35705080756887,3.12745877572445E-15,
-10.7625));
#359097=CARTESIAN_POINT('Ctrl Pts',(-1.01778810567665,-0.587620236790411,
-10.7208333333333));
#359098=CARTESIAN_POINT('Ctrl Pts',(-0.678525403784435,-1.17524047358083,
-10.6791666666667));
#359099=CARTESIAN_POINT('Ctrl Pts',(-1.43925448419918E-16,-1.17524047358083,
-10.6375));
#359100=CARTESIAN_POINT('Origin',(-1.38777878078146E-16,-5.55111512312578E-15,
-17.91875));
#359101=CARTESIAN_POINT('',(9.5136144500092E-15,-1.17524047358082,-11.7));
#359102=CARTESIAN_POINT('',(9.61206990504947E-15,-1.17524047358083,-11.6375));
#359103=CARTESIAN_POINT('',(-4.21481204576211E-16,-1.17524047358085,-17.91875));
#359104=CARTESIAN_POINT('Ctrl Pts',(-1.43925448419918E-16,-1.17524047358082,
-11.7));
#359105=CARTESIAN_POINT('Ctrl Pts',(0.678525403784434,-1.17524047358083,
-11.6583333333333));
#359106=CARTESIAN_POINT('Ctrl Pts',(1.01778810567665,-0.587620236790411,
-11.6166666666667));
#359107=CARTESIAN_POINT('Ctrl Pts',(1.35705080756887,3.1502174293469E-15,
-11.575));
#359108=CARTESIAN_POINT('Ctrl Pts',(1.01778810567665,0.587620236790417,
-11.5333333333333));
#359109=CARTESIAN_POINT('Ctrl Pts',(0.678525403784435,1.17524047358083,
-11.4916666666667));
#359110=CARTESIAN_POINT('Ctrl Pts',(0.,1.17524047358083,-11.45));
#359111=CARTESIAN_POINT('Ctrl Pts',(-0.678525403784434,1.17524047358083,
-11.4083333333333));
#359112=CARTESIAN_POINT('Ctrl Pts',(-1.01778810567665,0.587620236790417,
-11.3666666666667));
#359113=CARTESIAN_POINT('Ctrl Pts',(-1.35705080756887,3.37332509515423E-15,
-11.325));
#359114=CARTESIAN_POINT('Ctrl Pts',(-1.01778810567665,-0.587620236790411,
-11.2833333333333));
#359115=CARTESIAN_POINT('Ctrl Pts',(-0.678525403784435,-1.17524047358082,
-11.2416666666667));
#359116=CARTESIAN_POINT('Ctrl Pts',(-1.43925448419918E-16,-1.17524047358082,
-11.2));
#359117=CARTESIAN_POINT('Ctrl Pts',(-1.43925448419918E-16,-1.17524047358083,
-11.6375));
#359118=CARTESIAN_POINT('Ctrl Pts',(0.678525403784434,-1.17524047358083,
-11.5958333333333));
#359119=CARTESIAN_POINT('Ctrl Pts',(1.01778810567665,-0.587620236790411,
-11.5541666666667));
#359120=CARTESIAN_POINT('Ctrl Pts',(1.35705080756887,3.12289894941025E-15,
-11.5125));
#359121=CARTESIAN_POINT('Ctrl Pts',(1.01778810567665,0.587620236790417,
-11.4708333333333));
#359122=CARTESIAN_POINT('Ctrl Pts',(0.678525403784435,1.17524047358083,
-11.4291666666667));
#359123=CARTESIAN_POINT('Ctrl Pts',(0.,1.17524047358083,-11.3875));
#359124=CARTESIAN_POINT('Ctrl Pts',(-0.678525403784434,1.17524047358083,
-11.3458333333333));
#359125=CARTESIAN_POINT('Ctrl Pts',(-1.01778810567665,0.587620236790418,
-11.3041666666667));
#359126=CARTESIAN_POINT('Ctrl Pts',(-1.35705080756887,3.34600661521759E-15,
-11.2625));
#359127=CARTESIAN_POINT('Ctrl Pts',(-1.01778810567665,-0.587620236790411,
-11.2208333333333));
#359128=CARTESIAN_POINT('Ctrl Pts',(-0.678525403784435,-1.17524047358083,
-11.1791666666667));
#359129=CARTESIAN_POINT('Ctrl Pts',(-1.43925448419918E-16,-1.17524047358083,
-11.1375));
#359130=CARTESIAN_POINT('Origin',(-1.38777878078146E-16,-5.55111512312578E-15,
-17.91875));
#359131=CARTESIAN_POINT('',(8.72597080968701E-15,-1.17524047358082,-12.2));
#359132=CARTESIAN_POINT('',(8.82442626472729E-15,-1.17524047358082,-12.1375));
#359133=CARTESIAN_POINT('',(-4.21481204576211E-16,-1.17524047358085,-17.91875));
#359134=CARTESIAN_POINT('Ctrl Pts',(-1.43925448419918E-16,-1.17524047358082,
-12.2));
#359135=CARTESIAN_POINT('Ctrl Pts',(0.678525403784434,-1.17524047358082,
-12.1583333333333));
#359136=CARTESIAN_POINT('Ctrl Pts',(1.01778810567665,-0.587620236790411,
-12.1166666666667));
#359137=CARTESIAN_POINT('Ctrl Pts',(1.35705080756887,3.36876526884004E-15,
-12.075));
#359138=CARTESIAN_POINT('Ctrl Pts',(1.01778810567665,0.587620236790417,
-12.0333333333333));
#359139=CARTESIAN_POINT('Ctrl Pts',(0.678525403784435,1.17524047358083,
-11.9916666666667));
#359140=CARTESIAN_POINT('Ctrl Pts',(0.,1.17524047358083,-11.95));
#359141=CARTESIAN_POINT('Ctrl Pts',(-0.678525403784434,1.17524047358083,
-11.9083333333333));
#359142=CARTESIAN_POINT('Ctrl Pts',(-1.01778810567665,0.587620236790418,
-11.8666666666667));
#359143=CARTESIAN_POINT('Ctrl Pts',(-1.35705080756887,3.59187293464738E-15,
-11.825));
#359144=CARTESIAN_POINT('Ctrl Pts',(-1.01778810567665,-0.58762023679041,
-11.7833333333333));
#359145=CARTESIAN_POINT('Ctrl Pts',(-0.678525403784435,-1.17524047358082,
-11.7416666666667));
#359146=CARTESIAN_POINT('Ctrl Pts',(-1.43925448419918E-16,-1.17524047358082,
-11.7));
#359147=CARTESIAN_POINT('Ctrl Pts',(-1.43925448419918E-16,-1.17524047358082,
-12.1375));
#359148=CARTESIAN_POINT('Ctrl Pts',(0.678525403784434,-1.17524047358083,
-12.0958333333333));
#359149=CARTESIAN_POINT('Ctrl Pts',(1.01778810567665,-0.587620236790411,
-12.0541666666667));
#359150=CARTESIAN_POINT('Ctrl Pts',(1.35705080756887,3.34144678890339E-15,
-12.0125));
#359151=CARTESIAN_POINT('Ctrl Pts',(1.01778810567665,0.587620236790417,
-11.9708333333333));
#359152=CARTESIAN_POINT('Ctrl Pts',(0.678525403784435,1.17524047358083,
-11.9291666666667));
#359153=CARTESIAN_POINT('Ctrl Pts',(0.,1.17524047358083,-11.8875));
#359154=CARTESIAN_POINT('Ctrl Pts',(-0.678525403784434,1.17524047358083,
-11.8458333333333));
#359155=CARTESIAN_POINT('Ctrl Pts',(-1.01778810567665,0.587620236790418,
-11.8041666666667));
#359156=CARTESIAN_POINT('Ctrl Pts',(-1.35705080756887,3.56455445471073E-15,
-11.7625));
#359157=CARTESIAN_POINT('Ctrl Pts',(-1.01778810567665,-0.587620236790411,
-11.7208333333333));
#359158=CARTESIAN_POINT('Ctrl Pts',(-0.678525403784435,-1.17524047358083,
-11.6791666666667));
#359159=CARTESIAN_POINT('Ctrl Pts',(-1.43925448419918E-16,-1.17524047358083,
-11.6375));
#359160=CARTESIAN_POINT('Origin',(-1.38777878078146E-16,-5.55111512312578E-15,
-17.91875));
#359161=CARTESIAN_POINT('',(7.93832716936482E-15,-1.17524047358082,-12.7));
#359162=CARTESIAN_POINT('',(8.03678262440509E-15,-1.17524047358082,-12.6375));
#359163=CARTESIAN_POINT('',(-4.21481204576211E-16,-1.17524047358085,-17.91875));
#359164=CARTESIAN_POINT('Ctrl Pts',(-1.43925448419918E-16,-1.17524047358082,
-12.7));
#359165=CARTESIAN_POINT('Ctrl Pts',(0.678525403784434,-1.17524047358082,
-12.6583333333333));
#359166=CARTESIAN_POINT('Ctrl Pts',(1.01778810567665,-0.587620236790411,
-12.6166666666667));
#359167=CARTESIAN_POINT('Ctrl Pts',(1.35705080756887,3.58731310833318E-15,
-12.575));
#359168=CARTESIAN_POINT('Ctrl Pts',(1.01778810567665,0.587620236790417,
-12.5333333333333));
#359169=CARTESIAN_POINT('Ctrl Pts',(0.678525403784435,1.17524047358083,
-12.4916666666667));
#359170=CARTESIAN_POINT('Ctrl Pts',(0.,1.17524047358083,-12.45));
#359171=CARTESIAN_POINT('Ctrl Pts',(-0.678525403784434,1.17524047358083,
-12.4083333333333));
#359172=CARTESIAN_POINT('Ctrl Pts',(-1.01778810567665,0.587620236790418,
-12.3666666666667));
#359173=CARTESIAN_POINT('Ctrl Pts',(-1.35705080756887,3.81042077414052E-15,
-12.325));
#359174=CARTESIAN_POINT('Ctrl Pts',(-1.01778810567665,-0.58762023679041,
-12.2833333333333));
#359175=CARTESIAN_POINT('Ctrl Pts',(-0.678525403784435,-1.17524047358082,
-12.2416666666667));
#359176=CARTESIAN_POINT('Ctrl Pts',(-1.43925448419918E-16,-1.17524047358082,
-12.2));
#359177=CARTESIAN_POINT('Ctrl Pts',(-1.43925448419918E-16,-1.17524047358082,
-12.6375));
#359178=CARTESIAN_POINT('Ctrl Pts',(0.678525403784434,-1.17524047358083,
-12.5958333333333));
#359179=CARTESIAN_POINT('Ctrl Pts',(1.01778810567665,-0.587620236790411,
-12.5541666666667));
#359180=CARTESIAN_POINT('Ctrl Pts',(1.35705080756887,3.55999462839654E-15,
-12.5125));
#359181=CARTESIAN_POINT('Ctrl Pts',(1.01778810567665,0.587620236790417,
-12.4708333333333));
#359182=CARTESIAN_POINT('Ctrl Pts',(0.678525403784435,1.17524047358083,
-12.4291666666667));
#359183=CARTESIAN_POINT('Ctrl Pts',(0.,1.17524047358083,-12.3875));
#359184=CARTESIAN_POINT('Ctrl Pts',(-0.678525403784434,1.17524047358083,
-12.3458333333333));
#359185=CARTESIAN_POINT('Ctrl Pts',(-1.01778810567665,0.587620236790418,
-12.3041666666667));
#359186=CARTESIAN_POINT('Ctrl Pts',(-1.35705080756887,3.78310229420388E-15,
-12.2625));
#359187=CARTESIAN_POINT('Ctrl Pts',(-1.01778810567665,-0.58762023679041,
-12.2208333333333));
#359188=CARTESIAN_POINT('Ctrl Pts',(-0.678525403784435,-1.17524047358082,
-12.1791666666667));
#359189=CARTESIAN_POINT('Ctrl Pts',(-1.43925448419918E-16,-1.17524047358082,
-12.1375));
#359190=CARTESIAN_POINT('Origin',(-1.38777878078146E-16,-5.55111512312578E-15,
-17.91875));
#359191=CARTESIAN_POINT('',(7.15068352904263E-15,-1.17524047358082,-13.2));
#359192=CARTESIAN_POINT('',(7.2491389840829E-15,-1.17524047358082,-13.1375));
#359193=CARTESIAN_POINT('',(-4.21481204576211E-16,-1.17524047358085,-17.91875));
#359194=CARTESIAN_POINT('Ctrl Pts',(-1.43925448419918E-16,-1.17524047358082,
-13.2));
#359195=CARTESIAN_POINT('Ctrl Pts',(0.678525403784434,-1.17524047358082,
-13.1583333333333));
#359196=CARTESIAN_POINT('Ctrl Pts',(1.01778810567665,-0.587620236790411,
-13.1166666666667));
#359197=CARTESIAN_POINT('Ctrl Pts',(1.35705080756887,3.80586094782632E-15,
-13.075));
#359198=CARTESIAN_POINT('Ctrl Pts',(1.01778810567665,0.587620236790417,
-13.0333333333333));
#359199=CARTESIAN_POINT('Ctrl Pts',(0.678525403784435,1.17524047358083,
-12.9916666666667));
#359200=CARTESIAN_POINT('Ctrl Pts',(0.,1.17524047358083,-12.95));
#359201=CARTESIAN_POINT('Ctrl Pts',(-0.678525403784434,1.17524047358083,
-12.9083333333333));
#359202=CARTESIAN_POINT('Ctrl Pts',(-1.01778810567665,0.587620236790418,
-12.8666666666667));
#359203=CARTESIAN_POINT('Ctrl Pts',(-1.35705080756887,4.02896861363366E-15,
-12.825));
#359204=CARTESIAN_POINT('Ctrl Pts',(-1.01778810567665,-0.58762023679041,
-12.7833333333333));
#359205=CARTESIAN_POINT('Ctrl Pts',(-0.678525403784435,-1.17524047358082,
-12.7416666666667));
#359206=CARTESIAN_POINT('Ctrl Pts',(-1.43925448419918E-16,-1.17524047358082,
-12.7));
#359207=CARTESIAN_POINT('Ctrl Pts',(-1.43925448419918E-16,-1.17524047358082,
-13.1375));
#359208=CARTESIAN_POINT('Ctrl Pts',(0.678525403784434,-1.17524047358082,
-13.0958333333333));
#359209=CARTESIAN_POINT('Ctrl Pts',(1.01778810567665,-0.587620236790411,
-13.0541666666667));
#359210=CARTESIAN_POINT('Ctrl Pts',(1.35705080756887,3.77854246788968E-15,
-13.0125));
#359211=CARTESIAN_POINT('Ctrl Pts',(1.01778810567665,0.587620236790417,
-12.9708333333333));
#359212=CARTESIAN_POINT('Ctrl Pts',(0.678525403784435,1.17524047358083,
-12.9291666666667));
#359213=CARTESIAN_POINT('Ctrl Pts',(0.,1.17524047358083,-12.8875));
#359214=CARTESIAN_POINT('Ctrl Pts',(-0.678525403784434,1.17524047358083,
-12.8458333333333));
#359215=CARTESIAN_POINT('Ctrl Pts',(-1.01778810567665,0.587620236790418,
-12.8041666666667));
#359216=CARTESIAN_POINT('Ctrl Pts',(-1.35705080756887,4.00165013369702E-15,
-12.7625));
#359217=CARTESIAN_POINT('Ctrl Pts',(-1.01778810567665,-0.58762023679041,
-12.7208333333333));
#359218=CARTESIAN_POINT('Ctrl Pts',(-0.678525403784435,-1.17524047358082,
-12.6791666666667));
#359219=CARTESIAN_POINT('Ctrl Pts',(-1.43925448419918E-16,-1.17524047358082,
-12.6375));
#359220=CARTESIAN_POINT('Origin',(-1.38777878078146E-16,-5.55111512312578E-15,
-17.91875));
#359221=CARTESIAN_POINT('',(6.36303988872043E-15,-1.17524047358082,-13.7));
#359222=CARTESIAN_POINT('',(6.46149534376071E-15,-1.17524047358082,-13.6375));
#359223=CARTESIAN_POINT('',(-4.21481204576211E-16,-1.17524047358085,-17.91875));
#359224=CARTESIAN_POINT('Ctrl Pts',(-1.43925448419918E-16,-1.17524047358082,
-13.7));
#359225=CARTESIAN_POINT('Ctrl Pts',(0.678525403784434,-1.17524047358082,
-13.6583333333333));
#359226=CARTESIAN_POINT('Ctrl Pts',(1.01778810567665,-0.58762023679041,
-13.6166666666667));
#359227=CARTESIAN_POINT('Ctrl Pts',(1.35705080756887,4.02440878731946E-15,
-13.575));
#359228=CARTESIAN_POINT('Ctrl Pts',(1.01778810567665,0.587620236790417,
-13.5333333333333));
#359229=CARTESIAN_POINT('Ctrl Pts',(0.678525403784435,1.17524047358083,
-13.4916666666667));
#359230=CARTESIAN_POINT('Ctrl Pts',(0.,1.17524047358083,-13.45));
#359231=CARTESIAN_POINT('Ctrl Pts',(-0.678525403784434,1.17524047358083,
-13.4083333333333));
#359232=CARTESIAN_POINT('Ctrl Pts',(-1.01778810567665,0.587620236790418,
-13.3666666666667));
#359233=CARTESIAN_POINT('Ctrl Pts',(-1.35705080756887,4.2475164531268E-15,
-13.325));
#359234=CARTESIAN_POINT('Ctrl Pts',(-1.01778810567665,-0.58762023679041,
-13.2833333333333));
#359235=CARTESIAN_POINT('Ctrl Pts',(-0.678525403784435,-1.17524047358082,
-13.2416666666667));
#359236=CARTESIAN_POINT('Ctrl Pts',(-1.43925448419918E-16,-1.17524047358082,
-13.2));
#359237=CARTESIAN_POINT('Ctrl Pts',(-1.43925448419918E-16,-1.17524047358082,
-13.6375));
#359238=CARTESIAN_POINT('Ctrl Pts',(0.678525403784434,-1.17524047358082,
-13.5958333333333));
#359239=CARTESIAN_POINT('Ctrl Pts',(1.01778810567665,-0.58762023679041,
-13.5541666666667));
#359240=CARTESIAN_POINT('Ctrl Pts',(1.35705080756887,3.99709030738282E-15,
-13.5125));
#359241=CARTESIAN_POINT('Ctrl Pts',(1.01778810567665,0.587620236790418,
-13.4708333333333));
#359242=CARTESIAN_POINT('Ctrl Pts',(0.678525403784435,1.17524047358083,
-13.4291666666667));
#359243=CARTESIAN_POINT('Ctrl Pts',(0.,1.17524047358083,-13.3875));
#359244=CARTESIAN_POINT('Ctrl Pts',(-0.678525403784434,1.17524047358083,
-13.3458333333333));
#359245=CARTESIAN_POINT('Ctrl Pts',(-1.01778810567665,0.587620236790419,
-13.3041666666667));
#359246=CARTESIAN_POINT('Ctrl Pts',(-1.35705080756887,4.22019797319016E-15,
-13.2625));
#359247=CARTESIAN_POINT('Ctrl Pts',(-1.01778810567665,-0.58762023679041,
-13.2208333333333));
#359248=CARTESIAN_POINT('Ctrl Pts',(-0.678525403784435,-1.17524047358082,
-13.1791666666667));
#359249=CARTESIAN_POINT('Ctrl Pts',(-1.43925448419918E-16,-1.17524047358082,
-13.1375));
#359250=CARTESIAN_POINT('Origin',(-1.38777878078146E-16,-5.55111512312578E-15,
-17.91875));
#359251=CARTESIAN_POINT('',(5.57539624839824E-15,-1.17524047358082,-14.2));
#359252=CARTESIAN_POINT('',(5.67385170343851E-15,-1.17524047358082,-14.1375));
#359253=CARTESIAN_POINT('',(-4.21481204576211E-16,-1.17524047358085,-17.91875));
#359254=CARTESIAN_POINT('Ctrl Pts',(-1.43925448419918E-16,-1.17524047358082,
-14.2));
#359255=CARTESIAN_POINT('Ctrl Pts',(0.678525403784434,-1.17524047358082,
-14.1583333333333));
#359256=CARTESIAN_POINT('Ctrl Pts',(1.01778810567665,-0.58762023679041,
-14.1166666666667));
#359257=CARTESIAN_POINT('Ctrl Pts',(1.35705080756887,4.2429566268126E-15,
-14.075));
#359258=CARTESIAN_POINT('Ctrl Pts',(1.01778810567665,0.587620236790418,
-14.0333333333333));
#359259=CARTESIAN_POINT('Ctrl Pts',(0.678525403784435,1.17524047358083,
-13.9916666666667));
#359260=CARTESIAN_POINT('Ctrl Pts',(0.,1.17524047358083,-13.95));
#359261=CARTESIAN_POINT('Ctrl Pts',(-0.678525403784434,1.17524047358083,
-13.9083333333333));
#359262=CARTESIAN_POINT('Ctrl Pts',(-1.01778810567665,0.587620236790419,
-13.8666666666667));
#359263=CARTESIAN_POINT('Ctrl Pts',(-1.35705080756887,4.46606429261994E-15,
-13.825));
#359264=CARTESIAN_POINT('Ctrl Pts',(-1.01778810567665,-0.58762023679041,
-13.7833333333333));
#359265=CARTESIAN_POINT('Ctrl Pts',(-0.678525403784435,-1.17524047358082,
-13.7416666666667));
#359266=CARTESIAN_POINT('Ctrl Pts',(-1.43925448419918E-16,-1.17524047358082,
-13.7));
#359267=CARTESIAN_POINT('Ctrl Pts',(-1.43925448419918E-16,-1.17524047358082,
-14.1375));
#359268=CARTESIAN_POINT('Ctrl Pts',(0.678525403784434,-1.17524047358082,
-14.0958333333333));
#359269=CARTESIAN_POINT('Ctrl Pts',(1.01778810567665,-0.58762023679041,
-14.0541666666667));
#359270=CARTESIAN_POINT('Ctrl Pts',(1.35705080756887,4.21563814687596E-15,
-14.0125));
#359271=CARTESIAN_POINT('Ctrl Pts',(1.01778810567665,0.587620236790418,
-13.9708333333333));
#359272=CARTESIAN_POINT('Ctrl Pts',(0.678525403784435,1.17524047358083,
-13.9291666666667));
#359273=CARTESIAN_POINT('Ctrl Pts',(0.,1.17524047358083,-13.8875));
#359274=CARTESIAN_POINT('Ctrl Pts',(-0.678525403784434,1.17524047358083,
-13.8458333333333));
#359275=CARTESIAN_POINT('Ctrl Pts',(-1.01778810567665,0.587620236790419,
-13.8041666666667));
#359276=CARTESIAN_POINT('Ctrl Pts',(-1.35705080756887,4.4387458126833E-15,
-13.7625));
#359277=CARTESIAN_POINT('Ctrl Pts',(-1.01778810567665,-0.58762023679041,
-13.7208333333333));
#359278=CARTESIAN_POINT('Ctrl Pts',(-0.678525403784435,-1.17524047358082,
-13.6791666666667));
#359279=CARTESIAN_POINT('Ctrl Pts',(-1.43925448419918E-16,-1.17524047358082,
-13.6375));
#359280=CARTESIAN_POINT('Origin',(-1.38777878078146E-16,-5.55111512312578E-15,
-17.91875));
#359281=CARTESIAN_POINT('',(4.78775260807605E-15,-1.17524047358082,-14.7));
#359282=CARTESIAN_POINT('',(4.88620806311632E-15,-1.17524047358082,-14.6375));
#359283=CARTESIAN_POINT('',(-4.21481204576211E-16,-1.17524047358085,-17.91875));
#359284=CARTESIAN_POINT('Ctrl Pts',(-1.43925448419918E-16,-1.17524047358082,
-14.7));
#359285=CARTESIAN_POINT('Ctrl Pts',(0.678525403784434,-1.17524047358082,
-14.6583333333333));
#359286=CARTESIAN_POINT('Ctrl Pts',(1.01778810567665,-0.58762023679041,
-14.6166666666667));
#359287=CARTESIAN_POINT('Ctrl Pts',(1.35705080756887,4.46150446630574E-15,
-14.575));
#359288=CARTESIAN_POINT('Ctrl Pts',(1.01778810567665,0.587620236790418,
-14.5333333333333));
#359289=CARTESIAN_POINT('Ctrl Pts',(0.678525403784435,1.17524047358083,
-14.4916666666667));
#359290=CARTESIAN_POINT('Ctrl Pts',(0.,1.17524047358083,-14.45));
#359291=CARTESIAN_POINT('Ctrl Pts',(-0.678525403784434,1.17524047358083,
-14.4083333333333));
#359292=CARTESIAN_POINT('Ctrl Pts',(-1.01778810567665,0.587620236790419,
-14.3666666666667));
#359293=CARTESIAN_POINT('Ctrl Pts',(-1.35705080756887,4.68461213211308E-15,
-14.325));
#359294=CARTESIAN_POINT('Ctrl Pts',(-1.01778810567665,-0.587620236790409,
-14.2833333333333));
#359295=CARTESIAN_POINT('Ctrl Pts',(-0.678525403784435,-1.17524047358082,
-14.2416666666667));
#359296=CARTESIAN_POINT('Ctrl Pts',(-1.43925448419918E-16,-1.17524047358082,
-14.2));
#359297=CARTESIAN_POINT('Ctrl Pts',(-1.43925448419918E-16,-1.17524047358082,
-14.6375));
#359298=CARTESIAN_POINT('Ctrl Pts',(0.678525403784434,-1.17524047358082,
-14.5958333333333));
#359299=CARTESIAN_POINT('Ctrl Pts',(1.01778810567665,-0.58762023679041,
-14.5541666666667));
#359300=CARTESIAN_POINT('Ctrl Pts',(1.35705080756887,4.4341859863691E-15,
-14.5125));
#359301=CARTESIAN_POINT('Ctrl Pts',(1.01778810567665,0.587620236790418,
-14.4708333333333));
#359302=CARTESIAN_POINT('Ctrl Pts',(0.678525403784435,1.17524047358083,
-14.4291666666667));
#359303=CARTESIAN_POINT('Ctrl Pts',(0.,1.17524047358083,-14.3875));
#359304=CARTESIAN_POINT('Ctrl Pts',(-0.678525403784434,1.17524047358083,
-14.3458333333333));
#359305=CARTESIAN_POINT('Ctrl Pts',(-1.01778810567665,0.587620236790419,
-14.3041666666667));
#359306=CARTESIAN_POINT('Ctrl Pts',(-1.35705080756887,4.65729365217644E-15,
-14.2625));
#359307=CARTESIAN_POINT('Ctrl Pts',(-1.01778810567665,-0.587620236790409,
-14.2208333333333));
#359308=CARTESIAN_POINT('Ctrl Pts',(-0.678525403784435,-1.17524047358082,
-14.1791666666667));
#359309=CARTESIAN_POINT('Ctrl Pts',(-1.43925448419918E-16,-1.17524047358082,
-14.1375));
#359310=CARTESIAN_POINT('Origin',(-1.38777878078146E-16,-5.55111512312578E-15,
-17.91875));
#359311=CARTESIAN_POINT('',(4.00010896775386E-15,-1.17524047358082,-15.2));
#359312=CARTESIAN_POINT('',(4.09856442279413E-15,-1.17524047358082,-15.1375));
#359313=CARTESIAN_POINT('',(-4.21481204576211E-16,-1.17524047358085,-17.91875));
#359314=CARTESIAN_POINT('Ctrl Pts',(-1.43925448419918E-16,-1.17524047358082,
-15.2));
#359315=CARTESIAN_POINT('Ctrl Pts',(0.678525403784434,-1.17524047358082,
-15.1583333333333));
#359316=CARTESIAN_POINT('Ctrl Pts',(1.01778810567665,-0.58762023679041,
-15.1166666666667));
#359317=CARTESIAN_POINT('Ctrl Pts',(1.35705080756887,4.68005230579889E-15,
-15.075));
#359318=CARTESIAN_POINT('Ctrl Pts',(1.01778810567665,0.587620236790418,
-15.0333333333333));
#359319=CARTESIAN_POINT('Ctrl Pts',(0.678525403784435,1.17524047358083,
-14.9916666666667));
#359320=CARTESIAN_POINT('Ctrl Pts',(0.,1.17524047358083,-14.95));
#359321=CARTESIAN_POINT('Ctrl Pts',(-0.678525403784434,1.17524047358083,
-14.9083333333333));
#359322=CARTESIAN_POINT('Ctrl Pts',(-1.01778810567665,0.587620236790419,
-14.8666666666667));
#359323=CARTESIAN_POINT('Ctrl Pts',(-1.35705080756887,4.90315997160622E-15,
-14.825));
#359324=CARTESIAN_POINT('Ctrl Pts',(-1.01778810567665,-0.587620236790409,
-14.7833333333333));
#359325=CARTESIAN_POINT('Ctrl Pts',(-0.678525403784435,-1.17524047358082,
-14.7416666666667));
#359326=CARTESIAN_POINT('Ctrl Pts',(-1.43925448419918E-16,-1.17524047358082,
-14.7));
#359327=CARTESIAN_POINT('Ctrl Pts',(-1.43925448419918E-16,-1.17524047358082,
-15.1375));
#359328=CARTESIAN_POINT('Ctrl Pts',(0.678525403784434,-1.17524047358082,
-15.0958333333333));
#359329=CARTESIAN_POINT('Ctrl Pts',(1.01778810567665,-0.58762023679041,
-15.0541666666667));
#359330=CARTESIAN_POINT('Ctrl Pts',(1.35705080756887,4.65273382586224E-15,
-15.0125));
#359331=CARTESIAN_POINT('Ctrl Pts',(1.01778810567665,0.587620236790418,
-14.9708333333333));
#359332=CARTESIAN_POINT('Ctrl Pts',(0.678525403784435,1.17524047358083,
-14.9291666666667));
#359333=CARTESIAN_POINT('Ctrl Pts',(0.,1.17524047358083,-14.8875));
#359334=CARTESIAN_POINT('Ctrl Pts',(-0.678525403784434,1.17524047358083,
-14.8458333333333));
#359335=CARTESIAN_POINT('Ctrl Pts',(-1.01778810567665,0.587620236790419,
-14.8041666666667));
#359336=CARTESIAN_POINT('Ctrl Pts',(-1.35705080756887,4.87584149166958E-15,
-14.7625));
#359337=CARTESIAN_POINT('Ctrl Pts',(-1.01778810567665,-0.587620236790409,
-14.7208333333333));
#359338=CARTESIAN_POINT('Ctrl Pts',(-0.678525403784435,-1.17524047358082,
-14.6791666666667));
#359339=CARTESIAN_POINT('Ctrl Pts',(-1.43925448419918E-16,-1.17524047358082,
-14.6375));
#359340=CARTESIAN_POINT('Origin',(-1.38777878078146E-16,-5.55111512312578E-15,
-17.91875));
#359341=CARTESIAN_POINT('',(3.21246532743166E-15,-1.17524047358082,-15.7));
#359342=CARTESIAN_POINT('',(3.31092078247193E-15,-1.17524047358082,-15.6375));
#359343=CARTESIAN_POINT('',(-4.21481204576211E-16,-1.17524047358085,-17.91875));
#359344=CARTESIAN_POINT('Ctrl Pts',(-1.43925448419918E-16,-1.17524047358082,
-15.7));
#359345=CARTESIAN_POINT('Ctrl Pts',(0.678525403784434,-1.17524047358082,
-15.6583333333333));
#359346=CARTESIAN_POINT('Ctrl Pts',(1.01778810567665,-0.587620236790409,
-15.6166666666667));
#359347=CARTESIAN_POINT('Ctrl Pts',(1.35705080756887,4.89860014529203E-15,
-15.575));
#359348=CARTESIAN_POINT('Ctrl Pts',(1.01778810567665,0.587620236790418,
-15.5333333333333));
#359349=CARTESIAN_POINT('Ctrl Pts',(0.678525403784435,1.17524047358083,
-15.4916666666667));
#359350=CARTESIAN_POINT('Ctrl Pts',(0.,1.17524047358083,-15.45));
#359351=CARTESIAN_POINT('Ctrl Pts',(-0.678525403784434,1.17524047358083,
-15.4083333333333));
#359352=CARTESIAN_POINT('Ctrl Pts',(-1.01778810567665,0.587620236790419,
-15.3666666666667));
#359353=CARTESIAN_POINT('Ctrl Pts',(-1.35705080756887,5.12170781109936E-15,
-15.325));
#359354=CARTESIAN_POINT('Ctrl Pts',(-1.01778810567665,-0.587620236790409,
-15.2833333333333));
#359355=CARTESIAN_POINT('Ctrl Pts',(-0.678525403784435,-1.17524047358082,
-15.2416666666667));
#359356=CARTESIAN_POINT('Ctrl Pts',(-1.43925448419918E-16,-1.17524047358082,
-15.2));
#359357=CARTESIAN_POINT('Ctrl Pts',(-1.43925448419918E-16,-1.17524047358082,
-15.6375));
#359358=CARTESIAN_POINT('Ctrl Pts',(0.678525403784434,-1.17524047358082,
-15.5958333333333));
#359359=CARTESIAN_POINT('Ctrl Pts',(1.01778810567665,-0.58762023679041,
-15.5541666666667));
#359360=CARTESIAN_POINT('Ctrl Pts',(1.35705080756887,4.87128166535538E-15,
-15.5125));
#359361=CARTESIAN_POINT('Ctrl Pts',(1.01778810567665,0.587620236790418,
-15.4708333333333));
#359362=CARTESIAN_POINT('Ctrl Pts',(0.678525403784435,1.17524047358083,
-15.4291666666667));
#359363=CARTESIAN_POINT('Ctrl Pts',(0.,1.17524047358083,-15.3875));
#359364=CARTESIAN_POINT('Ctrl Pts',(-0.678525403784434,1.17524047358083,
-15.3458333333333));
#359365=CARTESIAN_POINT('Ctrl Pts',(-1.01778810567665,0.587620236790419,
-15.3041666666667));
#359366=CARTESIAN_POINT('Ctrl Pts',(-1.35705080756887,5.09438933116272E-15,
-15.2625));
#359367=CARTESIAN_POINT('Ctrl Pts',(-1.01778810567665,-0.587620236790409,
-15.2208333333333));
#359368=CARTESIAN_POINT('Ctrl Pts',(-0.678525403784435,-1.17524047358082,
-15.1791666666667));
#359369=CARTESIAN_POINT('Ctrl Pts',(-1.43925448419918E-16,-1.17524047358082,
-15.1375));
#359370=CARTESIAN_POINT('Origin',(-1.38777878078146E-16,-5.55111512312578E-15,
-17.91875));
#359371=CARTESIAN_POINT('',(2.42482168710947E-15,-1.17524047358082,-16.2));
#359372=CARTESIAN_POINT('',(2.52327714214975E-15,-1.17524047358082,-16.1375));
#359373=CARTESIAN_POINT('',(-4.21481204576211E-16,-1.17524047358085,-17.91875));
#359374=CARTESIAN_POINT('Ctrl Pts',(-1.43925448419918E-16,-1.17524047358082,
-16.2));
#359375=CARTESIAN_POINT('Ctrl Pts',(0.678525403784434,-1.17524047358082,
-16.1583333333333));
#359376=CARTESIAN_POINT('Ctrl Pts',(1.01778810567665,-0.587620236790409,
-16.1166666666667));
#359377=CARTESIAN_POINT('Ctrl Pts',(1.35705080756887,5.11714798478517E-15,
-16.075));
#359378=CARTESIAN_POINT('Ctrl Pts',(1.01778810567665,0.587620236790419,
-16.0333333333333));
#359379=CARTESIAN_POINT('Ctrl Pts',(0.678525403784435,1.17524047358083,
-15.9916666666667));
#359380=CARTESIAN_POINT('Ctrl Pts',(0.,1.17524047358083,-15.95));
#359381=CARTESIAN_POINT('Ctrl Pts',(-0.678525403784434,1.17524047358083,
-15.9083333333333));
#359382=CARTESIAN_POINT('Ctrl Pts',(-1.01778810567665,0.58762023679042,
-15.8666666666667));
#359383=CARTESIAN_POINT('Ctrl Pts',(-1.35705080756887,5.34025565059251E-15,
-15.825));
#359384=CARTESIAN_POINT('Ctrl Pts',(-1.01778810567665,-0.587620236790409,
-15.7833333333333));
#359385=CARTESIAN_POINT('Ctrl Pts',(-0.678525403784435,-1.17524047358082,
-15.7416666666667));
#359386=CARTESIAN_POINT('Ctrl Pts',(-1.43925448419918E-16,-1.17524047358082,
-15.7));
#359387=CARTESIAN_POINT('Ctrl Pts',(-1.43925448419918E-16,-1.17524047358082,
-16.1375));
#359388=CARTESIAN_POINT('Ctrl Pts',(0.678525403784434,-1.17524047358082,
-16.0958333333333));
#359389=CARTESIAN_POINT('Ctrl Pts',(1.01778810567665,-0.587620236790409,
-16.0541666666667));
#359390=CARTESIAN_POINT('Ctrl Pts',(1.35705080756887,5.08982950484852E-15,
-16.0125));
#359391=CARTESIAN_POINT('Ctrl Pts',(1.01778810567665,0.587620236790419,
-15.9708333333333));
#359392=CARTESIAN_POINT('Ctrl Pts',(0.678525403784435,1.17524047358083,
-15.9291666666667));
#359393=CARTESIAN_POINT('Ctrl Pts',(0.,1.17524047358083,-15.8875));
#359394=CARTESIAN_POINT('Ctrl Pts',(-0.678525403784434,1.17524047358083,
-15.8458333333333));
#359395=CARTESIAN_POINT('Ctrl Pts',(-1.01778810567665,0.58762023679042,
-15.8041666666667));
#359396=CARTESIAN_POINT('Ctrl Pts',(-1.35705080756887,5.31293717065586E-15,
-15.7625));
#359397=CARTESIAN_POINT('Ctrl Pts',(-1.01778810567665,-0.587620236790409,
-15.7208333333333));
#359398=CARTESIAN_POINT('Ctrl Pts',(-0.678525403784435,-1.17524047358082,
-15.6791666666667));
#359399=CARTESIAN_POINT('Ctrl Pts',(-1.43925448419918E-16,-1.17524047358082,
-15.6375));
#359400=CARTESIAN_POINT('Origin',(-1.38777878078146E-16,-5.55111512312578E-15,
-17.91875));
#359401=CARTESIAN_POINT('',(1.63717804678728E-15,-1.17524047358082,-16.7));
#359402=CARTESIAN_POINT('',(1.73563350182756E-15,-1.17524047358082,-16.6375));
#359403=CARTESIAN_POINT('',(-4.21481204576211E-16,-1.17524047358085,-17.91875));
#359404=CARTESIAN_POINT('Ctrl Pts',(-1.43925448419918E-16,-1.17524047358082,
-16.7));
#359405=CARTESIAN_POINT('Ctrl Pts',(0.678525403784434,-1.17524047358082,
-16.6583333333333));
#359406=CARTESIAN_POINT('Ctrl Pts',(1.01778810567665,-0.587620236790409,
-16.6166666666667));
#359407=CARTESIAN_POINT('Ctrl Pts',(1.35705080756887,5.33569582427831E-15,
-16.575));
#359408=CARTESIAN_POINT('Ctrl Pts',(1.01778810567665,0.587620236790419,
-16.5333333333333));
#359409=CARTESIAN_POINT('Ctrl Pts',(0.678525403784435,1.17524047358083,
-16.4916666666667));
#359410=CARTESIAN_POINT('Ctrl Pts',(0.,1.17524047358083,-16.45));
#359411=CARTESIAN_POINT('Ctrl Pts',(-0.678525403784434,1.17524047358083,
-16.4083333333333));
#359412=CARTESIAN_POINT('Ctrl Pts',(-1.01778810567665,0.58762023679042,
-16.3666666666667));
#359413=CARTESIAN_POINT('Ctrl Pts',(-1.35705080756887,5.55880349008565E-15,
-16.325));
#359414=CARTESIAN_POINT('Ctrl Pts',(-1.01778810567665,-0.587620236790408,
-16.2833333333333));
#359415=CARTESIAN_POINT('Ctrl Pts',(-0.678525403784435,-1.17524047358082,
-16.2416666666667));
#359416=CARTESIAN_POINT('Ctrl Pts',(-1.43925448419918E-16,-1.17524047358082,
-16.2));
#359417=CARTESIAN_POINT('Ctrl Pts',(-1.43925448419918E-16,-1.17524047358082,
-16.6375));
#359418=CARTESIAN_POINT('Ctrl Pts',(0.678525403784434,-1.17524047358082,
-16.5958333333333));
#359419=CARTESIAN_POINT('Ctrl Pts',(1.01778810567665,-0.587620236790409,
-16.5541666666667));
#359420=CARTESIAN_POINT('Ctrl Pts',(1.35705080756887,5.30837734434166E-15,
-16.5125));
#359421=CARTESIAN_POINT('Ctrl Pts',(1.01778810567665,0.587620236790419,
-16.4708333333333));
#359422=CARTESIAN_POINT('Ctrl Pts',(0.678525403784435,1.17524047358083,
-16.4291666666667));
#359423=CARTESIAN_POINT('Ctrl Pts',(0.,1.17524047358083,-16.3875));
#359424=CARTESIAN_POINT('Ctrl Pts',(-0.678525403784434,1.17524047358083,
-16.3458333333333));
#359425=CARTESIAN_POINT('Ctrl Pts',(-1.01778810567665,0.58762023679042,
-16.3041666666667));
#359426=CARTESIAN_POINT('Ctrl Pts',(-1.35705080756887,5.53148501014901E-15,
-16.2625));
#359427=CARTESIAN_POINT('Ctrl Pts',(-1.01778810567665,-0.587620236790409,
-16.2208333333333));
#359428=CARTESIAN_POINT('Ctrl Pts',(-0.678525403784435,-1.17524047358082,
-16.1791666666667));
#359429=CARTESIAN_POINT('Ctrl Pts',(-1.43925448419918E-16,-1.17524047358082,
-16.1375));
#359430=CARTESIAN_POINT('Origin',(-1.38777878078146E-16,-5.55111512312578E-15,
-17.91875));
#359431=CARTESIAN_POINT('',(8.49534406465091E-16,-1.17524047358082,-17.2));
#359432=CARTESIAN_POINT('',(9.47989861505363E-16,-1.17524047358082,-17.1375));
#359433=CARTESIAN_POINT('',(-4.21481204576211E-16,-1.17524047358085,-17.91875));
#359434=CARTESIAN_POINT('Ctrl Pts',(-1.43925448419918E-16,-1.17524047358082,
-17.2));
#359435=CARTESIAN_POINT('Ctrl Pts',(0.678525403784434,-1.17524047358082,
-17.1583333333333));
#359436=CARTESIAN_POINT('Ctrl Pts',(1.01778810567665,-0.587620236790409,
-17.1166666666667));
#359437=CARTESIAN_POINT('Ctrl Pts',(1.35705080756887,5.55424366377145E-15,
-17.075));
#359438=CARTESIAN_POINT('Ctrl Pts',(1.01778810567665,0.587620236790419,
-17.0333333333333));
#359439=CARTESIAN_POINT('Ctrl Pts',(0.678525403784435,1.17524047358083,
-16.9916666666667));
#359440=CARTESIAN_POINT('Ctrl Pts',(0.,1.17524047358083,-16.95));
#359441=CARTESIAN_POINT('Ctrl Pts',(-0.678525403784434,1.17524047358083,
-16.9083333333333));
#359442=CARTESIAN_POINT('Ctrl Pts',(-1.01778810567665,0.58762023679042,
-16.8666666666667));
#359443=CARTESIAN_POINT('Ctrl Pts',(-1.35705080756887,5.77735132957879E-15,
-16.825));
#359444=CARTESIAN_POINT('Ctrl Pts',(-1.01778810567665,-0.587620236790408,
-16.7833333333333));
#359445=CARTESIAN_POINT('Ctrl Pts',(-0.678525403784435,-1.17524047358082,
-16.7416666666667));
#359446=CARTESIAN_POINT('Ctrl Pts',(-1.43925448419918E-16,-1.17524047358082,
-16.7));
#359447=CARTESIAN_POINT('Ctrl Pts',(-1.43925448419918E-16,-1.17524047358082,
-17.1375));
#359448=CARTESIAN_POINT('Ctrl Pts',(0.678525403784434,-1.17524047358082,
-17.0958333333333));
#359449=CARTESIAN_POINT('Ctrl Pts',(1.01778810567665,-0.587620236790409,
-17.0541666666667));
#359450=CARTESIAN_POINT('Ctrl Pts',(1.35705080756887,5.52692518383481E-15,
-17.0125));
#359451=CARTESIAN_POINT('Ctrl Pts',(1.01778810567665,0.587620236790419,
-16.9708333333333));
#359452=CARTESIAN_POINT('Ctrl Pts',(0.678525403784435,1.17524047358083,
-16.9291666666667));
#359453=CARTESIAN_POINT('Ctrl Pts',(0.,1.17524047358083,-16.8875));
#359454=CARTESIAN_POINT('Ctrl Pts',(-0.678525403784434,1.17524047358083,
-16.8458333333333));
#359455=CARTESIAN_POINT('Ctrl Pts',(-1.01778810567665,0.58762023679042,
-16.8041666666667));
#359456=CARTESIAN_POINT('Ctrl Pts',(-1.35705080756887,5.75003284964215E-15,
-16.7625));
#359457=CARTESIAN_POINT('Ctrl Pts',(-1.01778810567665,-0.587620236790408,
-16.7208333333333));
#359458=CARTESIAN_POINT('Ctrl Pts',(-0.678525403784435,-1.17524047358082,
-16.6791666666667));
#359459=CARTESIAN_POINT('Ctrl Pts',(-1.43925448419918E-16,-1.17524047358082,
-16.6375));
#359460=CARTESIAN_POINT('Origin',(-1.38777878078146E-16,-5.55111512312578E-15,
-17.91875));
#359461=CARTESIAN_POINT('',(4.25993338715498E-16,-1.17524047358085,-17.6497595264195));
#359462=CARTESIAN_POINT('',(1.60346221183174E-16,-1.17524047358082,-17.6375));
#359463=CARTESIAN_POINT('',(-4.21481204576211E-16,-1.17524047358085,-17.91875));
#359464=CARTESIAN_POINT('',(0.689217670442693,-0.951929185124621,-17.6497595264192));
#359465=CARTESIAN_POINT('Origin',(1.61565205658576E-12,-4.96575003339217E-12,
-17.6497595264242));
#359466=CARTESIAN_POINT('Ctrl Pts',(0.689217670442693,-0.951929185124621,
-17.6497595264192));
#359467=CARTESIAN_POINT('Ctrl Pts',(0.892378271989712,-0.80483644050495,
-17.6320689189856));
#359468=CARTESIAN_POINT('Ctrl Pts',(1.01778810567665,-0.587620236790409,
-17.6166666666667));
#359469=CARTESIAN_POINT('Ctrl Pts',(1.35705080756887,5.77279150326459E-15,
-17.575));
#359470=CARTESIAN_POINT('Ctrl Pts',(1.01778810567665,0.587620236790419,
-17.5333333333333));
#359471=CARTESIAN_POINT('Ctrl Pts',(0.678525403784435,1.17524047358083,
-17.4916666666667));
#359472=CARTESIAN_POINT('Ctrl Pts',(0.,1.17524047358083,-17.45));
#359473=CARTESIAN_POINT('Ctrl Pts',(-0.678525403784434,1.17524047358083,
-17.4083333333333));
#359474=CARTESIAN_POINT('Ctrl Pts',(-1.01778810567665,0.58762023679042,
-17.3666666666667));
#359475=CARTESIAN_POINT('Ctrl Pts',(-1.35705080756887,5.99589916907193E-15,
-17.325));
#359476=CARTESIAN_POINT('Ctrl Pts',(-1.01778810567665,-0.587620236790408,
-17.2833333333333));
#359477=CARTESIAN_POINT('Ctrl Pts',(-0.678525403784435,-1.17524047358082,
-17.2416666666667));
#359478=CARTESIAN_POINT('Ctrl Pts',(-1.43925448419918E-16,-1.17524047358082,
-17.2));
#359479=CARTESIAN_POINT('Ctrl Pts',(-1.43925448419918E-16,-1.17524047358082,
-17.6375));
#359480=CARTESIAN_POINT('Ctrl Pts',(0.678525403784434,-1.17524047358082,
-17.5958333333333));
#359481=CARTESIAN_POINT('Ctrl Pts',(1.01778810567665,-0.587620236790409,
-17.5541666666667));
#359482=CARTESIAN_POINT('Ctrl Pts',(1.35705080756887,5.74547302332795E-15,
-17.5125));
#359483=CARTESIAN_POINT('Ctrl Pts',(1.01778810567665,0.587620236790419,
-17.4708333333333));
#359484=CARTESIAN_POINT('Ctrl Pts',(0.678525403784435,1.17524047358083,
-17.4291666666667));
#359485=CARTESIAN_POINT('Ctrl Pts',(0.,1.17524047358083,-17.3875));
#359486=CARTESIAN_POINT('Ctrl Pts',(-0.678525403784434,1.17524047358083,
-17.3458333333333));
#359487=CARTESIAN_POINT('Ctrl Pts',(-1.01778810567665,0.58762023679042,
-17.3041666666667));
#359488=CARTESIAN_POINT('Ctrl Pts',(-1.35705080756887,5.96858068913529E-15,
-17.2625));
#359489=CARTESIAN_POINT('Ctrl Pts',(-1.01778810567665,-0.587620236790408,
-17.2208333333333));
#359490=CARTESIAN_POINT('Ctrl Pts',(-0.678525403784435,-1.17524047358082,
-17.1791666666667));
#359491=CARTESIAN_POINT('Ctrl Pts',(-1.43925448419918E-16,-1.17524047358082,
-17.1375));
#359492=CARTESIAN_POINT('Origin',(0.,1.30104260698261E-15,-17.7));
#359493=CARTESIAN_POINT('',(-1.83697019872102E-16,-1.5,-1.95));
#359494=CARTESIAN_POINT('',(-6.61501184751346E-14,-1.5,-1.88750000000001));
#359495=CARTESIAN_POINT('',(-1.83697019872103E-16,-1.5,-17.7));
#359496=CARTESIAN_POINT('',(0.,1.49999999999999,-1.7));
#359497=CARTESIAN_POINT('Ctrl Pts',(-1.83697019872102E-16,-1.5,-1.95));
#359498=CARTESIAN_POINT('Ctrl Pts',(0.866025403784435,-1.5,-1.90833333333333));
#359499=CARTESIAN_POINT('Ctrl Pts',(1.29903810567665,-0.749999999999999,
-1.86666666666667));
#359500=CARTESIAN_POINT('Ctrl Pts',(1.73205080756887,-1.1803518232214E-15,
-1.825));
#359501=CARTESIAN_POINT('Ctrl Pts',(1.29903810567666,0.749999999999996,
-1.78333333333333));
#359502=CARTESIAN_POINT('Ctrl Pts',(0.866025403784437,1.49999999999999,
-1.74166666666667));
#359503=CARTESIAN_POINT('Ctrl Pts',(0.,1.49999999999999,-1.7));
#359504=CARTESIAN_POINT('',(1.05094390383304,1.07028823734365,-1.7));
#359505=CARTESIAN_POINT('Origin',(0.,0.,-1.7));
#359506=CARTESIAN_POINT('Ctrl Pts',(1.05094390383304,1.07028823734365,-1.7));
#359507=CARTESIAN_POINT('Ctrl Pts',(1.14778830372624,0.975194198058742,
-1.70730092945357));
#359508=CARTESIAN_POINT('Ctrl Pts',(1.23123736281864,0.867435515515267,
-1.71430913802694));
#359509=CARTESIAN_POINT('Ctrl Pts',(1.36688476559254,0.632484953062897,
-1.72736194705207));
#359510=CARTESIAN_POINT('Ctrl Pts',(1.41846105744624,0.506328944455555,
-1.73437061419692));
#359511=CARTESIAN_POINT('Ctrl Pts',(1.50131107274971,0.18544000545117,-1.75219777747494));
#359512=CARTESIAN_POINT('Ctrl Pts',(1.51267225119167,-0.0118599651810934,
-1.76315888695451));
#359513=CARTESIAN_POINT('Ctrl Pts',(1.45854265849392,-0.402738183258619,
-1.78487434351437));
#359514=CARTESIAN_POINT('Ctrl Pts',(1.39237486911582,-0.592268370697173,
-1.79529456539463));
#359515=CARTESIAN_POINT('Ctrl Pts',(1.19416446946585,-0.927559693188778,
-1.81414461554112));
#359516=CARTESIAN_POINT('Ctrl Pts',(1.06665301676792,-1.07173833930981,
-1.8242844755617));
#359517=CARTESIAN_POINT('Ctrl Pts',(0.758646728034023,-1.3090883887425,
-1.84569649196644));
#359518=CARTESIAN_POINT('Ctrl Pts',(0.579280583753319,-1.39774711600699,
-1.85678899203078));
#359519=CARTESIAN_POINT('Ctrl Pts',(0.261088126463976,-1.48292231711216,
-1.87446401157843));
#359520=CARTESIAN_POINT('Ctrl Pts',(0.130699839833624,-1.50000000000001,
-1.88121170102409));
#359521=CARTESIAN_POINT('Ctrl Pts',(-1.34267597040605E-13,-1.5,-1.88750000000001));
#359522=CARTESIAN_POINT('Origin',(0.,1.30104260698261E-15,-17.7));
#359523=CARTESIAN_POINT('',(-9.90402146771155E-14,-1.5,-2.45000000000001));
#359524=CARTESIAN_POINT('',(-9.90925172839362E-14,-1.5,-2.38750000000001));
#359525=CARTESIAN_POINT('',(-1.83697019872103E-16,-1.5,-17.7));
#359526=CARTESIAN_POINT('Ctrl Pts',(-1.9671764217577E-13,-1.5,-2.45000000000001));
#359527=CARTESIAN_POINT('Ctrl Pts',(0.13402462108747,-1.50000000000002,
-2.44355173741143));
#359528=CARTESIAN_POINT('Ctrl Pts',(0.267693944681743,-1.48204243818681,
-2.43662174791999));
#359529=CARTESIAN_POINT('Ctrl Pts',(0.588398068733159,-1.39391513012925,
-2.418743882778));
#359530=CARTESIAN_POINT('Ctrl Pts',(0.767066381476009,-1.30415324991582,
-2.40765431401171));
#359531=CARTESIAN_POINT('Ctrl Pts',(1.07336246827429,-1.06499776836812,
-2.38627442884388));
#359532=CARTESIAN_POINT('Ctrl Pts',(1.19989176294859,-0.920114875846726,
-2.37616226052323));
#359533=CARTESIAN_POINT('Ctrl Pts',(1.39597225273381,-0.583731732015755,
-2.35738435734234));
#359534=CARTESIAN_POINT('Ctrl Pts',(1.46097640834344,-0.393813415120927,
-2.34687852306227));
#359535=CARTESIAN_POINT('Ctrl Pts',(1.51270125975872,-0.00273603458184616,
-2.32515200192121));
#359536=CARTESIAN_POINT('Ctrl Pts',(1.50016560131882,0.194373847288857,
-2.31420145292839));
#359537=CARTESIAN_POINT('Ctrl Pts',(1.40151516251111,0.567386311023262,
-2.29347853827648));
#359538=CARTESIAN_POINT('Ctrl Pts',(1.31838001246478,0.740295537016906,
-2.28453348967375));
#359539=CARTESIAN_POINT('Ctrl Pts',(1.0867276214625,1.05289539990168,-2.26470477929054));
#359540=CARTESIAN_POINT('Ctrl Pts',(0.937699507927868,1.18754656333423,
-2.25379435073969));
#359541=CARTESIAN_POINT('Ctrl Pts',(0.600554016430472,1.38807100973555,
-2.23200330720587));
#359542=CARTESIAN_POINT('Ctrl Pts',(0.416746893615161,1.45387169407227,
-2.22133208609904));
#359543=CARTESIAN_POINT('Ctrl Pts',(0.0343336710579792,1.51202215612334,
-2.20131793073775));
#359544=CARTESIAN_POINT('Ctrl Pts',(-0.160626851633572,1.50385916690459,
-2.1923790360782));
#359545=CARTESIAN_POINT('Ctrl Pts',(-0.541938187767889,1.41271939452019,
-2.17150152552067));
#359546=CARTESIAN_POINT('Ctrl Pts',(-0.724074881041112,1.32860097202541,
-2.16040184693271));
#359547=CARTESIAN_POINT('Ctrl Pts',(-1.03892987114642,1.09871648363606,
-2.13886769892525));
#359548=CARTESIAN_POINT('Ctrl Pts',(-1.17039619602381,0.957469831855792,
-2.12861900431547));
#359549=CARTESIAN_POINT('Ctrl Pts',(-1.37806863845292,0.625379279765833,
-2.10940262171244));
#359550=CARTESIAN_POINT('Ctrl Pts',(-1.44923266130069,0.435817040915999,
-2.09921205782865));
#359551=CARTESIAN_POINT('Ctrl Pts',(-1.51212785796491,0.0441443608115303,
-2.07745246448952));
#359552=CARTESIAN_POINT('Ctrl Pts',(-1.50493731564591,-0.153773201783428,
-2.06645704434535));
#359553=CARTESIAN_POINT('Ctrl Pts',(-1.4162035687073,-0.529582002360993,
-2.0455787776466));
#359554=CARTESIAN_POINT('Ctrl Pts',(-1.33783840494363,-0.704459485177441,
-2.03646512790282));
#359555=CARTESIAN_POINT('Ctrl Pts',(-1.11489389214297,-1.02301975413814,
-2.01688980866948));
#359556=CARTESIAN_POINT('Ctrl Pts',(-0.969591515547866,-1.16164946042504,
-2.00604811964142));
#359557=CARTESIAN_POINT('Ctrl Pts',(-0.680123042456934,-1.34464086446392,
-1.9870379666797));
#359558=CARTESIAN_POINT('Ctrl Pts',(-0.548326703601818,-1.40355542471544,
-1.97906039680748));
#359559=CARTESIAN_POINT('Ctrl Pts',(-0.276687652879418,-1.48077724317562,
-1.96384610637328));
#359560=CARTESIAN_POINT('Ctrl Pts',(-0.138651093382613,-1.5,-1.95667085384066));
#359561=CARTESIAN_POINT('Ctrl Pts',(-3.52148865623292E-14,-1.5,-1.95));
#359562=CARTESIAN_POINT('Ctrl Pts',(-1.32116539930397E-13,-1.5,-1.88750000000001));
#359563=CARTESIAN_POINT('Ctrl Pts',(-0.0630459354937167,-1.49999999999999,
-1.89053329898572));
#359564=CARTESIAN_POINT('Ctrl Pts',(-0.126153654145855,-1.49602560948929,
-1.89367997025144));
#359565=CARTESIAN_POINT('Ctrl Pts',(-0.380391049639784,-1.46374247408504,
-1.90680872640654));
#359566=CARTESIAN_POINT('Ctrl Pts',(-0.565328631914033,-1.40272109928616,
-1.91740157817117));
#359567=CARTESIAN_POINT('Ctrl Pts',(-0.908590211261669,-1.21025079912723,
-1.93926315583438));
#359568=CARTESIAN_POINT('Ctrl Pts',(-1.06213966579464,-1.07801640891699,
-1.95032398491593));
#359569=CARTESIAN_POINT('Ctrl Pts',(-1.30190549243595,-0.768979436081477,
-1.97044408398529));
#359570=CARTESIAN_POINT('Ctrl Pts',(-1.3889317576496,-0.597629494593554,
-1.97929836141147));
#359571=CARTESIAN_POINT('Ctrl Pts',(-1.49553456304681,-0.226916662076369,
-1.99989351877353));
#359572=CARTESIAN_POINT('Ctrl Pts',(-1.51234048224347,-0.0305584413693756,
-2.01080230881281));
#359573=CARTESIAN_POINT('Ctrl Pts',(-1.46940043446806,0.361063630422814,
-2.03255909057905));
#359574=CARTESIAN_POINT('Ctrl Pts',(-1.40867884223088,0.552407827581791,
-2.04318932375454));
#359575=CARTESIAN_POINT('Ctrl Pts',(-1.22029994828342,0.892772080145689,
-2.06209844889699));
#359576=CARTESIAN_POINT('Ctrl Pts',(-1.09735642690313,1.04020596571789,
-2.07193135778637));
#359577=CARTESIAN_POINT('Ctrl Pts',(-0.797217630311482,1.28587258658769,
-2.09319586517218));
#359578=CARTESIAN_POINT('Ctrl Pts',(-0.621124840206183,1.37957647161791,
-2.1042710191816));
#359579=CARTESIAN_POINT('Ctrl Pts',(-0.244153347521547,1.49293041144923,
-2.12555678913066));
#359580=CARTESIAN_POINT('Ctrl Pts',(-0.0471526458057884,1.51202381890725,
-2.13489737230127));
#359581=CARTESIAN_POINT('Ctrl Pts',(0.33946412644781,1.47370339852615,-2.15456293655079));
#359582=CARTESIAN_POINT('Ctrl Pts',(0.525520914200402,1.41804336382786,
-2.1650607100002));
#359583=CARTESIAN_POINT('Ctrl Pts',(0.873141096667831,1.23597292300454,
-2.18684310607224));
#359584=CARTESIAN_POINT('Ctrl Pts',(1.02999901103478,1.10865716365545,-2.19792648486674));
#359585=CARTESIAN_POINT('Ctrl Pts',(1.27886345971825,0.806867253437241,
-2.21828303429828));
#359586=CARTESIAN_POINT('Ctrl Pts',(1.371146755331,0.637561816499381,-2.22707989908337));
#359587=CARTESIAN_POINT('Ctrl Pts',(1.48829207763262,0.269974513241264,
-2.24750141593104));
#359588=CARTESIAN_POINT('Ctrl Pts',(1.51072886710611,0.0747545175846843,
-2.2583469712453));
#359589=CARTESIAN_POINT('Ctrl Pts',(1.47944113616424,-0.317448794119751,
-2.28013604411777));
#359590=CARTESIAN_POINT('Ctrl Pts',(1.42439209642333,-0.510539588190993,
-2.29086331045506));
#359591=CARTESIAN_POINT('Ctrl Pts',(1.24625240280759,-0.856112386695717,
-2.31006179926088));
#359592=CARTESIAN_POINT('Ctrl Pts',(1.12794162744611,-1.00690142291868,
-2.31953470045029));
#359593=CARTESIAN_POINT('Ctrl Pts',(0.836017749690881,-1.26089744854786,
-2.34063533972373));
#359594=CARTESIAN_POINT('Ctrl Pts',(0.663421738107635,-1.35965436438064,
-2.3516826168648));
#359595=CARTESIAN_POINT('Ctrl Pts',(0.322789903704657,-1.47382168933245,
-2.37124258822072));
#359596=CARTESIAN_POINT('Ctrl Pts',(0.161815744149655,-1.50000000000002,
-2.37971463637968));
#359597=CARTESIAN_POINT('Ctrl Pts',(-1.94774751882676E-13,-1.5,-2.38750000000001));
#359598=CARTESIAN_POINT('Origin',(0.,1.30104260698261E-15,-17.7));
#359599=CARTESIAN_POINT('',(-8.25256904935245E-14,-1.5,-2.95000000000001));
#359600=CARTESIAN_POINT('',(-1.78584683734892E-16,-1.5,-2.8875));
#359601=CARTESIAN_POINT('',(-1.83697019872103E-16,-1.5,-17.7));
#359602=CARTESIAN_POINT('Ctrl Pts',(-1.61849700308636E-13,-1.5,-2.95000000000001));
#359603=CARTESIAN_POINT('Ctrl Pts',(0.165288383140628,-1.50000000000002,
-2.94204755895832));
#359604=CARTESIAN_POINT('Ctrl Pts',(0.329658389342383,-1.47268563787592,
-2.93338057106647));
#359605=CARTESIAN_POINT('Ctrl Pts',(0.672640418581653,-1.35509817342272,
-2.91361252203373));
#359606=CARTESIAN_POINT('Ctrl Pts',(0.844448431113153,-1.25524630653446,
-2.90257274220761));
#359607=CARTESIAN_POINT('Ctrl Pts',(1.13455909306952,-0.999432396303687,
-2.88150884452548));
#359608=CARTESIAN_POINT('Ctrl Pts',(1.25185338819377,-0.847895132696047,
-2.87210528514977));
#359609=CARTESIAN_POINT('Ctrl Pts',(1.42771316089353,-0.501179875879174,
-2.85284332643772));
#359610=CARTESIAN_POINT('Ctrl Pts',(1.48149535181862,-0.307724647052924,
-2.84209581372515));
#359611=CARTESIAN_POINT('Ctrl Pts',(1.51019581240691,0.0845604829928128,
-2.82030219538927));
#359612=CARTESIAN_POINT('Ctrl Pts',(1.48651547065014,0.279506231582944,
-2.80947187602315));
#359613=CARTESIAN_POINT('Ctrl Pts',(1.36703139770437,0.646388427216387,
-2.7890895318213));
#359614=CARTESIAN_POINT('Ctrl Pts',(1.27356576840097,0.815243309367391,
-2.78029548078564));
#359615=CARTESIAN_POINT('Ctrl Pts',(1.02267248733059,1.11539498923852,-2.7598868255089));
#359616=CARTESIAN_POINT('Ctrl Pts',(0.865093561537473,1.24159755754438,
-2.74879967900941));
#359617=CARTESIAN_POINT('Ctrl Pts',(0.516538142626489,1.42132404965192,
-2.72703739603956));
#359618=CARTESIAN_POINT('Ctrl Pts',(0.330251435818131,1.47577996610756,
-2.71656200833338));
#359619=CARTESIAN_POINT('Ctrl Pts',(-0.0568477531729474,1.51173860477736,
-2.6969388388453));
#359620=CARTESIAN_POINT('Ctrl Pts',(-0.254103822357107,1.49131850056533,
-2.68753327138459));
#359621=CARTESIAN_POINT('Ctrl Pts',(-0.630514143493244,1.37529133677861,
-2.66620024459326));
#359622=CARTESIAN_POINT('Ctrl Pts',(-0.805847286381485,1.28046165486068,
-2.65513036699184));
#359623=CARTESIAN_POINT('Ctrl Pts',(-1.10417677040217,1.03294703285061,
-2.63390157683268));
#359624=CARTESIAN_POINT('Ctrl Pts',(-1.22609577350809,0.884778776179429,
-2.62415437645441));
#359625=CARTESIAN_POINT('Ctrl Pts',(-1.41223190619847,0.54326288429914,
-2.60518127134995));
#359626=CARTESIAN_POINT('Ctrl Pts',(-1.47171370609588,0.351520774197525,
-2.59452893189986));
#359627=CARTESIAN_POINT('Ctrl Pts',(-1.51209751636429,-0.0402586447386417,
-2.57276340862563));
#359628=CARTESIAN_POINT('Ctrl Pts',(-1.49405206137872,-0.236380762456758,
-2.56186773541907));
#359629=CARTESIAN_POINT('Ctrl Pts',(-1.38513458137321,-0.606414827864824,
-2.54131028734084));
#359630=CARTESIAN_POINT('Ctrl Pts',(-1.2969640075808,-0.777313818812451,
-2.53247482605294));
#359631=CARTESIAN_POINT('Ctrl Pts',(-1.05520727397145,-1.08477866057793,
-2.51230260973492));
#359632=CARTESIAN_POINT('Ctrl Pts',(-0.900923590882587,-1.21594716801792,
-2.50123606292023));
#359633=CARTESIAN_POINT('Ctrl Pts',(-0.556685633384153,-1.40615771484799,
-2.47939028016714));
#359634=CARTESIAN_POINT('Ctrl Pts',(-0.37149097115162,-1.46601150780009,
-2.46881749246633));
#359635=CARTESIAN_POINT('Ctrl Pts',(-0.120167666258793,-1.4963939642998,
-2.45588173719688));
#359636=CARTESIAN_POINT('Ctrl Pts',(-0.0600530205189941,-1.49999999999999,
-2.45288930229686));
#359637=CARTESIAN_POINT('Ctrl Pts',(-1.97896732334359E-13,-1.5,-2.45000000000001));
#359638=CARTESIAN_POINT('Ctrl Pts',(-1.98001337548E-13,-1.5,-2.38750000000001));
#359639=CARTESIAN_POINT('Ctrl Pts',(-0.0354619996939313,-1.5,-2.38920616625578));
#359640=CARTESIAN_POINT('Ctrl Pts',(-0.0709610799037976,-1.49874248423541,
-2.39094904754232));
#359641=CARTESIAN_POINT('Ctrl Pts',(-0.297872095609908,-1.48260149916315,
-2.4023146695721));
#359642=CARTESIAN_POINT('Ctrl Pts',(-0.484903676285203,-1.43236976673905,
-2.41270855659359));
#359643=CARTESIAN_POINT('Ctrl Pts',(-0.83661435230043,-1.26088978502587,
-2.43439357720847));
#359644=CARTESIAN_POINT('Ctrl Pts',(-0.99665928184499,-1.13861690195684,
-2.44549021144553));
#359645=CARTESIAN_POINT('Ctrl Pts',(-1.25463111003332,-0.844246553149174,
-2.46607884094973));
#359646=CARTESIAN_POINT('Ctrl Pts',(-1.35225256821551,-0.676952070131101,
-2.47489155165953));
#359647=CARTESIAN_POINT('Ctrl Pts',(-1.47986428692361,-0.312552254437961,
-2.49513598586471));
#359648=CARTESIAN_POINT('Ctrl Pts',(-1.50784766080662,-0.118620346000367,
-2.5059099807779));
#359649=CARTESIAN_POINT('Ctrl Pts',(-1.48813911227417,0.27381573292194,
-2.52771198516247));
#359650=CARTESIAN_POINT('Ctrl Pts',(-1.43878040665445,0.468471388304962,
-2.5385261882393));
#359651=CARTESIAN_POINT('Ctrl Pts',(-1.27086766016973,0.819118665189983,
-2.55800659251069));
#359652=CARTESIAN_POINT('Ctrl Pts',(-1.1570763481502,0.973268823233719,
-2.56719871666685));
#359653=CARTESIAN_POINT('Ctrl Pts',(-0.873239887321544,1.23531833702727,
-2.58813395791655));
#359654=CARTESIAN_POINT('Ctrl Pts',(-0.704201890786818,1.33890131196317,
-2.5991441071761));
#359655=CARTESIAN_POINT('Ctrl Pts',(-0.332586384393808,1.47625092023645,
-2.62083873346016));
#359656=CARTESIAN_POINT('Ctrl Pts',(-0.133240227340225,1.50736305210793,
-2.63088494734811));
#359657=CARTESIAN_POINT('Ctrl Pts',(0.257535381626867,1.49007251733879,
-2.65016644023308));
#359658=CARTESIAN_POINT('Ctrl Pts',(0.445359126004437,1.44508610081268,
-2.66045273702907));
#359659=CARTESIAN_POINT('Ctrl Pts',(0.800717433943054,1.28389709171077,
-2.68202739406638));
#359660=CARTESIAN_POINT('Ctrl Pts',(0.963688186958386,1.16655655682656,
-2.693127787379));
#359661=CARTESIAN_POINT('Ctrl Pts',(1.23037332501627,0.879446537972054,
-2.71393396036773));
#359662=CARTESIAN_POINT('Ctrl Pts',(1.33317837581294,0.71405706917474,-2.72283016282377));
#359663=CARTESIAN_POINT('Ctrl Pts',(1.47073067960114,0.352758008589517,
-2.74290233285627));
#359664=CARTESIAN_POINT('Ctrl Pts',(1.50393194006517,0.160192748766035,
-2.75360040284647));
#359665=CARTESIAN_POINT('Ctrl Pts',(1.49520969110581,-0.232146380068924,
-2.77539702111507));
#359666=CARTESIAN_POINT('Ctrl Pts',(1.45129899090333,-0.428128946154902,
-2.78628494145318));
#359667=CARTESIAN_POINT('Ctrl Pts',(1.29315560005151,-0.783500996520054,
-2.80602783314013));
#359668=CARTESIAN_POINT('Ctrl Pts',(1.18359106897811,-0.940876127785583,
-2.81502322947043));
#359669=CARTESIAN_POINT('Ctrl Pts',(0.90736895290096,-1.21038374162605,
-2.83579929483321));
#359670=CARTESIAN_POINT('Ctrl Pts',(0.741778816430195,-1.31837276364729,
-2.8467659490449));
#359671=CARTESIAN_POINT('Ctrl Pts',(0.38197060730477,-1.46320976555244,
-2.86810047963075));
#359672=CARTESIAN_POINT('Ctrl Pts',(0.191810212068219,-1.5,-2.87827152686909));
#359673=CARTESIAN_POINT('Ctrl Pts',(1.04083408558608E-15,-1.5,-2.8875));
#359674=CARTESIAN_POINT('Origin',(0.,1.30104260698261E-15,-17.7));
#359675=CARTESIAN_POINT('',(-2.30626176757078E-16,-1.5,-3.45));
#359676=CARTESIAN_POINT('',(3.27638141250644E-14,-1.5,-3.3875));
#359677=CARTESIAN_POINT('',(-1.83697019872103E-16,-1.5,-17.7));
#359678=CARTESIAN_POINT('Ctrl Pts',(-1.2490009027033E-15,-1.5,-3.45));
#359679=CARTESIAN_POINT('Ctrl Pts',(0.194839574775211,-1.5,-3.44062577658789));
#359680=CARTESIAN_POINT('Ctrl Pts',(0.387930314093105,-1.46203733311044,
-3.4302811755361));
#359681=CARTESIAN_POINT('Ctrl Pts',(0.749532372686592,-1.31396321843056,
-3.40877041852818));
#359682=CARTESIAN_POINT('Ctrl Pts',(0.914390188142045,-1.20507006247664,
-3.39781388329645));
#359683=CARTESIAN_POINT('Ctrl Pts',(1.18902016837216,-0.934017544320743,
-3.37707150559656));
#359684=CARTESIAN_POINT('Ctrl Pts',(1.29770352229627,-0.775960061968662,
-3.36810889233159));
#359685=CARTESIAN_POINT('Ctrl Pts',(1.4537863214166,-0.419607064539616,
-3.34831150358553));
#359686=CARTESIAN_POINT('Ctrl Pts',(1.49654731889376,-0.22336553782117,
-3.33740919654562));
#359687=CARTESIAN_POINT('Ctrl Pts',(1.50296332271505,0.168913881670837,
-3.31561589546273));
#359688=CARTESIAN_POINT('Ctrl Pts',(1.46867222228306,0.361174373701028,
-3.3049347570166));
#359689=CARTESIAN_POINT('Ctrl Pts',(1.32903047402259,0.721812101030813,
-3.2848993277205));
#359690=CARTESIAN_POINT('Ctrl Pts',(1.22512055917265,0.88680186686731,-3.27597692186157));
#359691=CARTESIAN_POINT('Ctrl Pts',(0.956596926263572,1.17235797709162,
-3.25512545837668));
#359692=CARTESIAN_POINT('Ctrl Pts',(0.793024621943816,1.28864441531711,
-3.24402540337617));
#359693=CARTESIAN_POINT('Ctrl Pts',(0.436930598254616,1.44764249247397,
-3.222476208419));
#359694=CARTESIAN_POINT('Ctrl Pts',(0.248957567346252,1.49151587549274,
-3.21221364666887));
#359695=CARTESIAN_POINT('Ctrl Pts',(-0.14223671704898,1.50659840697105,
-3.19297334367772));
#359696=CARTESIAN_POINT('Ctrl Pts',(-0.341836891795151,1.47419638644906,
-3.18283659783216));
#359697=CARTESIAN_POINT('Ctrl Pts',(-0.712841222585338,1.33430327539119,
-3.16110072389287));
#359698=CARTESIAN_POINT('Ctrl Pts',(-0.881101165984585,1.22970378321009,
-3.15009977214211));
#359699=CARTESIAN_POINT('Ctrl Pts',(-1.16320142576591,0.965943362945885,
-3.12920053872451));
#359700=CARTESIAN_POINT('Ctrl Pts',(-1.27602687227312,0.811063267079022,
-3.12005907039326));
#359701=CARTESIAN_POINT('Ctrl Pts',(-1.44172429156805,0.459333958594898,
-3.10051855325525));
#359702=CARTESIAN_POINT('Ctrl Pts',(-1.48984827443744,0.264363031137791,
-3.0896868350632));
#359703=CARTESIAN_POINT('Ctrl Pts',(-1.50705846407638,-0.128078201215698,
-3.06788454437689));
#359704=CARTESIAN_POINT('Ctrl Pts',(-1.47788469594228,-0.321711687080483,
-3.05712712849551));
#359705=CARTESIAN_POINT('Ctrl Pts',(-1.34801380858588,-0.685413434451986,
-3.03692147586376));
#359706=CARTESIAN_POINT('Ctrl Pts',(-1.24922467390369,-0.852274225083107,
-3.02809573278294));
#359707=CARTESIAN_POINT('Ctrl Pts',(-0.989277642706516,-1.14501350029092,
-3.00745737887967));
#359708=CARTESIAN_POINT('Ctrl Pts',(-0.828558780463521,-1.26617753568454,
-2.99635912136486));
#359709=CARTESIAN_POINT('Ctrl Pts',(-0.475998210173412,-1.43533829293318,
-2.9746976330944));
#359710=CARTESIAN_POINT('Ctrl Pts',(-0.288774906769266,-1.48438540427964,
-2.96432742794986));
#359711=CARTESIAN_POINT('Ctrl Pts',(-0.0649141658325175,-1.49894762113898,
-2.95315241700592));
#359712=CARTESIAN_POINT('Ctrl Pts',(-0.0324407882280855,-1.5,-2.95156080815135));
#359713=CARTESIAN_POINT('Ctrl Pts',(-1.64867683967177E-13,-1.5,-2.95000000000001));
#359714=CARTESIAN_POINT('Ctrl Pts',(-1.73472347597681E-16,-1.5,-2.8875));
#359715=CARTESIAN_POINT('Ctrl Pts',(-0.00680225146496058,-1.5,-2.8878272734762));
#359716=CARTESIAN_POINT('Ctrl Pts',(-0.0136064557941092,-1.49995372940945,
-2.88815592620393));
#359717=CARTESIAN_POINT('Ctrl Pts',(-0.211233729968314,-1.49726414908849,
-2.89773898343038));
#359718=CARTESIAN_POINT('Ctrl Pts',(-0.399784487207624,-1.4582757419572,
-2.90789364727691));
#359719=CARTESIAN_POINT('Ctrl Pts',(-0.758949723752875,-1.30892323684144,
-2.92932267347481));
#359720=CARTESIAN_POINT('Ctrl Pts',(-0.925082722468769,-1.19729391658118,
-2.94041656555398));
#359721=CARTESIAN_POINT('Ctrl Pts',(-1.2016354215255,-0.918618321764496,
-2.961463202236));
#359722=CARTESIAN_POINT('Ctrl Pts',(-1.31041923475783,-0.755369011804498,
-2.97053505489987));
#359723=CARTESIAN_POINT('Ctrl Pts',(-1.45915684505256,-0.397648821272951,
-2.99040839881829));
#359724=CARTESIAN_POINT('Ctrl Pts',(-1.49816125722044,-0.206784743462552,
-3.00101195869664));
#359725=CARTESIAN_POINT('Ctrl Pts',(-1.50178248966322,0.186871424042968,
-3.02288174578028));
#359726=CARTESIAN_POINT('Ctrl Pts',(-1.46334013568441,0.385907260634357,
-3.03393929225757));
#359727=CARTESIAN_POINT('Ctrl Pts',(-1.31431367096058,0.747558741474286,
-3.05403104119312));
#359728=CARTESIAN_POINT('Ctrl Pts',(-1.20891120623186,0.908187109041197,
-3.06289698550034));
#359729=CARTESIAN_POINT('Ctrl Pts',(-0.940219556538581,1.18495896237142,
-3.08351252556057));
#359730=CARTESIAN_POINT('Ctrl Pts',(-0.778126123883215,1.29717127951698,
-3.09442825828496));
#359731=CARTESIAN_POINT('Ctrl Pts',(-0.416887645352554,1.4545471223638,
-3.11617990387692));
#359732=CARTESIAN_POINT('Ctrl Pts',(-0.220672017695724,1.49694110218437,
-3.12679794321473));
#359733=CARTESIAN_POINT('Ctrl Pts',(0.168346646154897,1.50261480167819,
-3.1456722151696));
#359734=CARTESIAN_POINT('Ctrl Pts',(0.357434014427285,1.46917687899588,
-3.15555324984303));
#359735=CARTESIAN_POINT('Ctrl Pts',(0.719875708815306,1.33072603506776,
-3.17683709077051));
#359736=CARTESIAN_POINT('Ctrl Pts',(0.888744481011991,1.2244139174965,-3.18791490773795));
#359737=CARTESIAN_POINT('Ctrl Pts',(1.17428852738021,0.953635167188392,
-3.2091747840273));
#359738=CARTESIAN_POINT('Ctrl Pts',(1.28863081923191,0.792333496165166,
-3.21848147243537));
#359739=CARTESIAN_POINT('Ctrl Pts',(1.44750540073537,0.437938742750646,
-3.23817006984728));
#359740=CARTESIAN_POINT('Ctrl Pts',(1.49169755897839,0.248761868219999,
-3.24867989621009));
#359741=CARTESIAN_POINT('Ctrl Pts',(1.50646529866692,-0.143512298964429,
-3.27047290549811));
#359742=CARTESIAN_POINT('Ctrl Pts',(1.4739124382648,-0.342972525396591,
-3.28155402918879));
#359743=CARTESIAN_POINT('Ctrl Pts',(1.33565999918759,-0.708876004675973,
-3.30188200025986));
#359744=CARTESIAN_POINT('Ctrl Pts',(1.23464257562583,-0.873013653000563,
-3.31068194396756));
#359745=CARTESIAN_POINT('Ctrl Pts',(0.973902526018742,-1.15734155812929,
-3.331124802818));
#359746=CARTESIAN_POINT('Ctrl Pts',(0.815587524526735,-1.27386548968896,
-3.34197851275534));
#359747=CARTESIAN_POINT('Ctrl Pts',(0.459622713352567,-1.44161889024216,
-3.36376469440016));
#359748=CARTESIAN_POINT('Ctrl Pts',(0.264706404361307,-1.4897894342995,
-3.37448068035721));
#359749=CARTESIAN_POINT('Ctrl Pts',(0.0440258635328815,-1.49951579390308,
-3.38536835448388));
#359750=CARTESIAN_POINT('Ctrl Pts',(0.0220047927330057,-1.5,-3.38644129391602));
#359751=CARTESIAN_POINT('Ctrl Pts',(6.57113252700009E-14,-1.5,-3.3875));
#359752=CARTESIAN_POINT('Origin',(0.,1.30104260698261E-15,-17.7));
#359753=CARTESIAN_POINT('',(4.93129457402405E-14,-1.5,-3.94999999999999));
#359754=CARTESIAN_POINT('',(9.87353479164595E-14,-1.5,-3.8875));
#359755=CARTESIAN_POINT('',(-1.83697019872103E-16,-1.5,-17.7));
#359756=CARTESIAN_POINT('Ctrl Pts',(9.88095885003532E-14,-1.5,-3.94999999999999));
#359757=CARTESIAN_POINT('Ctrl Pts',(0.0252363046513762,-1.5,-3.94878581772634));
#359758=CARTESIAN_POINT('Ctrl Pts',(0.0504931155048277,-1.49936313763594,
-3.94755295822627));
#359759=CARTESIAN_POINT('Ctrl Pts',(0.274351419805314,-1.48804434710496,
-3.93646815969084));
#359760=CARTESIAN_POINT('Ctrl Pts',(0.468958796760554,-1.4386100389388,
-3.92573193267472));
#359761=CARTESIAN_POINT('Ctrl Pts',(0.823724856932467,-1.26860007743464,
-3.90394074371575));
#359762=CARTESIAN_POINT('Ctrl Pts',(0.98119478738767,-1.15114526004823,
-3.89310183433799));
#359763=CARTESIAN_POINT('Ctrl Pts',(1.2401797942288,-0.86516491335197,-3.87269751386733));
#359764=CARTESIAN_POINT('Ctrl Pts',(1.34022968995924,-0.700242027381734,
-3.86390233485444));
#359765=CARTESIAN_POINT('Ctrl Pts',(1.47608668686549,-0.333411407452506,
-3.84352285596948));
#359766=CARTESIAN_POINT('Ctrl Pts',(1.50733450778141,-0.133879754122094,
-3.83243776411779));
#359767=CARTESIAN_POINT('Ctrl Pts',(1.49010447480495,0.258046256224327,
-3.81066409687632));
#359768=CARTESIAN_POINT('Ctrl Pts',(1.44477012137807,0.446830042571911,
-3.8001761087459));
#359769=CARTESIAN_POINT('Ctrl Pts',(1.28364395592772,0.800475544085902,
-3.78052913643957));
#359770=CARTESIAN_POINT('Ctrl Pts',(1.16804841780491,0.961342385648734,
-3.77116046721349));
#359771=CARTESIAN_POINT('Ctrl Pts',(0.880501965450157,1.2303334256396,-3.74985390874111));
#359772=CARTESIAN_POINT('Ctrl Pts',(0.711043389639699,1.33544695234033,
-3.73878100902493));
#359773=CARTESIAN_POINT('Ctrl Pts',(0.347914392787633,1.47144820878648,
-3.71753214433895));
#359774=CARTESIAN_POINT('Ctrl Pts',(0.158707277139125,1.50365303014975,
-3.70773728049114));
#359775=CARTESIAN_POINT('Ctrl Pts',(-0.230192531608629,1.49550768211014,
-3.68880007005102));
#359776=CARTESIAN_POINT('Ctrl Pts',(-0.426142613523374,1.45186383770904,
-3.67816008832811));
#359777=CARTESIAN_POINT('Ctrl Pts',(-0.786268478591804,1.29223388845718,
-3.6563993593095));
#359778=CARTESIAN_POINT('Ctrl Pts',(-0.947556031090891,1.17908082335176,
-3.64549626762443));
#359779=CARTESIAN_POINT('Ctrl Pts',(-1.21453656609161,0.9006732389317,-3.62491761663351));
#359780=CARTESIAN_POINT('Ctrl Pts',(-1.31899490525424,0.739296289883646,
-3.61607201610451));
#359781=CARTESIAN_POINT('Ctrl Pts',(-1.46571371508099,0.376722917367835,
-3.59592905096475));
#359782=CARTESIAN_POINT('Ctrl Pts',(-1.50289217353618,0.177581924215279,
-3.58486566245628));
#359783=CARTESIAN_POINT('Ctrl Pts',(-1.49687413194325,-0.215803765191046,
-3.5630109019337));
#359784=CARTESIAN_POINT('Ctrl Pts',(-1.45675185089939,-0.406317737064526,
-3.55242679238518));
#359785=CARTESIAN_POINT('Ctrl Pts',(-1.30584168430246,-0.76333179073737,
-3.53259267829224));
#359786=CARTESIAN_POINT('Ctrl Pts',(-1.19587799087183,-0.926164735135001,
-3.52347657513065));
#359787=CARTESIAN_POINT('Ctrl Pts',(-0.917401819753913,-1.20316849336213,
-3.50238383526119));
#359788=CARTESIAN_POINT('Ctrl Pts',(-0.750671697114279,-1.3136693089406,
-3.49129256139612));
#359789=CARTESIAN_POINT('Ctrl Pts',(-0.390805454198223,-1.46069276297905,
-3.46989450387673));
#359790=CARTESIAN_POINT('Ctrl Pts',(-0.202134426667967,-1.49850529477196,
-3.45976671672697));
#359791=CARTESIAN_POINT('Ctrl Pts',(-0.00760865885340758,-1.49998552947111,
-3.45036647372877));
#359792=CARTESIAN_POINT('Ctrl Pts',(-0.00380401527166274,-1.5,-3.45018302077009));
#359793=CARTESIAN_POINT('Ctrl Pts',(-2.77555333642052E-16,-1.5,-3.45));
#359794=CARTESIAN_POINT('Ctrl Pts',(6.57113252700015E-14,-1.5,-3.3875));
#359795=CARTESIAN_POINT('Ctrl Pts',(-0.16761611737248,-1.5,-3.39556443420713));
#359796=CARTESIAN_POINT('Ctrl Pts',(-0.334213726482098,-1.47190970465187,
-3.40436015139458));
#359797=CARTESIAN_POINT('Ctrl Pts',(-0.678945946275743,-1.35197959587786,
-3.42427747996298));
#359798=CARTESIAN_POINT('Ctrl Pts',(-0.85046217873718,-1.25121188156459,
-3.43532866172018));
#359799=CARTESIAN_POINT('Ctrl Pts',(-1.1451974958732,-0.988730720393048,
-3.4568002646434));
#359800=CARTESIAN_POINT('Ctrl Pts',(-1.26534098283104,-0.82943209907657,
-3.46642043894027));
#359801=CARTESIAN_POINT('Ctrl Pts',(-1.43453600430935,-0.478503581222086,
-3.48591646770996));
#359802=CARTESIAN_POINT('Ctrl Pts',(-1.48393134676266,-0.291181964977092,
-3.49632322416801));
#359803=CARTESIAN_POINT('Ctrl Pts',(-1.50994025159247,0.0993750919537776,
-3.51802083844195));
#359804=CARTESIAN_POINT('Ctrl Pts',(-1.4833573561422,0.299094962127195,
-3.52911638678492));
#359805=CARTESIAN_POINT('Ctrl Pts',(-1.35609196549547,0.669195420552612,
-3.5496775233641));
#359806=CARTESIAN_POINT('Ctrl Pts',(-1.25949329466154,0.836949511057635,
-3.55848453146984));
#359807=CARTESIAN_POINT('Ctrl Pts',(-1.00676462571169,1.12877695229422,
-3.57875026303614));
#359808=CARTESIAN_POINT('Ctrl Pts',(-0.85233765382573,1.24948843320678,
-3.5895332308772));
#359809=CARTESIAN_POINT('Ctrl Pts',(-0.501943041270044,1.42743993730768,
-3.61133469687014));
#359810=CARTESIAN_POINT('Ctrl Pts',(-0.308500469336784,1.48134423889683,
-3.62213904866248));
#359811=CARTESIAN_POINT('Ctrl Pts',(0.0792170696405466,1.50989463401122,
-3.64158618398494));
#359812=CARTESIAN_POINT('Ctrl Pts',(0.269529698574956,1.48776003391195,
-3.65080775272698));
#359813=CARTESIAN_POINT('Ctrl Pts',(0.638048212583981,1.37167077299751,
-3.67176280969109));
#359814=CARTESIAN_POINT('Ctrl Pts',(0.811997675149301,1.27641844396522,
-3.68277785513955));
#359815=CARTESIAN_POINT('Ctrl Pts',(1.1157031316742,1.02227239288957,-3.70444950325934));
#359816=CARTESIAN_POINT('Ctrl Pts',(1.24163378932754,0.864955149023215,
-3.71444693616545));
#359817=CARTESIAN_POINT('Ctrl Pts',(1.42087250911037,0.517479170344761,
-3.73375115720314));
#359818=CARTESIAN_POINT('Ctrl Pts',(1.47524805007958,0.332091519884599,
-3.7440504711176));
#359819=CARTESIAN_POINT('Ctrl Pts',(1.51207615194257,-0.0565007591672,-3.76563893106491));
#359820=CARTESIAN_POINT('Ctrl Pts',(1.49126859977781,-0.256308138098137,
-3.77673934100552));
#359821=CARTESIAN_POINT('Ctrl Pts',(1.37471246826402,-0.630365116330303,
-3.79752028424064));
#359822=CARTESIAN_POINT('Ctrl Pts',(1.28238542201467,-0.801673142681147,
-3.80640323435747));
#359823=CARTESIAN_POINT('Ctrl Pts',(1.0373700788615,-1.10062417721052,-3.82649573595481));
#359824=CARTESIAN_POINT('Ctrl Pts',(0.88675666197649,-1.22521801098215,
-3.83720306718031));
#359825=CARTESIAN_POINT('Ctrl Pts',(0.541955371827883,-1.41273746701526,
-3.85900120076603));
#359826=CARTESIAN_POINT('Ctrl Pts',(0.350082293045064,-1.47207493742894,
-3.8698809616402));
#359827=CARTESIAN_POINT('Ctrl Pts',(0.10154674091477,-1.4974249080659,-3.88254279981836));
#359828=CARTESIAN_POINT('Ctrl Pts',(0.0507470353532034,-1.5,-3.8850584321232));
#359829=CARTESIAN_POINT('Ctrl Pts',(1.97654392852791E-13,-1.5,-3.8875));
#359830=CARTESIAN_POINT('Origin',(0.,1.30104260698261E-15,-17.7));
#359831=CARTESIAN_POINT('',(9.87177402016726E-14,-1.5,-4.44999999999999));
#359832=CARTESIAN_POINT('',(1.6283941103285E-14,-1.5,-4.3875));
#359833=CARTESIAN_POINT('',(-1.83697019872103E-16,-1.5,-17.7));
#359834=CARTESIAN_POINT('Ctrl Pts',(1.97619177423217E-13,-1.5,-4.44999999999999));
#359835=CARTESIAN_POINT('Ctrl Pts',(0.0536659410771262,-1.5,-4.44741799620606));
#359836=CARTESIAN_POINT('Ctrl Pts',(0.1073867709094,-1.49712018000069,-4.44475335657562));
#359837=CARTESIAN_POINT('Ctrl Pts',(0.35869308253257,-1.47000106983716,
-4.43190906740457));
#359838=CARTESIAN_POINT('Ctrl Pts',(0.550220156758184,-1.40953987858202,
-4.4210147392146));
#359839=CARTESIAN_POINT('Ctrl Pts',(0.893825668233847,-1.22005325383621,
-4.39921949398176));
#359840=CARTESIAN_POINT('Ctrl Pts',(1.04363434848904,-1.09466695908024,
-4.38852886786029));
#359841=CARTESIAN_POINT('Ctrl Pts',(1.28703766229849,-0.794239658280263,
-4.3684729176645));
#359842=CARTESIAN_POINT('Ctrl Pts',(1.37846968947488,-0.62217906936543,
-4.35956550385356));
#359843=CARTESIAN_POINT('Ctrl Pts',(1.49277156972031,-0.247307197039821,
-4.33873928872436));
#359844=CARTESIAN_POINT('Ctrl Pts',(1.5123698773978,-0.0475019270911679,
-4.32763899594943));
#359845=CARTESIAN_POINT('Ctrl Pts',(1.47328339087223,0.340641046412763,
-4.30607549742144));
#359846=CARTESIAN_POINT('Ctrl Pts',(1.41787176708579,0.525606384079794,
-4.29579964532883));
#359847=CARTESIAN_POINT('Ctrl Pts',(1.23652112732012,0.872346283609986,
-4.27653631757715));
#359848=CARTESIAN_POINT('Ctrl Pts',(1.109355542849,1.02924165184833,-4.26645051422282));
#359849=CARTESIAN_POINT('Ctrl Pts',(0.803761806030416,1.28160144517232,
-4.24473763444591));
#359850=CARTESIAN_POINT('Ctrl Pts',(0.629319521599276,1.37567974358715,
-4.23373149005597));
#359851=CARTESIAN_POINT('Ctrl Pts',(0.260188389018742,1.48942342421312,
-4.21281211347512));
#359852=CARTESIAN_POINT('Ctrl Pts',(0.0697293660230309,1.5103645083182,
-4.20364275869574));
#359853=CARTESIAN_POINT('Ctrl Pts',(-0.317821920574179,1.47937306722689,
-4.18413581536196));
#359854=CARTESIAN_POINT('Ctrl Pts',(-0.510927176963519,1.4242498582582,
-4.17331383413297));
#359855=CARTESIAN_POINT('Ctrl Pts',(-0.860093885236144,1.24414368954539,
-4.15151159391762));
#359856=CARTESIAN_POINT('Ctrl Pts',(-1.01367636304737,1.1225539271368,-4.14074486010845));
#359857=CARTESIAN_POINT('Ctrl Pts',(-1.26468576506506,0.829129986433944,
-4.12051749960359));
#359858=CARTESIAN_POINT('Ctrl Pts',(-1.36033356412408,0.660590476072913,
-4.11169947089286));
#359859=CARTESIAN_POINT('Ctrl Pts',(-1.48522288246882,0.28960013190703,
-4.09108889621698));
#359860=CARTESIAN_POINT('Ctrl Pts',(-1.51052027468975,0.0898468405231036,
-4.07999149114009));
#359861=CARTESIAN_POINT('Ctrl Pts',(-1.48209844719908,-0.300298759920324,
-4.0583167355599));
#359862=CARTESIAN_POINT('Ctrl Pts',(-1.43159003781814,-0.487201763436985,
-4.04793323536453));
#359863=CARTESIAN_POINT('Ctrl Pts',(-1.26016510721411,-0.837370550868243,
-4.02847941384058));
#359864=CARTESIAN_POINT('Ctrl Pts',(-1.13874891978242,-0.996232451394284,
-4.01878162596472));
#359865=CARTESIAN_POINT('Ctrl Pts',(-0.842023813037466,-1.25688555572448,
-3.99726506860101));
#359866=CARTESIAN_POINT('Ctrl Pts',(-0.669954807064273,-1.35643867491598,
-3.9862210302692));
#359867=CARTESIAN_POINT('Ctrl Pts',(-0.327676386565897,-1.4730079980737,
-3.96651511533044));
#359868=CARTESIAN_POINT('Ctrl Pts',(-0.16430845139944,-1.5,-3.9579052940538));
#359869=CARTESIAN_POINT('Ctrl Pts',(9.88095885003532E-14,-1.5,-3.94999999999999));
#359870=CARTESIAN_POINT('Ctrl Pts',(1.96613558767211E-13,-1.5,-3.8875));
#359871=CARTESIAN_POINT('Ctrl Pts',(-0.138634473684809,-1.5,-3.89417005422507));
#359872=CARTESIAN_POINT('Ctrl Pts',(-0.276824301836837,-1.48078591559129,
-3.90135243999896));
#359873=CARTESIAN_POINT('Ctrl Pts',(-0.599047816188526,-1.38906927158903,
-3.91940311061709));
#359874=CARTESIAN_POINT('Ctrl Pts',(-0.775129142386704,-1.29905433022896,
-3.93037524241151));
#359875=CARTESIAN_POINT('Ctrl Pts',(-1.0850704461416,-1.0545952725511,-3.95207782972111));
#359876=CARTESIAN_POINT('Ctrl Pts',(-1.21512345799834,-0.901650532435833,
-3.96240830375363));
#359877=CARTESIAN_POINT('Ctrl Pts',(-1.40419865894282,-0.560954377034411,
-3.9813358679426));
#359878=CARTESIAN_POINT('Ctrl Pts',(-1.46410683422466,-0.377903713047335,
-3.99150534927522));
#359879=CARTESIAN_POINT('Ctrl Pts',(-1.51302559794633,0.00812305449483835,
-4.01295128080534));
#359880=CARTESIAN_POINT('Ctrl Pts',(-1.49870712012392,0.207835929291366,
-4.02404644051625));
#359881=CARTESIAN_POINT('Ctrl Pts',(-1.39430286120284,0.586210525188623,
-4.04506725139943));
#359882=CARTESIAN_POINT('Ctrl Pts',(-1.30678759085172,0.761592770298813,
-4.0541158407846));
#359883=CARTESIAN_POINT('Ctrl Pts',(-1.07041521160284,1.06840943409679,
-4.07401099728912));
#359884=CARTESIAN_POINT('Ctrl Pts',(-0.924144716585857,1.19717501877484,
-4.08462526155845));
#359885=CARTESIAN_POINT('Ctrl Pts',(-0.584243801589745,1.39605139479538,
-4.10650309573436));
#359886=CARTESIAN_POINT('Ctrl Pts',(-0.39235336545844,1.46163492695531,
-4.11755719342952));
#359887=CARTESIAN_POINT('Ctrl Pts',(-0.00444466178164925,1.51202609255691,
-4.13762021423696));
#359888=CARTESIAN_POINT('Ctrl Pts',(0.187267707385404,1.5003931503397,-4.14649900092975));
#359889=CARTESIAN_POINT('Ctrl Pts',(0.560989217050382,1.4047981157727,-4.16713510307386));
#359890=CARTESIAN_POINT('Ctrl Pts',(0.73898084414497,1.3198739653424,-4.17805773340386));
#359891=CARTESIAN_POINT('Ctrl Pts',(1.05510406697226,1.08455338950986,-4.19980390171558));
#359892=CARTESIAN_POINT('Ctrl Pts',(1.18939206035747,0.93534677759051,-4.21040946391861));
#359893=CARTESIAN_POINT('Ctrl Pts',(1.38764837771989,0.6005357697735,-4.22924838120778));
#359894=CARTESIAN_POINT('Ctrl Pts',(1.45260179965292,0.419773285277553,
-4.23917926192909));
#359895=CARTESIAN_POINT('Ctrl Pts',(1.51253535323791,0.0363127431133576,
-4.26048262538265));
#359896=CARTESIAN_POINT('Ctrl Pts',(1.50415187691205,-0.163133846561529,
-4.2715629914757));
#359897=CARTESIAN_POINT('Ctrl Pts',(1.41099361663282,-0.545336891269971,
-4.2927964939595));
#359898=CARTESIAN_POINT('Ctrl Pts',(1.32791096548009,-0.72452520745869,
-4.3020698874256));
#359899=CARTESIAN_POINT('Ctrl Pts',(1.09943657015848,-1.03842500385281,
-4.32178180568448));
#359900=CARTESIAN_POINT('Ctrl Pts',(0.957189594028571,-1.17083620866552,
-4.33230375553705));
#359901=CARTESIAN_POINT('Ctrl Pts',(0.623996435521955,-1.37865567349936,
-4.3541072817621));
#359902=CARTESIAN_POINT('Ctrl Pts',(0.434652990837125,-1.44953602151726,
-4.36518597104799));
#359903=CARTESIAN_POINT('Ctrl Pts',(0.158428898702364,-1.49372931639775,
-4.37970340040167));
#359904=CARTESIAN_POINT('Ctrl Pts',(0.0791936740651888,-1.5,-4.38368979258003));
#359905=CARTESIAN_POINT('Ctrl Pts',(3.2751579226442E-14,-1.5,-4.3875));
#359906=CARTESIAN_POINT('Origin',(0.,1.30104260698261E-15,-17.7));
#359907=CARTESIAN_POINT('',(-2.30626176757078E-16,-1.5,-4.95));
#359908=CARTESIAN_POINT('',(-1.78584683734892E-16,-1.5,-4.8875));
#359909=CARTESIAN_POINT('',(-1.83697019872103E-16,-1.5,-17.7));
#359910=CARTESIAN_POINT('Ctrl Pts',(-2.77555333642053E-16,-1.5,-4.95));
#359911=CARTESIAN_POINT('Ctrl Pts',(0.0824958291875462,-1.5,-4.94603091756763));
#359912=CARTESIAN_POINT('Ctrl Pts',(0.16502570294818,-1.49319553879669,
-4.9418711843537));
#359913=CARTESIAN_POINT('Ctrl Pts',(0.444096067626895,-1.44665240227896,
-4.92715154026959));
#359914=CARTESIAN_POINT('Ctrl Pts',(0.632848634143494,-1.37459550558921,
-4.91606859771527));
#359915=CARTESIAN_POINT('Ctrl Pts',(0.964504827724244,-1.16479808605149,
-4.89428407556348));
#359916=CARTESIAN_POINT('Ctrl Pts',(1.10583642355268,-1.03158532803245,
-4.88378390159935));
#359917=CARTESIAN_POINT('Ctrl Pts',(1.33252634451301,-0.716098755421027,
-4.86411376178606));
#359918=CARTESIAN_POINT('Ctrl Pts',(1.41460159353572,-0.536039844954454,
-4.85477999138629));
#359919=CARTESIAN_POINT('Ctrl Pts',(1.50520018725126,-0.152988353758026,
-4.83349935298649));
#359920=CARTESIAN_POINT('Ctrl Pts',(1.51224315648876,0.0463741466220205,
-4.82242365852093));
#359921=CARTESIAN_POINT('Ctrl Pts',(1.44982998827206,0.42920448401609,-4.80115530644348));
#359922=CARTESIAN_POINT('Ctrl Pts',(1.38374422633269,0.609450013770549,
-4.79131292474764));
#359923=CARTESIAN_POINT('Ctrl Pts',(1.18339834352113,0.94292020681763,-4.77241071804865));
#359924=CARTESIAN_POINT('Ctrl Pts',(1.04815459284978,1.09127271927741,-4.76178289693674));
#359925=CARTESIAN_POINT('Ctrl Pts',(0.730623388172348,1.32450073202695,
-4.74002711381898));
#359926=CARTESIAN_POINT('Ctrl Pts',(0.5522144858791,1.40825391101116,-4.72911693431124));
#359927=CARTESIAN_POINT('Ctrl Pts',(0.177928023099586,1.50154238307282,
-4.70851772202843));
#359928=CARTESIAN_POINT('Ctrl Pts',(-0.0139591409807751,1.51198141638455,
-4.69966120763815));
#359929=CARTESIAN_POINT('Ctrl Pts',(-0.401514993380857,1.45912695278427,
-4.67954673845126));
#359930=CARTESIAN_POINT('Ctrl Pts',(-0.592867515187272,1.39239251750419,
-4.66848655164));
#359931=CARTESIAN_POINT('Ctrl Pts',(-0.931339951890241,1.19156772223471,
-4.6466233224011));
#359932=CARTESIAN_POINT('Ctrl Pts',(-1.07674957092274,1.06200494067013,
-4.63602833268893));
#359933=CARTESIAN_POINT('Ctrl Pts',(-1.31142404779312,0.753657216867543,
-4.6161723371061));
#359934=CARTESIAN_POINT('Ctrl Pts',(-1.39798967723732,0.577463336149325,
-4.60708129645266));
#359935=CARTESIAN_POINT('Ctrl Pts',(-1.49998770387374,0.198255910766289,
-4.58601421726472));
#359936=CARTESIAN_POINT('Ctrl Pts',(-1.51303031281888,-0.00141426859624101,
-4.57492142952236));
#359937=CARTESIAN_POINT('Ctrl Pts',(-1.46174252827966,-0.386891834351265,
-4.55350600920264));
#359938=CARTESIAN_POINT('Ctrl Pts',(-1.40075443310616,-0.569462491014262,
-4.54336319494358));
#359939=CARTESIAN_POINT('Ctrl Pts',(-1.2097054101922,-0.908902260595766,
-4.52450542996683));
#359940=CARTESIAN_POINT('Ctrl Pts',(-1.07875028277293,-1.06105747797526,
-4.51409424501289));
#359941=CARTESIAN_POINT('Ctrl Pts',(-0.767453057130266,-1.30358685489508,
-4.49238002312433));
#359942=CARTESIAN_POINT('Ctrl Pts',(-0.59095150297832,-1.39251717571052,
-4.48141780145151));
#359943=CARTESIAN_POINT('Ctrl Pts',(-0.271091858127589,-1.48157818723245,
-4.46355463012667));
#359944=CARTESIAN_POINT('Ctrl Pts',(-0.1357462741014,-1.5,-4.45653109565784));
#359945=CARTESIAN_POINT('Ctrl Pts',(1.94948224230274E-13,-1.5,-4.44999999999999));
#359946=CARTESIAN_POINT('Ctrl Pts',(3.19883008970123E-14,-1.5,-4.3875));
#359947=CARTESIAN_POINT('Ctrl Pts',(-0.110913948001448,-1.5,-4.3928363498113));
#359948=CARTESIAN_POINT('Ctrl Pts',(-0.22171316120533,-1.48770112800956,
-4.39850881477519));
#359949=CARTESIAN_POINT('Ctrl Pts',(-0.520412566157265,-1.42025452881046,
-4.41475351324092));
#359950=CARTESIAN_POINT('Ctrl Pts',(-0.700262820478156,-1.34073678233728,
-4.42561538892734));
#359951=CARTESIAN_POINT('Ctrl Pts',(-1.02275295061583,-1.11512001893908,
-4.44739833486446));
#359952=CARTESIAN_POINT('Ctrl Pts',(-1.16139496410988,-0.969898058418966,
-4.45810269519655));
#359953=CARTESIAN_POINT('Ctrl Pts',(-1.36924497449003,-0.641294126202712,
-4.47723077048956));
#359954=CARTESIAN_POINT('Ctrl Pts',(-1.43939885340151,-0.462875501925603,
-4.48678469433752));
#359955=CARTESIAN_POINT('Ctrl Pts',(-1.51065089300875,-0.0823363359099725,
-4.50792575911617));
#359956=CARTESIAN_POINT('Ctrl Pts',(-1.50838929550509,0.116653856281524,
-4.51898076979347));
#359957=CARTESIAN_POINT('Ctrl Pts',(-1.42698523896123,0.502681634254046,
-4.54042675745861));
#359958=CARTESIAN_POINT('Ctrl Pts',(-1.34852730843035,0.685879509405817,
-4.55000449155034));
#359959=CARTESIAN_POINT('Ctrl Pts',(-1.12820822467234,1.00699066427407,
-4.56952435271185));
#359960=CARTESIAN_POINT('Ctrl Pts',(-0.990161090964451,1.1429983335144,
-4.57994413934133));
#359961=CARTESIAN_POINT('Ctrl Pts',(-0.664051435313271,1.359727791393,-4.60165436018314));
#359962=CARTESIAN_POINT('Ctrl Pts',(-0.477452246906336,1.43592323106179,
-4.61274865781205));
#359963=CARTESIAN_POINT('Ctrl Pts',(-0.0930687907855808,1.50933861512221,
-4.63328163169123));
#359964=CARTESIAN_POINT('Ctrl Pts',(0.10039406181527,1.50886913682122,-4.64208384663953));
#359965=CARTESIAN_POINT('Ctrl Pts',(0.479189862593641,1.43461329576912,
-4.66237133035325));
#359966=CARTESIAN_POINT('Ctrl Pts',(0.660746812570658,1.36056626338781,
-4.67316335519238));
#359967=CARTESIAN_POINT('Ctrl Pts',(0.989336327789165,1.14487714546879,
-4.69496399000104));
#359968=CARTESIAN_POINT('Ctrl Pts',(1.13223308767084,1.00379293970986,-4.7057581192819));
#359969=CARTESIAN_POINT('Ctrl Pts',(1.34966095067724,0.681520941085277,
-4.72517112218003));
#359970=CARTESIAN_POINT('Ctrl Pts',(1.4250185150892,0.505369135961604,-4.73442393689107));
#359971=CARTESIAN_POINT('Ctrl Pts',(1.50740755905354,0.12781366438924,-4.75539924086731));
#359972=CARTESIAN_POINT('Ctrl Pts',(1.51117028761309,-0.0705449898243242,
-4.7664191661014));
#359973=CARTESIAN_POINT('Ctrl Pts',(1.44150798589776,-0.460208330221321,
-4.78806712945679));
#359974=CARTESIAN_POINT('Ctrl Pts',(1.36767342503713,-0.647437735766871,
-4.79801549654008));
#359975=CARTESIAN_POINT('Ctrl Pts',(1.15540391526562,-0.97556578511997,
-4.81734298612827));
#359976=CARTESIAN_POINT('Ctrl Pts',(1.02153769413881,-1.11495558673436,
-4.82765556662891));
#359977=CARTESIAN_POINT('Ctrl Pts',(0.702557269234278,-1.34015190852106,
-4.84925797286061));
#359978=CARTESIAN_POINT('Ctrl Pts',(0.518771176498625,-1.42143586031683,
-4.86035827292002));
#359979=CARTESIAN_POINT('Ctrl Pts',(0.217682547012256,-1.48814623858313,
-4.87669747242329));
#359980=CARTESIAN_POINT('Ctrl Pts',(0.108887916867443,-1.5,-4.88226112765709));
#359981=CARTESIAN_POINT('Ctrl Pts',(5.20417042793042E-16,-1.5,-4.8875));
#359982=CARTESIAN_POINT('Origin',(0.,1.30104260698261E-15,-17.7));
#359983=CARTESIAN_POINT('',(-1.6606372482269E-14,-1.5,-5.45));
#359984=CARTESIAN_POINT('',(-1.15641779244756E-13,-1.5,-5.38750000000002));
#359985=CARTESIAN_POINT('',(-1.83697019872103E-16,-1.5,-17.7));
#359986=CARTESIAN_POINT('Ctrl Pts',(-3.49373308061729E-14,-1.5,-5.45));
#359987=CARTESIAN_POINT('Ctrl Pts',(0.112003054863257,-1.5,-5.44461125051039));
#359988=CARTESIAN_POINT('Ctrl Pts',(0.223888553312252,-1.48745840617422,
-5.43887977935007));
#359989=CARTESIAN_POINT('Ctrl Pts',(0.527484059848593,-1.41820836785807,
-5.42234942155599));
#359990=CARTESIAN_POINT('Ctrl Pts',(0.71065598432425,-1.33585682220828,
-5.41124901529594));
#359991=CARTESIAN_POINT('Ctrl Pts',(1.0280958134585,-1.1088922984854,-5.38967161429235));
#359992=CARTESIAN_POINT('Ctrl Pts',(1.16106421329996,-0.968800792091161,
-5.37938273843899));
#359993=CARTESIAN_POINT('Ctrl Pts',(1.37161220704221,-0.639185045545452,
-5.36009675040735));
#359994=CARTESIAN_POINT('Ctrl Pts',(1.44444942378393,-0.451084517844767,
-5.35006025099132));
#359995=CARTESIAN_POINT('Ctrl Pts',(1.51158275655079,-0.0606628262206041,
-5.3283701570122));
#359996=CARTESIAN_POINT('Ctrl Pts',(1.50653511735836,0.137537473385722,
-5.31735902925629));
#359997=CARTESIAN_POINT('Ctrl Pts',(1.42176877315086,0.51444241460095,-5.29641986585545));
#359998=CARTESIAN_POINT('Ctrl Pts',(1.34528814091645,0.690115321675696,
-5.28722200247804));
#359999=CARTESIAN_POINT('Ctrl Pts',(1.12579830690998,1.01100565571827,-5.26774817252563));
#360000=CARTESIAN_POINT('Ctrl Pts',(0.981998413662409,1.15117848208361,
-5.25693590731471));
#360001=CARTESIAN_POINT('Ctrl Pts',(0.652130702799262,1.36469994382362,
-5.23513398796106));
#360002=CARTESIAN_POINT('Ctrl Pts',(0.470226250634372,1.43756025114342,
-5.22435820850016));
#360003=CARTESIAN_POINT('Ctrl Pts',(0.0908983809121798,1.50949658439628,
-5.20410955637965));
#360004=CARTESIAN_POINT('Ctrl Pts',(-0.102771112168562,1.50873485121521,
-5.1952980573163));
#360005=CARTESIAN_POINT('Ctrl Pts',(-0.486735105734459,1.43278497407186,
-5.17471486225306));
#360006=CARTESIAN_POINT('Ctrl Pts',(-0.672716466221491,1.35544265410054,
-5.16361843209763));
#360007=CARTESIAN_POINT('Ctrl Pts',(-0.997249614247433,1.13679935361176,
-5.14193089871957));
#360008=CARTESIAN_POINT('Ctrl Pts',(-1.13436838857621,1.00002407254916,
-5.13153445525092));
#360009=CARTESIAN_POINT('Ctrl Pts',(-1.35289485609955,0.677341621182997,
-5.11205719425328));
#360010=CARTESIAN_POINT('Ctrl Pts',(-1.43032859685897,0.493252080276599,
-5.10240289334864));
#360011=CARTESIAN_POINT('Ctrl Pts',(-1.50912976100891,0.106402252737442,
-5.08091123626313));
#360012=CARTESIAN_POINT('Ctrl Pts',(-1.5100477769608,-0.0924628700686707,
-5.06986317388501));
#360013=CARTESIAN_POINT('Ctrl Pts',(-1.43631256065921,-0.47234599370819,
-5.04875855590504));
#360014=CARTESIAN_POINT('Ctrl Pts',(-1.36500630795286,-0.650255823971049,
-5.03927790150147));
#360015=CARTESIAN_POINT('Ctrl Pts',(-1.15503253800454,-0.977467677855987,
-5.02008631562113));
#360016=CARTESIAN_POINT('Ctrl Pts',(-1.01543885274056,-1.12178581026751,
-5.00936127429601));
#360017=CARTESIAN_POINT('Ctrl Pts',(-0.691573620226702,-1.34522157913518,
-4.98757275189638));
#360018=CARTESIAN_POINT('Ctrl Pts',(-0.511331921199436,-1.42353235932602,
-4.97672556965892));
#360019=CARTESIAN_POINT('Ctrl Pts',(-0.215424642031656,-1.48839116583224,
-4.96068709053796));
#360020=CARTESIAN_POINT('Ctrl Pts',(-0.10775705142673,-1.5,-4.95518446355402));
#360021=CARTESIAN_POINT('Ctrl Pts',(1.38777878078145E-16,-1.5,-4.95));
#360022=CARTESIAN_POINT('Ctrl Pts',(-1.73472347597681E-16,-1.5,-4.8875));
#360023=CARTESIAN_POINT('Ctrl Pts',(-0.0829656057906737,-1.5,-4.89149168456973));
#360024=CARTESIAN_POINT('Ctrl Pts',(-0.165966768441516,-1.49311782380902,
-4.8956762514306));
#360025=CARTESIAN_POINT('Ctrl Pts',(-0.439227699570691,-1.44727789145615,
-4.91009685556371));
#360026=CARTESIAN_POINT('Ctrl Pts',(-0.622270263803716,-1.37851388291316,
-4.92081360638988));
#360027=CARTESIAN_POINT('Ctrl Pts',(-0.956428468696735,-1.17251273596787,
-4.9426130546006));
#360028=CARTESIAN_POINT('Ctrl Pts',(-1.10329198121541,-1.03552308732051,
-4.95348429665915));
#360029=CARTESIAN_POINT('Ctrl Pts',(-1.32985979386102,-0.719427485276971,
-4.97316547901764));
#360030=CARTESIAN_POINT('Ctrl Pts',(-1.41020596056088,-0.545375198674591,
-4.98220137785146));
#360031=CARTESIAN_POINT('Ctrl Pts',(-1.50308025472817,-0.170724223102751,
-5.00301532093878));
#360032=CARTESIAN_POINT('Ctrl Pts',(-1.51250478259511,0.0268736369112289,
-5.01399297982845));
#360033=CARTESIAN_POINT('Ctrl Pts',(-1.4544187016606,0.417393905079721,
-5.03568855028225));
#360034=CARTESIAN_POINT('Ctrl Pts',(-1.38634030608345,0.606270546843181,
-5.04597385278133));
#360035=CARTESIAN_POINT('Ctrl Pts',(-1.1846371610216,0.939735762001864,
-5.06494122251611));
#360036=CARTESIAN_POINT('Ctrl Pts',(-1.05551747552987,1.08274092934074,
-5.07512586204022));
#360037=CARTESIAN_POINT('Ctrl Pts',(-0.744718802559787,1.31709337644969,
-5.09658896036294));
#360038=CARTESIAN_POINT('Ctrl Pts',(-0.564218319239696,1.40392501056514,
-5.10768528375229));
#360039=CARTESIAN_POINT('Ctrl Pts',(-0.184060619143443,1.50125952084737,
-5.12867936602277));
#360040=CARTESIAN_POINT('Ctrl Pts',(0.0114524548753373,1.51245558484093,
-5.13770501802434));
#360041=CARTESIAN_POINT('Ctrl Pts',(0.395073662217544,1.45987301241593,
-5.15762262897996));
#360042=CARTESIAN_POINT('Ctrl Pts',(0.579570311002179,1.39692338827322,
-5.16824782880396));
#360043=CARTESIAN_POINT('Ctrl Pts',(0.921186075424326,1.20072738827768,
-5.19013371382177));
#360044=CARTESIAN_POINT('Ctrl Pts',(1.07350611906356,1.06673918590758,-5.20118410984856));
#360045=CARTESIAN_POINT('Ctrl Pts',(1.30997188084597,0.755112591702573,
-5.22121736840029));
#360046=CARTESIAN_POINT('Ctrl Pts',(1.39510822563865,0.583010368031759,
-5.23011053510939));
#360047=CARTESIAN_POINT('Ctrl Pts',(1.49786420173597,0.2111788391675,-5.25076784226851));
#360048=CARTESIAN_POINT('Ctrl Pts',(1.51260656519268,0.0144454872595902,
-5.26169747293006));
#360049=CARTESIAN_POINT('Ctrl Pts',(1.46542190804958,-0.37687821172446,
-5.28343767842918));
#360050=CARTESIAN_POINT('Ctrl Pts',(1.40264741672388,-0.567543360101546,
-5.29403018667235));
#360051=CARTESIAN_POINT('Ctrl Pts',(1.21054777309602,-0.905983865282138,
-5.31283243696015));
#360052=CARTESIAN_POINT('Ctrl Pts',(1.08589197369939,-1.05219972926723,
-5.32281610164694));
#360053=CARTESIAN_POINT('Ctrl Pts',(0.7827393931996,-1.2947706165297,-5.34413961717843));
#360054=CARTESIAN_POINT('Ctrl Pts',(0.605394774261556,-1.38658325786445,
-5.35522246528355));
#360055=CARTESIAN_POINT('Ctrl Pts',(0.280057864526816,-1.48033499714547,
-5.37347945963131));
#360056=CARTESIAN_POINT('Ctrl Pts',(0.140251536173992,-1.50000000000002,
-5.38075214481965));
#360057=CARTESIAN_POINT('Ctrl Pts',(-2.30961083591552E-13,-1.5,-5.38750000000002));
#360058=CARTESIAN_POINT('Origin',(0.,1.30104260698261E-15,-17.7));
#360059=CARTESIAN_POINT('',(-1.1555473864945E-13,-1.5,-5.95000000000001));
#360060=CARTESIAN_POINT('',(-4.9687592688114E-14,-1.5,-5.88750000000001));
#360061=CARTESIAN_POINT('',(-1.83697019872103E-16,-1.5,-17.7));
#360062=CARTESIAN_POINT('Ctrl Pts',(-2.30475361018279E-13,-1.5,-5.95000000000001));
#360063=CARTESIAN_POINT('Ctrl Pts',(0.143779545010459,-1.50000000000002,
-5.94308240341535));
#360064=CARTESIAN_POINT('Ctrl Pts',(0.287058207428915,-1.47933314649523,
-5.93561482629158));
#360065=CARTESIAN_POINT('Ctrl Pts',(0.614977937901949,-1.3823400805608,
-5.91714352907164));
#360066=CARTESIAN_POINT('Ctrl Pts',(0.791562999441172,-1.28937447526274,
-5.90606519841215));
#360067=CARTESIAN_POINT('Ctrl Pts',(1.09288206406366,-1.04491758451658,
-5.88477750896878));
#360068=CARTESIAN_POINT('Ctrl Pts',(1.21649528049569,-0.897961460651119,
-5.8748867478139));
#360069=CARTESIAN_POINT('Ctrl Pts',(1.40633352386383,-0.558349785555567,
-5.85601943253082));
#360070=CARTESIAN_POINT('Ctrl Pts',(1.46786090845376,-0.367269115374562,
-5.84540383974299));
#360071=CARTESIAN_POINT('Ctrl Pts',(1.5124652514401,0.0242414874161168,
-5.82365325069906));
#360072=CARTESIAN_POINT('Ctrl Pts',(1.49646765222344,0.220749313774995,
-5.81273614923468));
#360073=CARTESIAN_POINT('Ctrl Pts',(1.39137263960931,0.591902024894406,
-5.79211655417249));
#360074=CARTESIAN_POINT('Ctrl Pts',(1.30508888504187,0.763546397778705,
-5.78324816276405));
#360075=CARTESIAN_POINT('Ctrl Pts',(1.06661784566857,1.07360181688628,-5.76316206900194));
#360076=CARTESIAN_POINT('Ctrl Pts',(0.913548925461279,1.20652625226537,
-5.75210519171755));
#360077=CARTESIAN_POINT('Ctrl Pts',(0.570929032520845,1.40046132775147,
-5.73023379900248));
#360078=CARTESIAN_POINT('Ctrl Pts',(0.386162258818603,1.46224032027028,
-5.71962812033243));
#360079=CARTESIAN_POINT('Ctrl Pts',(0.0020511110498958,1.51253564557089,
-5.69975047174939));
#360080=CARTESIAN_POINT('Ctrl Pts',(-0.193693773628809,1.50008576426874,
-5.69068328631201));
#360081=CARTESIAN_POINT('Ctrl Pts',(-0.57336323662806,1.40019673354727,
-5.66964173545871));
#360082=CARTESIAN_POINT('Ctrl Pts',(-0.753177752293143,1.31225510532934,
-5.65854758253404));
#360083=CARTESIAN_POINT('Ctrl Pts',(-1.06228592207914,1.07608047106221,
-5.63711520227373));
#360084=CARTESIAN_POINT('Ctrl Pts',(-1.19043130071785,0.932361348999917,
-5.6269576070343));
#360085=CARTESIAN_POINT('Ctrl Pts',(-1.39001769707367,0.597784099544736,
-5.60806118957755));
#360086=CARTESIAN_POINT('Ctrl Pts',(-1.45693782306663,0.408508818217555,
-5.59769493434537));
#360087=CARTESIAN_POINT('Ctrl Pts',(-1.51262413695321,0.017766922124366,
-5.57598705122908));
#360088=CARTESIAN_POINT('Ctrl Pts',(-1.50202431525068,-0.179652463492326,
-5.56501930758371));
#360089=CARTESIAN_POINT('Ctrl Pts',(-1.40696945108533,-0.553688053995312,
-5.54423955255577));
#360090=CARTESIAN_POINT('Ctrl Pts',(-1.32557396250141,-0.727307733847383,
-5.53524038106649));
#360091=CARTESIAN_POINT('Ctrl Pts',(-1.09709073135385,-1.04209159986641,
-5.51550348020415));
#360092=CARTESIAN_POINT('Ctrl Pts',(-0.949408156168324,-1.17820536526802,
-5.50461716106483));
#360093=CARTESIAN_POINT('Ctrl Pts',(-0.614115170311688,-1.38215057165094,
-5.48282022513961));
#360094=CARTESIAN_POINT('Ctrl Pts',(-0.430779341403753,-1.44980022913289,
-5.47212031880633));
#360095=CARTESIAN_POINT('Ctrl Pts',(-0.160222428209957,-1.49358660537016,
-5.45788685502222));
#360096=CARTESIAN_POINT('Ctrl Pts',(-0.0800898247096889,-1.5,-5.45385332348796));
#360097=CARTESIAN_POINT('Ctrl Pts',(-3.30290479446659E-14,-1.5,-5.45));
#360098=CARTESIAN_POINT('Ctrl Pts',(-2.31099861469641E-13,-1.5,-5.38750000000002));
#360099=CARTESIAN_POINT('Ctrl Pts',(-0.0544776219942335,-1.49999999999999,
-5.39012105581027));
#360100=CARTESIAN_POINT('Ctrl Pts',(-0.109014443643155,-1.49703241159562,
-5.39282739287651));
#360101=CARTESIAN_POINT('Ctrl Pts',(-0.354873801016226,-1.47009450804401,
-5.40540458182202));
#360102=CARTESIAN_POINT('Ctrl Pts',(-0.540528018569387,-1.41241816543501,
-5.41593899515675));
#360103=CARTESIAN_POINT('Ctrl Pts',(-0.886546361924947,-1.22642949223115,
-5.43775316249693));
#360104=CARTESIAN_POINT('Ctrl Pts',(-1.0421788809374,-1.09725665011376,
-5.4488291700624));
#360105=CARTESIAN_POINT('Ctrl Pts',(-1.28763428030429,-0.792732570084186,
-5.46909765069365));
#360106=CARTESIAN_POINT('Ctrl Pts',(-1.37793947069467,-0.622665885247676,
-5.47790745081961));
#360107=CARTESIAN_POINT('Ctrl Pts',(-1.49114532153187,-0.253900482485394,
-5.49839441763973));
#360108=CARTESIAN_POINT('Ctrl Pts',(-1.51148259208429,-0.0582363393241967,
-5.50926464781536));
#360109=CARTESIAN_POINT('Ctrl Pts',(-1.47583816671478,0.333790424102859,
-5.53104391245019));
#360110=CARTESIAN_POINT('Ctrl Pts',(-1.41866188921323,0.526248347454362,
-5.54173601930305));
#360111=CARTESIAN_POINT('Ctrl Pts',(-1.23668878520016,0.869885949917901,
-5.56082699721769));
#360112=CARTESIAN_POINT('Ctrl Pts',(-1.11665679439315,1.01941802933088,
-5.57042532574517));
#360113=CARTESIAN_POINT('Ctrl Pts',(-0.821671034046308,1.2703276538985,
-5.59158754655066));
#360114=CARTESIAN_POINT('Ctrl Pts',(-0.647757502348754,1.36721878187072,
-5.60264638546722));
#360115=CARTESIAN_POINT('Ctrl Pts',(-0.272405721158414,1.48817955152494,
-5.62406552783909));
#360116=CARTESIAN_POINT('Ctrl Pts',(-0.074673845245232,1.51105565975916,
-5.63360015128558));
#360117=CARTESIAN_POINT('Ctrl Pts',(0.313302899921245,1.47944286236704,
-5.65314482440157));
#360118=CARTESIAN_POINT('Ctrl Pts',(0.499991719515697,1.42719956174785,
-5.66357809721717));
#360119=CARTESIAN_POINT('Ctrl Pts',(0.850224187064647,1.25178798296355,
-5.68530120852382));
#360120=CARTESIAN_POINT('Ctrl Pts',(1.00910707112899,1.12763903021001,-5.69639404686843));
#360121=CARTESIAN_POINT('Ctrl Pts',(1.26371524628725,0.830508905492942,
-5.7168975029827));
#360122=CARTESIAN_POINT('Ctrl Pts',(1.35935615291476,0.662474592684624,
-5.725695855962));
#360123=CARTESIAN_POINT('Ctrl Pts',(1.48311189740595,0.296891183797457,
-5.74600604534461));
#360124=CARTESIAN_POINT('Ctrl Pts',(1.50905759985487,0.102466567398649,
-5.75680741292233));
#360125=CARTESIAN_POINT('Ctrl Pts',(1.48508337510517,-0.289923734161056,
-5.77860687412009));
#360126=CARTESIAN_POINT('Ctrl Pts',(1.4336222203805,-0.484022734140751,
-5.78939015189674));
#360127=CARTESIAN_POINT('Ctrl Pts',(1.26193465712244,-0.832812097053497,
-5.80876733872522));
#360128=CARTESIAN_POINT('Ctrl Pts',(1.14648703796586,-0.985720116124361,
-5.81805406433748));
#360129=CARTESIAN_POINT('Ctrl Pts',(0.859679290268612,-1.24482706900436,
-5.83905052389015));
#360130=CARTESIAN_POINT('Ctrl Pts',(0.689321243795664,-1.34665430569042,
-5.85007541357502));
#360131=CARTESIAN_POINT('Ctrl Pts',(0.342146130245309,-1.47055648458404,
-5.8702206112052));
#360132=CARTESIAN_POINT('Ctrl Pts',(0.171606945087988,-1.50000000000001,
-5.87924355700489));
#360133=CARTESIAN_POINT('Ctrl Pts',(-9.70404312461426E-14,-1.5,-5.88750000000001));
#360134=CARTESIAN_POINT('Origin',(0.,1.30104260698261E-15,-17.7));
#360135=CARTESIAN_POINT('',(-4.96354202156783E-14,-1.5,-6.45));
#360136=CARTESIAN_POINT('',(-1.14379898485726E-8,-1.5,-6.38750000110063));
#360137=CARTESIAN_POINT('',(-1.83697019872103E-16,-1.5,-17.7));
#360138=CARTESIAN_POINT('Ctrl Pts',(-9.71098201851817E-14,-1.5,-6.45));
#360139=CARTESIAN_POINT('Ctrl Pts',(0.175083992004288,-1.50000000000001,
-6.44157626750713));
#360140=CARTESIAN_POINT('Ctrl Pts',(0.349012600883344,-1.46935064435116,
-6.43235675242051));
#360141=CARTESIAN_POINT('Ctrl Pts',(0.698448698264349,-1.34192367911046,
-6.4120048624232));
#360142=CARTESIAN_POINT('Ctrl Pts',(0.868000054047873,-1.23901878590965,
-6.40098884975903));
#360143=CARTESIAN_POINT('Ctrl Pts',(1.15298812289309,-0.978107547609196,
-6.3800298205065));
#360144=CARTESIAN_POINT('Ctrl Pts',(1.26742086259517,-0.824439858150199,
-6.37080221434165));
#360145=CARTESIAN_POINT('Ctrl Pts',(1.43679909501675,-0.474511758410586,
-6.35136176435611));
#360146=CARTESIAN_POINT('Ctrl Pts',(1.48697426927758,-0.280069300941365,
-6.34055940560782));
#360147=CARTESIAN_POINT('Ctrl Pts',(1.50833762378054,0.112354555701641,
-6.31875808023877));
#360148=CARTESIAN_POINT('Ctrl Pts',(1.48114395458428,0.306480120986939,
-6.30797332661181));
#360149=CARTESIAN_POINT('Ctrl Pts',(1.35502834861227,0.671340068733185,
-6.28770332951479));
#360150=CARTESIAN_POINT('Ctrl Pts',(1.25817688371938,0.83892209174003,-6.27889733877137));
#360151=CARTESIAN_POINT('Ctrl Pts',(1.00151140779071,1.13436656063906,-6.25834172450036));
#360152=CARTESIAN_POINT('Ctrl Pts',(0.841915584426592,1.25736979765705,
-6.2472464102848));
#360153=CARTESIAN_POINT('Ctrl Pts',(0.490774324217669,1.43037919615442,
-6.2255463019011));
#360154=CARTESIAN_POINT('Ctrl Pts',(0.303873417810742,1.48139293571001,
-6.21513697952796));
#360155=CARTESIAN_POINT('Ctrl Pts',(-0.0845860546829974,1.51058699485786,
-6.19563626835606));
#360156=CARTESIAN_POINT('Ctrl Pts',(-0.282585859991757,1.48633548906874,
-6.18602451172392));
#360157=CARTESIAN_POINT('Ctrl Pts',(-0.657333674027615,1.36262073996644,
-6.16455792830621));
#360158=CARTESIAN_POINT('Ctrl Pts',(-0.830444938790861,1.26458819942875,
-6.15350598257092));
#360159=CARTESIAN_POINT('Ctrl Pts',(-1.123561669514,1.01179206850437,-6.13238128254078));
#360160=CARTESIAN_POINT('Ctrl Pts',(-1.24254226875119,0.861493674918274,
-6.12286075971764));
#360161=CARTESIAN_POINT('Ctrl Pts',(-1.42217784205403,0.516673906685671,
-6.10370410592694));
#360162=CARTESIAN_POINT('Ctrl Pts',(-1.47805742018399,0.323827072437385,
-6.09299039291315));
#360163=CARTESIAN_POINT('Ctrl Pts',(-1.51104430075671,-0.0683131724668348,
-6.0712048237518));
#360164=CARTESIAN_POINT('Ctrl Pts',(-1.4894255194257,-0.263709025874027,
-6.06034949856251));
#360165=CARTESIAN_POINT('Ctrl Pts',(-1.3738163973829,-0.631757166629868,
-6.03990237963163));
#360166=CARTESIAN_POINT('Ctrl Pts',(-1.28230645468386,-0.801359093595513,
-6.0311016899108));
#360167=CARTESIAN_POINT('Ctrl Pts',(-1.03477263294274,-1.10421895362498,
-6.01077943946978));
#360168=CARTESIAN_POINT('Ctrl Pts',(-0.878390960016799,-1.23226158064842,
-5.99969878308356));
#360169=CARTESIAN_POINT('Ctrl Pts',(-0.531391503965922,-1.41586444003544,
-5.97790368454285));
#360170=CARTESIAN_POINT('Ctrl Pts',(-0.345489435132126,-1.47231253454326,
-5.96739146446062));
#360171=CARTESIAN_POINT('Ctrl Pts',(-0.102728496078983,-1.49736480502456,
-5.95501572693244));
#360172=CARTESIAN_POINT('Ctrl Pts',(-0.051335855383024,-1.49999999999999,
-5.9524698974937));
#360173=CARTESIAN_POINT('Ctrl Pts',(-2.30925780279027E-13,-1.5,-5.95000000000001));
#360174=CARTESIAN_POINT('Ctrl Pts',(-9.9191488356356E-14,-1.5,-5.88750000000001));
#360175=CARTESIAN_POINT('Ctrl Pts',(-0.0269718101574132,-1.5,-5.88879768182125));
#360176=CARTESIAN_POINT('Ctrl Pts',(-0.0539680776807263,-1.49927253331153,
-5.89011674775609));
#360177=CARTESIAN_POINT('Ctrl Pts',(-0.272282822061387,-1.48747218509173,
-5.900948208243));
#360178=CARTESIAN_POINT('Ctrl Pts',(-0.459834248908589,-1.44057020960743,
-5.91127461312677));
#360179=CARTESIAN_POINT('Ctrl Pts',(-0.813895030288931,-1.27561647138715,
-5.93289141869728));
#360180=CARTESIAN_POINT('Ctrl Pts',(-0.975814709361218,-1.15646792700745,
-5.94399146467723));
#360181=CARTESIAN_POINT('Ctrl Pts',(-1.23932740362783,-0.866694814313302,
-5.96471897822176));
#360182=CARTESIAN_POINT('Ctrl Pts',(-1.34023526021138,-0.700614022507633,
-5.9735769987496));
#360183=CARTESIAN_POINT('Ctrl Pts',(-1.4741757383099,-0.338179606973961,
-5.99371224405703));
#360184=CARTESIAN_POINT('Ctrl Pts',(-1.5054872376406,-0.145101799609199,
-6.00443878891062));
#360185=CARTESIAN_POINT('Ctrl Pts',(-1.49277552777813,0.2473083510385,-6.0262393528355));
#360186=CARTESIAN_POINT('Ctrl Pts',(-1.44688097502016,0.442826888870478,
-6.03710149382616));
#360187=CARTESIAN_POINT('Ctrl Pts',(-1.28518148216548,0.796493179373089,
-6.05674962107631));
#360188=CARTESIAN_POINT('Ctrl Pts',(-1.17408797917394,0.952692543573725,
-6.0658086808636));
#360189=CARTESIAN_POINT('Ctrl Pts',(-0.895106809654988,1.21951117217202,
-6.08664279721249));
#360190=CARTESIAN_POINT('Ctrl Pts',(-0.728256791418487,1.32591928233535,
-6.09762615329562));
#360191=CARTESIAN_POINT('Ctrl Pts',(-0.360421700012662,1.46957484044234,
-6.11931405955197));
#360192=CARTESIAN_POINT('Ctrl Pts',(-0.162675208069435,1.50434210548157,
-6.12955267136142));
#360193=CARTESIAN_POINT('Ctrl Pts',(0.227015314260759,1.49497783819363,
-6.14856178389453));
#360194=CARTESIAN_POINT('Ctrl Pts',(0.415339942011079,1.45394779639172,
-6.15876228015514));
#360195=CARTESIAN_POINT('Ctrl Pts',(0.77325279948223,1.30055810332152,-6.1802431953466));
#360196=CARTESIAN_POINT('Ctrl Pts',(0.938331290737864,1.18697628345601,
-6.19134058851207));
#360197=CARTESIAN_POINT('Ctrl Pts',(1.21153599193554,0.905412640553713,
-6.21230636812995));
#360198=CARTESIAN_POINT('Ctrl Pts',(1.31827759787906,0.741438308234929,
-6.22130898287587));
#360199=CARTESIAN_POINT('Ctrl Pts',(1.4632278868835,0.382495696924617,-6.24125023905977));
#360200=CARTESIAN_POINT('Ctrl Pts',(1.50027611261485,0.191036499153384,
-6.25188686115817));
#360201=CARTESIAN_POINT('Ctrl Pts',(1.49970970905734,-0.203057380420697,
-6.27378096557895));
#360202=CARTESIAN_POINT('Ctrl Pts',(1.45906238606611,-0.401891328845657,
-6.28482729604701));
#360203=CARTESIAN_POINT('Ctrl Pts',(1.30601490646584,-0.76192210186722,
-6.30482900565931));
#360204=CARTESIAN_POINT('Ctrl Pts',(1.19896038848152,-0.921249982630647,
-6.3137386020422));
#360205=CARTESIAN_POINT('Ctrl Pts',(0.927276772408091,-1.19514856435085,
-6.33441828005174));
#360206=CARTESIAN_POINT('Ctrl Pts',(0.763784138561927,-1.30569906008895,
-6.34535517016904));
#360207=CARTESIAN_POINT('Ctrl Pts',(0.400630272163701,-1.4591064707294,
-6.3670887356748));
#360208=CARTESIAN_POINT('Ctrl Pts',(0.20396914448713,-1.49930646016053,
-6.37766726496482));
#360209=CARTESIAN_POINT('Ctrl Pts',(0.00344368467581672,-1.49999703548051,
-6.38733423329604));
#360210=CARTESIAN_POINT('Ctrl Pts',(0.00172177422024196,-1.50000000001316,
-6.38741716109958));
#360211=CARTESIAN_POINT('Ctrl Pts',(-1.14645005182519E-8,-1.5,-6.38750000055159));
#360212=CARTESIAN_POINT('Origin',(0.,1.30104260698261E-15,-17.7));
#360213=CARTESIAN_POINT('',(-2.30626176757078E-16,-1.5,-6.95));
#360214=CARTESIAN_POINT('',(6.57929491076618E-14,-1.5,-6.8875));
#360215=CARTESIAN_POINT('',(-1.83697019872103E-16,-1.5,-17.7));
#360216=CARTESIAN_POINT('Ctrl Pts',(-2.77555333642053E-16,-1.5,-6.95));
#360217=CARTESIAN_POINT('Ctrl Pts',(0.00515159578593097,-1.5,-6.94975214373219));
#360218=CARTESIAN_POINT('Ctrl Pts',(0.010304272039539,-1.49997346107028,
-6.94950349828783));
#360219=CARTESIAN_POINT('Ctrl Pts',(0.214260531892348,-1.49787153589899,
-6.93963226135011));
#360220=CARTESIAN_POINT('Ctrl Pts',(0.410650232159253,-1.45631954863341,
-6.92902923562202));
#360221=CARTESIAN_POINT('Ctrl Pts',(0.772629447971819,-1.30046493189594,
-6.90728420757178));
#360222=CARTESIAN_POINT('Ctrl Pts',(0.935262174360835,-1.18888880266618,
-6.89636019995208));
#360223=CARTESIAN_POINT('Ctrl Pts',(1.20510378879389,-0.91321930699475,
-6.87571995323359));
#360224=CARTESIAN_POINT('Ctrl Pts',(1.31114101911631,-0.753092043636084,
-6.86683844686865));
#360225=CARTESIAN_POINT('Ctrl Pts',(1.46171506667493,-0.392062181413054,
-6.8467812323007));
#360226=CARTESIAN_POINT('Ctrl Pts',(1.50100567367457,-0.193101237105326,
-6.83572784650583));
#360227=CARTESIAN_POINT('Ctrl Pts',(1.49899449390294,0.200728458918543,
-6.81384841894895));
#360228=CARTESIAN_POINT('Ctrl Pts',(1.46074172941662,0.391823837709976,
-6.80323200901609));
#360229=CARTESIAN_POINT('Ctrl Pts',(1.31346150399244,0.750015710321186,
-6.78333246053769));
#360230=CARTESIAN_POINT('Ctrl Pts',(1.20546573420867,0.913544113679387,
-6.77428843846535));
#360231=CARTESIAN_POINT('Ctrl Pts',(0.930202151523462,1.19333499796725,
-6.75327284416057));
#360232=CARTESIAN_POINT('Ctrl Pts',(0.76447291305119,1.30571788673004,-6.74217744554678));
#360233=CARTESIAN_POINT('Ctrl Pts',(0.405785068228597,1.45662740857059,
-6.72072813740426));
#360234=CARTESIAN_POINT('Ctrl Pts',(0.217318862830531,1.49640270302223,
-6.71055568357896));
#360235=CARTESIAN_POINT('Ctrl Pts',(-0.172280751492315,1.50326942561258,
-6.69162032110099));
#360236=CARTESIAN_POINT('Ctrl Pts',(-0.369786999912835,1.46724472857059,
-6.68129874602062));
#360237=CARTESIAN_POINT('Ctrl Pts',(-0.736576190809934,1.3212977908628,
-6.6595975112426));
#360238=CARTESIAN_POINT('Ctrl Pts',(-0.90265365361906,1.21391640988091,
-6.64862428944928));
#360239=CARTESIAN_POINT('Ctrl Pts',(-1.17993993444525,0.945444154140981,
-6.62782578438337));
#360240=CARTESIAN_POINT('Ctrl Pts',(-1.29009387847771,0.788523511290764,
-6.61880686173835));
#360241=CARTESIAN_POINT('Ctrl Pts',(-1.44961106078853,0.433808503038918,
-6.59910047239102));
#360242=CARTESIAN_POINT('Ctrl Pts',(-1.49428821956553,0.238002628385505,
-6.58822236824361));
#360243=CARTESIAN_POINT('Ctrl Pts',(-1.50455029243796,-0.154368756750338,
-6.56642395795829));
#360244=CARTESIAN_POINT('Ctrl Pts',(-1.4720777523692,-0.34713404641117,
-6.55571477519935));
#360245=CARTESIAN_POINT('Ctrl Pts',(-1.33591987514471,-0.708872612955237,
-6.53561818816913));
#360246=CARTESIAN_POINT('Ctrl Pts',(-1.23384917159286,-0.874528906852802,
-6.52673779297838));
#360247=CARTESIAN_POINT('Ctrl Pts',(-0.968389679515266,-1.16267051032679,
-6.50596193378105));
#360248=CARTESIAN_POINT('Ctrl Pts',(-0.805823049353649,-1.28071119538738,
-6.49486153522228));
#360249=CARTESIAN_POINT('Ctrl Pts',(-0.450961842860782,-1.44335706912135,
-6.47327032652743));
#360250=CARTESIAN_POINT('Ctrl Pts',(-0.263241103996375,-1.48908431124072,
-6.46296840709779));
#360251=CARTESIAN_POINT('Ctrl Pts',(-0.0479753228231705,-1.49942508266729,
-6.45232418372142));
#360252=CARTESIAN_POINT('Ctrl Pts',(-0.0239775839369867,-1.5,-6.45115362204504));
#360253=CARTESIAN_POINT('Ctrl Pts',(-9.90871434114846E-14,-1.5,-6.45));
#360254=CARTESIAN_POINT('Ctrl Pts',(-1.14645056295548E-8,-1.5,-6.38750000055159));
#360255=CARTESIAN_POINT('Ctrl Pts',(-0.188662808098288,-1.49999999855805,
-6.39657704362686));
#360256=CARTESIAN_POINT('Ctrl Pts',(-0.375732974423939,-1.46440555920762,
-6.40656619562707));
#360257=CARTESIAN_POINT('Ctrl Pts',(-0.735347843155412,-1.32227358290303,
-6.42781628451887));
#360258=CARTESIAN_POINT('Ctrl Pts',(-0.903158276318748,-1.21385890059538,
-6.43890158670183));
#360259=CARTESIAN_POINT('Ctrl Pts',(-1.18516837418757,-0.939951322299202,
-6.46007834770329));
#360260=CARTESIAN_POINT('Ctrl Pts',(-1.29731274704456,-0.777883541388106,
-6.46928424770068));
#360261=CARTESIAN_POINT('Ctrl Pts',(-1.45220861002616,-0.422174255720655,
-6.48904587468221));
#360262=CARTESIAN_POINT('Ctrl Pts',(-1.4943732657924,-0.232318949561423,
-6.49959339169105));
#360263=CARTESIAN_POINT('Ctrl Pts',(-1.50477749816427,0.160533971298007,
-6.52141855396102));
#360264=CARTESIAN_POINT('Ctrl Pts',(-1.46991553600497,0.359847718473458,
-6.53249153991521));
#360265=CARTESIAN_POINT('Ctrl Pts',(-1.32743228933234,0.724097389575991,
-6.55272763275424));
#360266=CARTESIAN_POINT('Ctrl Pts',(-1.2246997029697,0.886852632687246,
-6.56154473675361));
#360267=CARTESIAN_POINT('Ctrl Pts',(-0.960848483996669,1.16823777752605,
-6.58205553846858));
#360268=CARTESIAN_POINT('Ctrl Pts',(-0.801045091118743,1.28309300914337,
-6.59293450589369));
#360269=CARTESIAN_POINT('Ctrl Pts',(-0.442985771522919,1.44681577111778,
-6.61470949743918));
#360270=CARTESIAN_POINT('Ctrl Pts',(-0.247541356316228,1.49273587299906,
-6.62538837963571));
#360271=CARTESIAN_POINT('Ctrl Pts',(0.141128398861992,1.50538917073519,
-6.64443974244321));
#360272=CARTESIAN_POINT('Ctrl Pts',(0.33056170368414,1.47542526933006,-6.65408678879133));
#360273=CARTESIAN_POINT('Ctrl Pts',(0.694924367490722,1.34387056049742,
-6.67527149309486));
#360274=CARTESIAN_POINT('Ctrl Pts',(0.865432912391379,1.24094139575771,
-6.68633423275131));
#360275=CARTESIAN_POINT('Ctrl Pts',(1.1566065168039,0.975216686342843,-6.70772457125354));
#360276=CARTESIAN_POINT('Ctrl Pts',(1.27448706127016,0.815139456408861,
-6.71721447464397));
#360277=CARTESIAN_POINT('Ctrl Pts',(1.4396870268363,0.462859443663064,-6.73678558646318));
#360278=CARTESIAN_POINT('Ctrl Pts',(1.48707811155273,0.274803502370941,
-6.74723313875718));
#360279=CARTESIAN_POINT('Ctrl Pts',(1.50874950767428,-0.116454945609269,
-6.76896971920053));
#360280=CARTESIAN_POINT('Ctrl Pts',(1.47985938284906,-0.316094836591576,
-6.7800608242551));
#360281=CARTESIAN_POINT('Ctrl Pts',(1.34833870965213,-0.684586646548388,
-6.80053259147493));
#360282=CARTESIAN_POINT('Ctrl Pts',(1.25003415541057,-0.850935687480155,
-6.80932813941981));
#360283=CARTESIAN_POINT('Ctrl Pts',(0.994214333933481,-1.13988251133932,
-6.82966257698205));
#360284=CARTESIAN_POINT('Ctrl Pts',(0.838278058707002,-1.25899700110724,
-6.84047380034881));
#360285=CARTESIAN_POINT('Ctrl Pts',(0.485704654348464,-1.43304486849454,
-6.86227165915808));
#360286=CARTESIAN_POINT('Ctrl Pts',(0.291674266058639,-1.4847475596941,
-6.87304313643391));
#360287=CARTESIAN_POINT('Ctrl Pts',(0.0621266763099901,-1.49903597661885,
-6.88448415046514));
#360288=CARTESIAN_POINT('Ctrl Pts',(0.0310490691749192,-1.5,-6.88600615096282));
#360289=CARTESIAN_POINT('Ctrl Pts',(1.31769595235196E-13,-1.5,-6.8875));
#360290=CARTESIAN_POINT('Origin',(0.,1.30104260698261E-15,-17.7));
#360291=CARTESIAN_POINT('',(8.22032160180837E-14,-1.5,-7.44999999999999));
#360292=CARTESIAN_POINT('',(8.22728221294406E-14,-1.5,-7.3875));
#360293=CARTESIAN_POINT('',(-1.83697019872103E-16,-1.5,-17.7));
#360294=CARTESIAN_POINT('Ctrl Pts',(1.6459012905604E-13,-1.5,-7.44999999999999));
#360295=CARTESIAN_POINT('Ctrl Pts',(0.03455812447074,-1.5,-7.44833732146117));
#360296=CARTESIAN_POINT('Ctrl Pts',(0.0691497002760394,-1.49880576977359,
-7.44663986043241));
#360297=CARTESIAN_POINT('Ctrl Pts',(0.302114127086169,-1.48265937575617,
-7.43498284327662));
#360298=CARTESIAN_POINT('Ctrl Pts',(0.495782990150613,-1.42959048582248,
-7.42419080992647));
#360299=CARTESIAN_POINT('Ctrl Pts',(0.847010260809035,-1.25311844319053,
-7.4023903788038));
#360300=CARTESIAN_POINT('Ctrl Pts',(1.00201236847691,-1.13301134049999,
-7.39159652801348));
#360301=CARTESIAN_POINT('Ctrl Pts',(1.25591620604731,-0.842277268864258,
-7.37130462749836));
#360302=CARTESIAN_POINT('Ctrl Pts',(1.35316374690191,-0.675058625776248,
-7.36250325698756));
#360303=CARTESIAN_POINT('Ctrl Pts',(1.48204932028991,-0.30556823892079,
-7.34197601327337));
#360304=CARTESIAN_POINT('Ctrl Pts',(1.50950991824371,-0.105875768471577,
-7.3308819871373));
#360305=CARTESIAN_POINT('Ctrl Pts',(1.48515003725264,0.284953719955094,
-7.30916923778026));
#360306=CARTESIAN_POINT('Ctrl Pts',(1.43651615666324,0.47255725663361,-7.2987468190759));
#360307=CARTESIAN_POINT('Ctrl Pts',(1.26884196249976,0.824001710507948,
-7.27922212719399));
#360308=CARTESIAN_POINT('Ctrl Pts',(1.14956252123489,0.98359727785109,-7.26965287265012));
#360309=CARTESIAN_POINT('Ctrl Pts',(0.856183569542317,1.24731793580582,
-7.24821209742352));
#360310=CARTESIAN_POINT('Ctrl Pts',(0.685048336856938,1.34891069025598,
-7.23715632874501));
#360311=CARTESIAN_POINT('Ctrl Pts',(0.319942559610042,1.47775569881861,
-7.21601114083136));
#360312=CARTESIAN_POINT('Ctrl Pts',(0.130365721284194,1.50635212239085,
-7.20644867153388));
#360313=CARTESIAN_POINT('Ctrl Pts',(-0.258154573885091,1.49093809666085,
-7.1873278127357));
#360314=CARTESIAN_POINT('Ctrl Pts',(-0.453275731059376,1.44362633538023,
-7.17662582609297));
#360315=CARTESIAN_POINT('Ctrl Pts',(-0.810045874231628,1.27740919884723,
-7.15484357189489));
#360316=CARTESIAN_POINT('Ctrl Pts',(-0.968931336943506,1.1615203888964,
-7.14398005789622));
#360317=CARTESIAN_POINT('Ctrl Pts',(-1.2308607245362,0.8783153976357,-7.12351116904715));
#360318=CARTESIAN_POINT('Ctrl Pts',(-1.33253379305841,0.71470765501183,
-7.11470598083397));
#360319=CARTESIAN_POINT('Ctrl Pts',(-1.47240593241364,0.349434861517134,
-7.09441304786204));
#360320=CARTESIAN_POINT('Ctrl Pts',(-1.50584219290995,0.150027641038111,
-7.08333486894654));
#360321=CARTESIAN_POINT('Ctrl Pts',(-1.49274278900061,-0.242473565082339,
-7.0615292463843));
#360322=CARTESIAN_POINT('Ctrl Pts',(-1.44932531302366,-0.431912567947767,
-7.05100485733622));
#360323=CARTESIAN_POINT('Ctrl Pts',(-1.29197362459708,-0.786811895684146,
-7.03128822801753));
#360324=CARTESIAN_POINT('Ctrl Pts',(-1.17847511117939,-0.94840711761969,
-7.02202143473327));
#360325=CARTESIAN_POINT('Ctrl Pts',(-0.894284412677067,-1.22038798917765,
-7.00079327916653));
#360326=CARTESIAN_POINT('Ctrl Pts',(-0.725818321526072,-1.32750722822041,
-6.98971241615906));
#360327=CARTESIAN_POINT('Ctrl Pts',(-0.368653448389195,-1.46575000433356,
-6.96868823607392));
#360328=CARTESIAN_POINT('Ctrl Pts',(-0.185069197507755,-1.5,-6.95890414591665));
#360329=CARTESIAN_POINT('Ctrl Pts',(1.28369537222284E-15,-1.5,-6.95));
#360330=CARTESIAN_POINT('Ctrl Pts',(1.30728761149612E-13,-1.5,-6.8875));
#360331=CARTESIAN_POINT('Ctrl Pts',(-0.158390152479677,-1.5,-6.89512054976426));
#360332=CARTESIAN_POINT('Ctrl Pts',(-0.315971192569039,-1.47491827510613,
-6.90339888567089));
#360333=CARTESIAN_POINT('Ctrl Pts',(-0.653783527509526,-1.3642731496121,
-6.92272536492185));
#360334=CARTESIAN_POINT('Ctrl Pts',(-0.826821260072185,-1.2669016416291,
-6.93375541082207));
#360335=CARTESIAN_POINT('Ctrl Pts',(-1.12709975345344,-1.00954237554425,
-6.95535143507322));
#360336=CARTESIAN_POINT('Ctrl Pts',(-1.25080423509296,-0.851464098715239,
-6.96519643896028));
#360337=CARTESIAN_POINT('Ctrl Pts',(-1.42620834036991,-0.502660638698363,
-6.98457440896122));
#360338=CARTESIAN_POINT('Ctrl Pts',(-1.47869263683948,-0.316519978066789,
-6.99491555677408));
#360339=CARTESIAN_POINT('Ctrl Pts',(-1.51140509127975,0.0728561626068144,
-7.01654756458928));
#360340=CARTESIAN_POINT('Ctrl Pts',(-1.48839713759346,0.272649213524213,
-7.02764717852914));
#360341=CARTESIAN_POINT('Ctrl Pts',(-1.36775008530669,0.645211339832847,
-7.04834507443517));
#360342=CARTESIAN_POINT('Ctrl Pts',(-1.27379537939998,0.815157568179255,
-7.05719109035035));
#360343=CARTESIAN_POINT('Ctrl Pts',(-1.02584434032439,1.11140911599787,
-7.07734984994165));
#360344=CARTESIAN_POINT('Ctrl Pts',(-0.873772080737687,1.23454293921033,
-7.0880868139205));
#360345=CARTESIAN_POINT('Ctrl Pts',(-0.526816590516345,1.41845091857688,
-7.10988827270924));
#360346=CARTESIAN_POINT('Ctrl Pts',(-0.334329224715241,1.47573134939196,
-7.12074044849251));
#360347=CARTESIAN_POINT('Ctrl Pts',(0.0529135656295898,1.51105373279578,
-7.14035285324656));
#360348=CARTESIAN_POINT('Ctrl Pts',(0.243639774933199,1.49222541955791,
-7.14943808470476));
#360349=CARTESIAN_POINT('Ctrl Pts',(0.613841908736108,1.38262455643514,
-7.17029391159198));
#360350=CARTESIAN_POINT('Ctrl Pts',(0.78913569727102,1.2906254016952,-7.18128327000125));
#360351=CARTESIAN_POINT('Ctrl Pts',(1.09805587513349,1.04144027019704,-7.20306800819678));
#360352=CARTESIAN_POINT('Ctrl Pts',(1.22741158823864,0.885293034339754,
-7.2133170536478));
#360353=CARTESIAN_POINT('Ctrl Pts',(1.41248141808405,0.539858055493316,
-7.23250788580594));
#360354=CARTESIAN_POINT('Ctrl Pts',(1.46970787911335,0.355649358979269,
-7.24274170227894));
#360355=CARTESIAN_POINT('Ctrl Pts',(1.51275662636364,-0.0316722665942642,
-7.26425957036636));
#360356=CARTESIAN_POINT('Ctrl Pts',(1.4952830293338,-0.23145665075453,-7.27535870281971));
#360357=CARTESIAN_POINT('Ctrl Pts',(1.38495302486129,-0.607748939222347,
-7.29626382995681));
#360358=CARTESIAN_POINT('Ctrl Pts',(1.29509509903591,-0.781139147078928,
-7.30522135096988));
#360359=CARTESIAN_POINT('Ctrl Pts',(1.05452240507017,-1.08414839220289,
-7.32521283358061));
#360360=CARTESIAN_POINT('Ctrl Pts',(0.906132804005084,-1.21091027722153,
-7.33587339506334));
#360361=CARTESIAN_POINT('Ctrl Pts',(0.564648562678366,-1.40382350051254,
-7.35766176393148));
#360362=CARTESIAN_POINT('Ctrl Pts',(0.373743734336722,-1.46624765479896,
-7.36858068105327));
#360363=CARTESIAN_POINT('Ctrl Pts',(0.117614019873121,-1.49654541479466,
-7.38174533213034));
#360364=CARTESIAN_POINT('Ctrl Pts',(0.0587783367701221,-1.5,-7.38467202595361));
#360365=CARTESIAN_POINT('Ctrl Pts',(1.64729341278753E-13,-1.5,-7.3875));
#360366=CARTESIAN_POINT('Origin',(0.,1.30104260698261E-15,-17.7));
#360367=CARTESIAN_POINT('',(6.58274699238299E-14,-1.5,-7.94999999999999));
#360368=CARTESIAN_POINT('',(-6.48430451891059E-15,-1.5,-7.8875));
#360369=CARTESIAN_POINT('',(-1.83697019872103E-16,-1.5,-17.7));
#360370=CARTESIAN_POINT('Ctrl Pts',(1.31838636867532E-13,-1.5,-7.94999999999999));
#360371=CARTESIAN_POINT('Ctrl Pts',(0.0622836217362446,-1.5,-7.94700337785203));
#360372=CARTESIAN_POINT('Ctrl Pts',(0.124625046031404,-1.4961211374503,
-7.94389622849522));
#360373=CARTESIAN_POINT('Ctrl Pts',(0.385989404538987,-1.46334076996953,
-7.93041076417012));
#360374=CARTESIAN_POINT('Ctrl Pts',(0.57824906146685,-1.39855788367082,
-7.91936114249391));
#360375=CARTESIAN_POINT('Ctrl Pts',(0.919134390997817,-1.20103864507334,
-7.89747364391336));
#360376=CARTESIAN_POINT('Ctrl Pts',(1.06599946847489,-1.07282927383352,
-7.88684622315537));
#360377=CARTESIAN_POINT('Ctrl Pts',(1.3035473165281,-0.767075269261111,
-7.86692403019345));
#360378=CARTESIAN_POINT('Ctrl Pts',(1.3917190920234,-0.592252778217645,
-7.8579029321232));
#360379=CARTESIAN_POINT('Ctrl Pts',(1.49778553788722,-0.214457793011997,
-7.83691432183399));
#360380=CARTESIAN_POINT('Ctrl Pts',(1.51298718653284,-0.014720015692516,
-7.82581777864958));
#360381=CARTESIAN_POINT('Ctrl Pts',(1.46570987294793,0.37167827682238,-7.80435120684319));
#360382=CARTESIAN_POINT('Ctrl Pts',(1.40655075449925,0.555057249933396,
-7.7941634861148));
#360383=CARTESIAN_POINT('Ctrl Pts',(1.2188455871199,0.896615758666252,-7.77518801340742));
#360384=CARTESIAN_POINT('Ctrl Pts',(1.08941924203679,1.05010363320528,-7.7649118290207));
#360385=CARTESIAN_POINT('Ctrl Pts',(0.780422341329571,1.29589316828388,
-7.74321772161835));
#360386=CARTESIAN_POINT('Ctrl Pts',(0.604635461528741,1.38665718104324,
-7.73223894884395));
#360387=CARTESIAN_POINT('Ctrl Pts',(0.233805272802087,1.49380325165562,
-7.71142109333097));
#360388=CARTESIAN_POINT('Ctrl Pts',(0.0429155053270266,1.51137658317992,
-7.70238078941218));
#360389=CARTESIAN_POINT('Ctrl Pts',(-0.344135327230572,1.47347614001839,
-7.68270600746043));
#360390=CARTESIAN_POINT('Ctrl Pts',(-0.536243143563457,1.41491503845189,
-7.67183651857192));
#360391=CARTESIAN_POINT('Ctrl Pts',(-0.881862737716797,1.22875704214068,
-7.65003683264203));
#360392=CARTESIAN_POINT('Ctrl Pts',(-1.03302891469827,1.10471282610045,
-7.63931817389319));
#360393=CARTESIAN_POINT('Ctrl Pts',(-1.27915452935369,0.806781048157432,
-7.61920056701624));
#360394=CARTESIAN_POINT('Ctrl Pts',(-1.37209747555576,0.635989373106926,
-7.61033274295038));
#360395=CARTESIAN_POINT('Ctrl Pts',(-1.49020295425105,0.262496115259053,
-7.58958311751438));
#360396=CARTESIAN_POINT('Ctrl Pts',(-1.51184297998452,0.0626914013643946,
-7.57848285563134));
#360397=CARTESIAN_POINT('Ctrl Pts',(-1.47657100600956,-0.326202548982423,
-7.55687763616763));
#360398=CARTESIAN_POINT('Ctrl Pts',(-1.42291007553314,-0.511877428139616,
-7.54656236510334));
#360399=CARTESIAN_POINT('Ctrl Pts',(-1.24512333107803,-0.859857421184804,
-7.5272301432675));
#360400=CARTESIAN_POINT('Ctrl Pts',(-1.12003804942027,-1.01746355631494,
-7.5172916458803));
#360401=CARTESIAN_POINT('Ctrl Pts',(-0.817630476530446,-1.27283083493107,
-7.49564851922878));
#360402=CARTESIAN_POINT('Ctrl Pts',(-0.644023691645171,-1.36888750420052,
-7.48462761808352));
#360403=CARTESIAN_POINT('Ctrl Pts',(-0.308938681843284,-1.47603136537536,
-7.46552961466667));
#360404=CARTESIAN_POINT('Ctrl Pts',(-0.15483694149587,-1.5,-7.4574495958211));
#360405=CARTESIAN_POINT('Ctrl Pts',(1.6976003935909E-13,-1.5,-7.44999999999999));
#360406=CARTESIAN_POINT('Ctrl Pts',(1.64139535296925E-13,-1.5,-7.3875));
#360407=CARTESIAN_POINT('Ctrl Pts',(-0.130711946418685,-1.5,-7.39378888145426));
#360408=CARTESIAN_POINT('Ctrl Pts',(-0.26109431040442,-1.48291923269925,
-7.40053637162469));
#360409=CARTESIAN_POINT('Ctrl Pts',(-0.576783675113658,-1.39841762954913,
-7.41807225002012));
#360410=CARTESIAN_POINT('Ctrl Pts',(-0.754002495834011,-1.31138315363872,
-7.42901631883833));
#360411=CARTESIAN_POINT('Ctrl Pts',(-1.0676374910888,-1.07223563176754,
-7.45074907630178));
#360412=CARTESIAN_POINT('Ctrl Pts',(-1.20015471344121,-0.921468937328372,
-7.46130728125954));
#360413=CARTESIAN_POINT('Ctrl Pts',(-1.39462578116005,-0.584246741581453,
-7.48004184768993));
#360414=CARTESIAN_POINT('Ctrl Pts',(-1.45748819449554,-0.402528118290563,
-7.49013732676164));
#360415=CARTESIAN_POINT('Ctrl Pts',(-1.5128948459604,-0.0180421993557636,
-7.51149765559135));
#360416=CARTESIAN_POINT('Ctrl Pts',(-1.5020740026234,0.181534635375859,
-7.52258525752089));
#360417=CARTESIAN_POINT('Ctrl Pts',(-1.40428067204569,0.562179549005838,
-7.543732197167));
#360418=CARTESIAN_POINT('Ctrl Pts',(-1.31937269119552,0.739795325885163,
-7.55290485529489));
#360419=CARTESIAN_POINT('Ctrl Pts',(-1.0876546246449,1.0507980282835,-7.57269235992532));
#360420=CARTESIAN_POINT('Ctrl Pts',(-0.943749465253424,1.18173131505699,
-7.5832530358784));
#360421=CARTESIAN_POINT('Ctrl Pts',(-0.607782292460559,1.3859150267921,
-7.60508903378639));
#360422=CARTESIAN_POINT('Ctrl Pts',(-0.41737912000973,1.45463755092375,
-7.6161587696958));
#360423=CARTESIAN_POINT('Ctrl Pts',(-0.0304488659793696,1.51176518887962,
-7.63636183905474));
#360424=CARTESIAN_POINT('Ctrl Pts',(0.161748775563658,1.50339693636403,
-7.64518778224929));
#360425=CARTESIAN_POINT('Ctrl Pts',(0.537002395637976,1.41409610431455,
-7.66572275913103));
#360426=CARTESIAN_POINT('Ctrl Pts',(0.716114530205454,1.3323705443853,-7.67661045016581));
#360427=CARTESIAN_POINT('Ctrl Pts',(1.03604574905603,1.10277800527287,-7.69838071864051));
#360428=CARTESIAN_POINT('Ctrl Pts',(1.17292778376266,0.955916148964611,
-7.70904595461449));
#360429=CARTESIAN_POINT('Ctrl Pts',(1.37687637469735,0.624772142429321,
-7.72805688039689));
#360430=CARTESIAN_POINT('Ctrl Pts',(1.44491471501658,0.445409432145121,
-7.7377550315475));
#360431=CARTESIAN_POINT('Ctrl Pts',(1.51158414892893,0.0636737338260033,
-7.75896257034301));
#360432=CARTESIAN_POINT('Ctrl Pts',(1.50684319464338,-0.135523662450533,
-7.77002909235837));
#360433=CARTESIAN_POINT('Ctrl Pts',(1.42065840926741,-0.520017926624075,
-7.79138988481246));
#360434=CARTESIAN_POINT('Ctrl Pts',(1.34031972299538,-0.701581490106598,
-7.80083554531923));
#360435=CARTESIAN_POINT('Ctrl Pts',(1.11669567601627,-1.01978268009016,
-7.82043358423994));
#360436=CARTESIAN_POINT('Ctrl Pts',(0.976941627781406,-1.15435347368589,
-7.83089558162055));
#360437=CARTESIAN_POINT('Ctrl Pts',(0.647943350348728,-1.36751217147121,
-7.85264559356225));
#360438=CARTESIAN_POINT('Ctrl Pts',(0.460218660943862,-1.44157281839024,
-7.86373474208457));
#360439=CARTESIAN_POINT('Ctrl Pts',(0.176319080109958,-1.49223079408003,
-7.87880103302739));
#360440=CARTESIAN_POINT('Ctrl Pts',(0.0881508891495514,-1.5,-7.88325883836835));
#360441=CARTESIAN_POINT('Ctrl Pts',(-1.73472347597681E-16,-1.5,-7.8875));
#360442=CARTESIAN_POINT('Origin',(0.,1.30104260698261E-15,-17.7));
#360443=CARTESIAN_POINT('',(1.62838980068328E-14,-1.5,-8.45));
#360444=CARTESIAN_POINT('',(-3.3120983492535E-14,-1.5,-8.38750000000001));
#360445=CARTESIAN_POINT('',(-1.83697019872103E-16,-1.5,-17.7));
#360446=CARTESIAN_POINT('Ctrl Pts',(3.27514930335377E-14,-1.5,-8.45));
#360447=CARTESIAN_POINT('Ctrl Pts',(0.0919060245909611,-1.5,-8.44557816933018));
#360448=CARTESIAN_POINT('Ctrl Pts',(0.183815329080158,-1.49155484907763,
-8.44092159333058));
#360449=CARTESIAN_POINT('Ctrl Pts',(0.470889171269676,-1.43810172702746,
-8.42562493771262));
#360450=CARTESIAN_POINT('Ctrl Pts',(0.657920267443974,-1.36271842253387,
-8.41453241922198));
#360451=CARTESIAN_POINT('Ctrl Pts',(0.985135825347778,-1.14734611051077,
-8.39280668912922));
#360452=CARTESIAN_POINT('Ctrl Pts',(1.123835536039,-1.01188384306565,-8.38237065542485));
#360453=CARTESIAN_POINT('Ctrl Pts',(1.34541672627809,-0.691881954295951,
-8.36282088408414));
#360454=CARTESIAN_POINT('Ctrl Pts',(1.42459400378327,-0.509309679182099,
-8.35329498217678));
#360455=CARTESIAN_POINT('Ctrl Pts',(1.50782651039528,-0.123864807282884,
-8.33188137818238));
#360456=CARTESIAN_POINT('Ctrl Pts',(1.51103461398953,0.0752080911527746,
-8.32082177271373));
#360457=CARTESIAN_POINT('Ctrl Pts',(1.44153190399057,0.456206191994516,
-8.29965521155586));
#360458=CARTESIAN_POINT('Ctrl Pts',(1.37218726699645,0.634984418918529,
-8.2900476012505));
#360459=CARTESIAN_POINT('Ctrl Pts',(1.16582929948974,0.964562380147401,
-8.27096425554225));
#360460=CARTESIAN_POINT('Ctrl Pts',(1.02785859315551,1.11041463298508,-8.26027468537101));
#360461=CARTESIAN_POINT('Ctrl Pts',(0.706342100872746,1.33755660851709,
-8.23849621660331));
#360462=CARTESIAN_POINT('Ctrl Pts',(0.526771233312194,1.41792015918229,
-8.22762428835778));
#360463=CARTESIAN_POINT('Ctrl Pts',(0.150875651795156,1.50454645245795,
-8.20713271783545));
#360464=CARTESIAN_POINT('Ctrl Pts',(-0.0415361031340621,1.51152080393762,
-8.1983216156378));
#360465=CARTESIAN_POINT('Ctrl Pts',(-0.428035479493202,1.45151678832234,
-8.17805937751105));
#360466=CARTESIAN_POINT('Ctrl Pts',(-0.617788120056051,1.38146223334104,
-8.16698393947476));
#360467=CARTESIAN_POINT('Ctrl Pts',(-0.952049697448619,1.17503292634832,
-8.14516762441768));
#360468=CARTESIAN_POINT('Ctrl Pts',(-1.09493439388521,1.04318612453353,
-8.1346306700936));
#360469=CARTESIAN_POINT('Ctrl Pts',(-1.32465451950825,0.730397000890158,
-8.1148896686285));
#360470=CARTESIAN_POINT('Ctrl Pts',(-1.40843905179061,0.55181414724647,
-8.10565634151369));
#360471=CARTESIAN_POINT('Ctrl Pts',(-1.50338010817072,0.170207103404275,
-8.08445595018912));
#360472=CARTESIAN_POINT('Ctrl Pts',(-1.51269957457772,-0.0292929547662327,
-8.07337261362409));
#360473=CARTESIAN_POINT('Ctrl Pts',(-1.45449801295143,-0.413190375994559,
-8.0520449791114));
#360474=CARTESIAN_POINT('Ctrl Pts',(-1.39033334183595,-0.594315098362038,
-8.04205035803207));
#360475=CARTESIAN_POINT('Ctrl Pts',(-1.1935325018415,-0.93005646632443,
-8.02325562409304));
#360476=CARTESIAN_POINT('Ctrl Pts',(-1.05991258445926,-1.07985343287618,
-8.01266580597191));
#360477=CARTESIAN_POINT('Ctrl Pts',(-0.744776913013553,-1.31662456257156,
-7.99092685808533));
#360478=CARTESIAN_POINT('Ctrl Pts',(-0.567079977833594,-1.40236211515631,
-7.9799958116224));
#360479=CARTESIAN_POINT('Ctrl Pts',(-0.254270975061089,-1.48380485968209,
-7.96268348300038));
#360480=CARTESIAN_POINT('Ctrl Pts',(-0.127278002173556,-1.5,-7.95612366573474));
#360481=CARTESIAN_POINT('Ctrl Pts',(1.32081845460874E-13,-1.5,-7.94999999999999));
#360482=CARTESIAN_POINT('Ctrl Pts',(-2.55004350968591E-15,-1.5,-7.8875));
#360483=CARTESIAN_POINT('Ctrl Pts',(-0.10237969393186,-1.5,-7.89242574532093));
#360484=CARTESIAN_POINT('Ctrl Pts',(-0.204707722448345,-1.489520686643,
-7.8976400969261));
#360485=CARTESIAN_POINT('Ctrl Pts',(-0.495809132059467,-1.42898472088833,
-7.91332727463043));
#360486=CARTESIAN_POINT('Ctrl Pts',(-0.676699620390658,-1.35273472674166,
-7.92414842770105));
#360487=CARTESIAN_POINT('Ctrl Pts',(-1.00287409426353,-1.13303498676165,
-7.94594427494716));
#360488=CARTESIAN_POINT('Ctrl Pts',(-1.14407565723151,-0.990271945330059,
-7.95670347835272));
#360489=CARTESIAN_POINT('Ctrl Pts',(-1.3576613618609,-0.665443132622998,
-7.97600264793315));
#360490=CARTESIAN_POINT('Ctrl Pts',(-1.43092922096547,-0.488390490422837,
-7.98536719497652));
#360491=CARTESIAN_POINT('Ctrl Pts',(-1.50886956974448,-0.109630465307728,
-8.00640941859402));
#360492=CARTESIAN_POINT('Ctrl Pts',(-1.51022654561875,0.0890022614738588,
-8.01744457008189));
#360493=CARTESIAN_POINT('Ctrl Pts',(-1.43585304738513,0.47722941824748,
-8.0390127454582));
#360494=CARTESIAN_POINT('Ctrl Pts',(-1.36016227437668,0.662838498285955,
-8.04880467590354));
#360495=CARTESIAN_POINT('Ctrl Pts',(-1.14467434096634,0.988173006718972,
-8.06820941361236));
#360496=CARTESIAN_POINT('Ctrl Pts',(-1.00913285985506,1.12623053363248,
-8.07856558746601));
#360497=CARTESIAN_POINT('Ctrl Pts',(-0.687286816935304,1.34808086137161,
-8.10021292152966));
#360498=CARTESIAN_POINT('Ctrl Pts',(-0.502364143957666,1.42734931561428,
-8.1113119192883));
#360499=CARTESIAN_POINT('Ctrl Pts',(-0.119122736408198,1.50757862908486,
-8.13197922214693));
#360500=CARTESIAN_POINT('Ctrl Pts',(0.0749006733276469,1.51042123685776,
-8.14081418152409));
#360501=CARTESIAN_POINT('Ctrl Pts',(0.455115960360642,1.442388450537,-8.16099709767065));
#360502=CARTESIAN_POINT('Ctrl Pts',(0.637587446377473,1.37152637789345,
-8.17174465204168));
#360503=CARTESIAN_POINT('Ctrl Pts',(0.969571590709034,1.16166609369766,
-8.19354669897183));
#360504=CARTESIAN_POINT('Ctrl Pts',(1.11487635577431,1.023038867733,-8.20438843401737));
#360505=CARTESIAN_POINT('Ctrl Pts',(1.33782638530658,0.704482335029449,
-8.22396391488966));
#360506=CARTESIAN_POINT('Ctrl Pts',(1.4161945616287,0.529606115593179,-8.23307743802261));
#360507=CARTESIAN_POINT('Ctrl Pts',(1.50493462866019,0.153799071573299,
-8.25395560713482));
#360508=CARTESIAN_POINT('Ctrl Pts',(1.51212858296256,-0.0441180221961207,
-8.26495100123312));
#360509=CARTESIAN_POINT('Ctrl Pts',(1.44924015520889,-0.435792680293736,
-8.28671070446077));
#360510=CARTESIAN_POINT('Ctrl Pts',(1.37807880670724,-0.625357255423701,
-8.29690152070481));
#360511=CARTESIAN_POINT('Ctrl Pts',(1.17041094760942,-0.957451741924483,
-8.3161177920814));
#360512=CARTESIAN_POINT('Ctrl Pts',(1.03894701909247,-1.09870021797266,
-8.32636642207035));
#360513=CARTESIAN_POINT('Ctrl Pts',(0.724096160060608,-1.32858932692728,
-8.34790049967047));
#360514=CARTESIAN_POINT('Ctrl Pts',(0.541961125988814,-1.41271054922394,
-8.35900017620234));
#360515=CARTESIAN_POINT('Ctrl Pts',(0.234231915043067,-1.48626832059935,
-8.37584907619419));
#360516=CARTESIAN_POINT('Ctrl Pts',(0.117197432864771,-1.50000000000001,
-8.38186133588227));
#360517=CARTESIAN_POINT('Ctrl Pts',(-6.44276298977786E-14,-1.5,-8.38750000000001));
#360518=CARTESIAN_POINT('Origin',(0.,1.30104260698261E-15,-17.7));
#360519=CARTESIAN_POINT('',(-4.96354202156784E-14,-1.5,-8.95));
#360520=CARTESIAN_POINT('',(-1.15641779244756E-13,-1.5,-8.88750000000002));
#360521=CARTESIAN_POINT('',(-1.83697019872103E-16,-1.5,-17.7));
#360522=CARTESIAN_POINT('Ctrl Pts',(-9.75608482889356E-14,-1.5,-8.95));
#360523=CARTESIAN_POINT('Ctrl Pts',(0.12285708034588,-1.50000000000001,
-8.94408903596587));
#360524=CARTESIAN_POINT('Ctrl Pts',(0.245494453006151,-1.48491021249227,
-8.93776948185859));
#360525=CARTESIAN_POINT('Ctrl Pts',(0.557659907759538,-1.40655610297248,
-8.92057391137191));
#360526=CARTESIAN_POINT('Ctrl Pts',(0.738647166664289,-1.32052182799538,
-8.90947631684627));
#360527=CARTESIAN_POINT('Ctrl Pts',(1.05064900131988,-1.0874803941173,-8.88799174841416));
#360528=CARTESIAN_POINT('Ctrl Pts',(1.18046342086137,-0.944990066599894,
-8.87778798458865));
#360529=CARTESIAN_POINT('Ctrl Pts',(1.38367733959653,-0.61232870455309,
-8.85877025697472));
#360530=CARTESIAN_POINT('Ctrl Pts',(1.45258311498454,-0.42374149198048,
-8.84854119399891));
#360531=CARTESIAN_POINT('Ctrl Pts',(1.5123857666276,-0.0333883641337487,
-8.82685490911854));
#360532=CARTESIAN_POINT('Ctrl Pts',(1.50380314579772,0.164332980671071,
-8.81587038996271));
#360533=CARTESIAN_POINT('Ctrl Pts',(1.41248988489652,0.539422119867692,
-8.79503210445179));
#360534=CARTESIAN_POINT('Ctrl Pts',(1.33289232409031,0.713784931995395,
-8.78596811928743));
#360535=CARTESIAN_POINT('Ctrl Pts',(1.10769266361828,1.03081373272249,-8.76632683999544));
#360536=CARTESIAN_POINT('Ctrl Pts',(0.961416840844422,1.16842525458379,
-8.75546659891697));
#360537=CARTESIAN_POINT('Ctrl Pts',(0.628076109264871,1.375889546242,-8.73366583850069));
#360538=CARTESIAN_POINT('Ctrl Pts',(0.44524688013909,1.44544802847379,-8.72293728305107));
#360539=CARTESIAN_POINT('Ctrl Pts',(0.0644587751524896,1.51093518733999,
-8.7027975190616));
#360540=CARTESIAN_POINT('Ctrl Pts',(-0.129800484908925,1.50672943834416,
-8.69394190010097));
#360541=CARTESIAN_POINT('Ctrl Pts',(-0.512558713165532,1.42370009868172,
-8.67322006571158));
#360542=CARTESIAN_POINT('Ctrl Pts',(-0.696778221911868,1.3431785199936,
-8.66212008994541));
#360543=CARTESIAN_POINT('Ctrl Pts',(-1.01684912889306,1.11924664383361,
-8.64050034135996));
#360544=CARTESIAN_POINT('Ctrl Pts',(-1.15135203977399,0.980359631790227,
-8.63017109448621));
#360545=CARTESIAN_POINT('Ctrl Pts',(-1.36484372826175,0.653290534438722,
-8.61081421813049));
#360546=CARTESIAN_POINT('Ctrl Pts',(-1.43938443401498,0.466677723103864,
-8.60092654017244));
#360547=CARTESIAN_POINT('Ctrl Pts',(-1.510838369229,0.0775569667310619,
-8.57930872037395));
#360548=CARTESIAN_POINT('Ctrl Pts',(-1.50798869035152,-0.120909140047158,
-8.56828282555293));
#360549=CARTESIAN_POINT('Ctrl Pts',(-1.42728835970505,-0.498923829940028,
-8.54728200944777));
#360550=CARTESIAN_POINT('Ctrl Pts',(-1.3527258432058,-0.6754168702095,-8.53798813941484));
#360551=CARTESIAN_POINT('Ctrl Pts',(-1.13675898689194,-0.998663807739,-8.51861834759773));
#360552=CARTESIAN_POINT('Ctrl Pts',(-0.994504962094306,-1.14038938093043,
-8.507837326161));
#360553=CARTESIAN_POINT('Ctrl Pts',(-0.666828702371811,-1.35760795376376,
-8.48603814551915));
#360554=CARTESIAN_POINT('Ctrl Pts',(-0.48552228395892,-1.4324939668161,
-8.47523486936688));
#360555=CARTESIAN_POINT('Ctrl Pts',(-0.197627808105292,-1.49023483420086,
-8.45977962695627));
#360556=CARTESIAN_POINT('Ctrl Pts',(-0.0988289996479366,-1.5,-8.45475491246254));
#360557=CARTESIAN_POINT('Ctrl Pts',(3.27514930335377E-14,-1.5,-8.45));
#360558=CARTESIAN_POINT('Ctrl Pts',(-6.60582699651979E-14,-1.5,-8.38750000000001));
#360559=CARTESIAN_POINT('Ctrl Pts',(-0.0753177345365689,-1.5,-8.39112372619246));
#360560=CARTESIAN_POINT('Ctrl Pts',(-0.150687448593511,-1.49432802738698,
-8.39490750804556));
#360561=CARTESIAN_POINT('Ctrl Pts',(-0.416724607344908,-1.45387804366168,
-8.40883083747289));
#360562=CARTESIAN_POINT('Ctrl Pts',(-0.600532463051642,-1.38808029394905,
-8.41950201232364));
#360563=CARTESIAN_POINT('Ctrl Pts',(-0.937680864741628,-1.18756128620999,
-8.44129304480022));
#360564=CARTESIAN_POINT('Ctrl Pts',(-1.08671110052146,-1.05291245336646,
-8.45220351071906));
#360565=CARTESIAN_POINT('Ctrl Pts',(-1.31836851280872,-0.740316064545367,
-8.47203236618718));
#360566=CARTESIAN_POINT('Ctrl Pts',(-1.4015064228706,-0.567407959064957,
-8.48097733560751));
#360567=CARTESIAN_POINT('Ctrl Pts',(-1.50016254659718,-0.194397121232557,
-8.50170015993153));
#360568=CARTESIAN_POINT('Ctrl Pts',(-1.51270126349758,0.0027122562987613,
-8.51265068090549));
#360569=CARTESIAN_POINT('Ctrl Pts',(-1.46098267953079,0.393790137894556,
-8.53437722988303));
#360570=CARTESIAN_POINT('Ctrl Pts',(-1.39598155896985,0.583709457498217,
-8.54488329085926));
#360571=CARTESIAN_POINT('Ctrl Pts',(-1.19990662713579,0.92009542914897,
-8.56366100518365));
#360572=CARTESIAN_POINT('Ctrl Pts',(-1.07337989682116,1.06498014824303,
-8.57377310086461));
#360573=CARTESIAN_POINT('Ctrl Pts',(-0.767088280050412,1.30414031891685,
-8.59515290122164));
#360574=CARTESIAN_POINT('Ctrl Pts',(-0.588421794296112,1.39390506697201,
-8.60624246174918));
#360575=CARTESIAN_POINT('Ctrl Pts',(-0.209575637272476,1.49801643981653,
-8.62736168855644));
#360576=CARTESIAN_POINT('Ctrl Pts',(-0.0134428537343731,1.51254306759813,
-8.63650481185376));
#360577=CARTESIAN_POINT('Ctrl Pts',(0.371467798904194,1.46601734040751,
-8.65631621557418));
#360578=CARTESIAN_POINT('Ctrl Pts',(0.556663120472392,1.40616658614029,
-8.66688895058939));
#360579=CARTESIAN_POINT('Ctrl Pts',(0.9009035992305,1.21596192414218,-8.68873469117908));
#360580=CARTESIAN_POINT('Ctrl Pts',(1.05518918317806,1.08479619456351,-8.69980125228606));
#360581=CARTESIAN_POINT('Ctrl Pts',(1.29695109115979,0.777335448538104,
-8.71997360378563));
#360582=CARTESIAN_POINT('Ctrl Pts',(1.3851246432063,0.60643762686481,-8.72880902072974));
#360583=CARTESIAN_POINT('Ctrl Pts',(1.49404813319494,0.236405329345541,
-8.74936637059192));
#360584=CARTESIAN_POINT('Ctrl Pts',(1.51209680439187,0.0402838347975675,
-8.76026200917792));
#360585=CARTESIAN_POINT('Ctrl Pts',(1.47171963321517,-0.351495970951461,
-8.78202755394175));
#360586=CARTESIAN_POINT('Ctrl Pts',(1.41224105671491,-0.543239103722307,
-8.7926799502068));
#360587=CARTESIAN_POINT('Ctrl Pts',(1.2261107511641,-0.884757979971881,
-8.81165322110956));
#360588=CARTESIAN_POINT('Ctrl Pts',(1.10419440264631,-1.03292814495696,
-8.82140020383724));
#360589=CARTESIAN_POINT('Ctrl Pts',(0.805869612369571,-1.28044755098058,
-8.8426289010578));
#360590=CARTESIAN_POINT('Ctrl Pts',(0.630538448004124,-1.37528014404724,
-8.85369876433274));
#360591=CARTESIAN_POINT('Ctrl Pts',(0.298471493246989,-1.4776451341655,
-8.87251881509031));
#360592=CARTESIAN_POINT('Ctrl Pts',(0.149535379941175,-1.50000000000002,
-8.88030547567814));
#360593=CARTESIAN_POINT('Ctrl Pts',(-2.32973362823685E-13,-1.5,-8.88750000000002));
#360594=CARTESIAN_POINT('Origin',(0.,1.30104260698261E-15,-17.7));
#360595=CARTESIAN_POINT('',(-1.23881389363399E-13,-1.5,-9.45000000000001));
#360596=CARTESIAN_POINT('',(-1.6641110470755E-14,-1.5,-9.38750000000001));
#360597=CARTESIAN_POINT('',(-1.83697019872103E-16,-1.5,-17.7));
#360598=CARTESIAN_POINT('Ctrl Pts',(-2.47232789796215E-13,-1.5,-9.45000000000001));
#360599=CARTESIAN_POINT('Ctrl Pts',(0.153335778247755,-1.50000000000002,
-9.44262262892935));
#360600=CARTESIAN_POINT('Ctrl Pts',(0.306002085618831,-1.47649420208641,
-9.43462452896035));
#360601=CARTESIAN_POINT('Ctrl Pts',(0.640761324790949,-1.37052596697953,
-9.4155748554699));
#360602=CARTESIAN_POINT('Ctrl Pts',(0.815254691016666,-1.27447028179578,
-9.40451132599572));
#360603=CARTESIAN_POINT('Ctrl Pts',(1.11160042974155,-1.02493836354319,
-9.38332194281987));
#360604=CARTESIAN_POINT('Ctrl Pts',(1.23239895244512,-0.875962061462964,
-9.37366455897016));
#360605=CARTESIAN_POINT('Ctrl Pts',(1.41606815869254,-0.533186370882533,
-9.35462146504903));
#360606=CARTESIAN_POINT('Ctrl Pts',(1.47418437701841,-0.341016503325073,
-9.34394536129583));
#360607=CARTESIAN_POINT('Ctrl Pts',(1.51175878871156,0.0509164925721334,
-9.32217130596821));
#360608=CARTESIAN_POINT('Ctrl Pts',(1.49235380541641,0.246770303443136,
-9.3112905386976));
#360609=CARTESIAN_POINT('Ctrl Pts',(1.38089384609243,0.616053945194668,
-9.29077478082252));
#360610=CARTESIAN_POINT('Ctrl Pts',(1.29146002028184,0.786459001367279,
-9.2819559824918));
#360611=CARTESIAN_POINT('Ctrl Pts',(1.04751200092349,1.09218476693379,-9.26172664556122));
#360612=CARTESIAN_POINT('Ctrl Pts',(0.892426789909005,1.22217335825025,
-9.2506543106641));
#360613=CARTESIAN_POINT('Ctrl Pts',(0.547128742727475,1.40988634583528,
-9.22882690096806));
#360614=CARTESIAN_POINT('Ctrl Pts',(0.36165896926966,1.46845139547383,-9.21827667539762));
#360615=CARTESIAN_POINT('Ctrl Pts',(-0.0237796560834993,1.51246183502246,
-9.19850973867929));
#360616=CARTESIAN_POINT('Ctrl Pts',(-0.22017516771744,1.4965421493116,-9.18931076589611));
#360617=CARTESIAN_POINT('Ctrl Pts',(-0.598458835159482,1.38960499905061,
-9.16814010806433));
#360618=CARTESIAN_POINT('Ctrl Pts',(-0.776347226521873,1.29862832019234,
-9.15705431887615));
#360619=CARTESIAN_POINT('Ctrl Pts',(-1.08082195073198,1.05742257052299,
-9.13570511216443));
#360620=CARTESIAN_POINT('Ctrl Pts',(-1.20623129179855,0.911739110792384,
-9.1256521728218));
#360621=CARTESIAN_POINT('Ctrl Pts',(-1.39995741045566,0.574144676287531,
-9.10689692646042));
#360622=CARTESIAN_POINT('Ctrl Pts',(-1.4636276388161,0.383783756873773,
-9.09632131982632));
#360623=CARTESIAN_POINT('Ctrl Pts',(-1.5126690241621,-0.00739484925308877,
-9.07458917504149));
#360624=CARTESIAN_POINT('Ctrl Pts',(-1.49883142016827,-0.204285647767434,
-9.06365079734625));
#360625=CARTESIAN_POINT('Ctrl Pts',(-1.39775968728795,-0.576603269734524,
-9.04296648501475));
#360626=CARTESIAN_POINT('Ctrl Pts',(-1.31344625078534,-0.749036025861445,
-9.03405332259749));
#360627=CARTESIAN_POINT('Ctrl Pts',(-1.07842187507997,-1.06178743086891,
-9.0140581680212));
#360628=CARTESIAN_POINT('Ctrl Pts',(-0.92664358218245,-1.19653654936018,
-9.0030127004302));
#360629=CARTESIAN_POINT('Ctrl Pts',(-0.585757273911393,-1.39435192995385,
-8.98111692859344));
#360630=CARTESIAN_POINT('Ctrl Pts',(-0.401458959921958,-1.45814093494388,
-8.97047795502207));
#360631=CARTESIAN_POINT('Ctrl Pts',(-0.140359897804498,-1.49507947307301,
-8.95688975003526));
#360632=CARTESIAN_POINT('Ctrl Pts',(-0.0701507731510393,-1.5,-8.95337513064688));
#360633=CARTESIAN_POINT('Ctrl Pts',(-9.90871434114846E-14,-1.5,-8.95));
#360634=CARTESIAN_POINT('Ctrl Pts',(-2.31099861469641E-13,-1.5,-8.88750000000002));
#360635=CARTESIAN_POINT('Ctrl Pts',(-0.0462362988015458,-1.49999999999999,
-8.88972454496329));
#360636=CARTESIAN_POINT('Ctrl Pts',(-0.0925241731482299,-1.49786231858749,
-8.89201095139538));
#360637=CARTESIAN_POINT('Ctrl Pts',(-0.330227573982773,-1.47578526622149,
-8.90406071305492));
#360638=CARTESIAN_POINT('Ctrl Pts',(-0.516514865900817,-1.42133246726656,
-8.91453604231496));
#360639=CARTESIAN_POINT('Ctrl Pts',(-0.865072685483243,-1.24161204761194,
-8.93629827210792));
#360640=CARTESIAN_POINT('Ctrl Pts',(-1.02265346756099,-1.1154123654225,
-8.94738542774805));
#360641=CARTESIAN_POINT('Ctrl Pts',(-1.27355199468674,-0.815264932438499,
-8.96779421745666));
#360642=CARTESIAN_POINT('Ctrl Pts',(-1.36702068629316,-0.64641121301876,
-8.97658826594341));
#360643=CARTESIAN_POINT('Ctrl Pts',(-1.48651080122788,-0.279530844467869,
-8.99697050864068));
#360644=CARTESIAN_POINT('Ctrl Pts',(-1.51019435270887,-0.0845858145439524,
-9.0078007880809));
#360645=CARTESIAN_POINT('Ctrl Pts',(-1.48150057665828,0.307699504671352,
-9.02959441692619));
#360646=CARTESIAN_POINT('Ctrl Pts',(-1.42772166223408,0.501155664052166,
-9.04034198133624));
#360647=CARTESIAN_POINT('Ctrl Pts',(-1.2518677835424,0.847873866069245,
-9.05960410367052));
#360648=CARTESIAN_POINT('Ctrl Pts',(-1.13457610937044,0.999413064688373,
-9.06900748883903));
#360649=CARTESIAN_POINT('Ctrl Pts',(-0.844470127281307,1.25523165752531,
-9.09007129143333));
#360650=CARTESIAN_POINT('Ctrl Pts',(-0.672664155995585,1.35508634082449,
-9.1011110512836));
#360651=CARTESIAN_POINT('Ctrl Pts',(-0.29890801101406,1.48323177510825,
-9.12265299759007));
#360652=CARTESIAN_POINT('Ctrl Pts',(-0.100474031127314,1.50970308148693,
-9.13239641088221));
#360653=CARTESIAN_POINT('Ctrl Pts',(0.288751466663172,1.48438992600939,
-9.15182617458365));
#360654=CARTESIAN_POINT('Ctrl Pts',(0.475975254188957,1.43534586575904,
-9.16219631826783));
#360655=CARTESIAN_POINT('Ctrl Pts',(0.828537993751511,1.26619108559502,
-9.18385774487733));
#360656=CARTESIAN_POINT('Ctrl Pts',(0.989258581834231,1.14502990997947,
-9.19495600598836));
#360657=CARTESIAN_POINT('Ctrl Pts',(1.24921069463572,0.852294842000582,
-9.21559448751297));
#360658=CARTESIAN_POINT('Ctrl Pts',(1.34800283882696,0.685435165555885,
-9.22442026858023));
#360659=CARTESIAN_POINT('Ctrl Pts',(1.47787953383756,0.321735217753049,
-9.24462582123595));
#360660=CARTESIAN_POINT('Ctrl Pts',(1.50705635882641,0.128102508318784,
-9.25538319398229));
#360661=CARTESIAN_POINT('Ctrl Pts',(1.48985259088274,-0.264338716780145,
-9.27718548426557));
#360662=CARTESIAN_POINT('Ctrl Pts',(1.4417317848399,-0.459310444280137,
-9.28801724688994));
#360663=CARTESIAN_POINT('Ctrl Pts',(1.2730166596941,-0.817460642341476,
-9.30791448011514));
#360664=CARTESIAN_POINT('Ctrl Pts',(1.15477104626469,-0.977412057057087,
-9.31742472038381));
#360665=CARTESIAN_POINT('Ctrl Pts',(0.863020796908887,-1.24261409236543,
-9.33882828400363));
#360666=CARTESIAN_POINT('Ctrl Pts',(0.692347529270165,-1.3451944222219,
-9.34988925902865));
#360667=CARTESIAN_POINT('Ctrl Pts',(0.343997953858306,-1.47022374519527,
-9.37012227253926));
#360668=CARTESIAN_POINT('Ctrl Pts',(0.172569709406923,-1.5,-9.379197235985));
#360669=CARTESIAN_POINT('Ctrl Pts',(-4.01068067645838E-14,-1.5,-9.38750000000001));
#360670=CARTESIAN_POINT('Origin',(0.,1.30104260698261E-15,-17.7));
#360671=CARTESIAN_POINT('',(-2.19086391586799E-15,-1.5,-9.95));
#360672=CARTESIAN_POINT('',(1.6283941103285E-14,-1.5,-9.8875));
#360673=CARTESIAN_POINT('',(-1.83697019872103E-16,-1.5,-17.7));
#360674=CARTESIAN_POINT('Ctrl Pts',(9.0205620750794E-16,-1.5,-9.95));
#360675=CARTESIAN_POINT('Ctrl Pts',(0.178088883907783,-1.5,-9.94143169457801));
#360676=CARTESIAN_POINT('Ctrl Pts',(0.354890543523405,-1.46828714038846,
-9.93204440799667));
#360677=CARTESIAN_POINT('Ctrl Pts',(0.707188235513081,-1.33748407770702,
-9.91146105898009));
#360678=CARTESIAN_POINT('Ctrl Pts',(0.876901019913129,-1.23289333983374,
-9.90039045055931));
#360679=CARTESIAN_POINT('Ctrl Pts',(1.16531814612726,-0.964683033771861,
-9.87906368882493));
#360680=CARTESIAN_POINT('Ctrl Pts',(1.28146042125905,-0.80400547991937,
-9.86966697110663));
#360681=CARTESIAN_POINT('Ctrl Pts',(1.44356501014691,-0.450686773216476,
-9.85003815406758));
#360682=CARTESIAN_POINT('Ctrl Pts',(1.4893945075153,-0.26207584969327,-9.8395597694274));
#360683=CARTESIAN_POINT('Ctrl Pts',(1.50769287712137,0.129694242943233,
-9.81779476428093));
#360684=CARTESIAN_POINT('Ctrl Pts',(1.47701174301179,0.329254357118478,
-9.80670809127119));
#360685=CARTESIAN_POINT('Ctrl Pts',(1.34219595633325,0.696485874846017,
-9.78630634028633));
#360686=CARTESIAN_POINT('Ctrl Pts',(1.24256584198251,0.861750648578542,
-9.77751212565835));
#360687=CARTESIAN_POINT('Ctrl Pts',(0.981262552504138,1.15186543864246,
-9.75688142110808));
#360688=CARTESIAN_POINT('Ctrl Pts',(0.81982443484921,1.27182850496678,-9.74578191859663));
#360689=CARTESIAN_POINT('Ctrl Pts',(0.466363054652606,1.43848111664446,
-9.72414676079964));
#360690=CARTESIAN_POINT('Ctrl Pts',(0.278941091517629,1.486248760098,-9.71380253840915));
#360691=CARTESIAN_POINT('Ctrl Pts',(-0.110776066338477,1.50904249147282,
-9.69441910370462));
#360692=CARTESIAN_POINT('Ctrl Pts',(-0.309494515954199,1.48112142747415,
-9.68458503336604));
#360693=CARTESIAN_POINT('Ctrl Pts',(-0.682591741918069,1.35009195881611,
-9.66299467724964));
#360694=CARTESIAN_POINT('Ctrl Pts',(-0.853538502154639,1.24906072552042,
-9.6519635742659));
#360695=CARTESIAN_POINT('Ctrl Pts',(-1.14168220498132,0.991282903465424,
-9.63093975884279));
#360696=CARTESIAN_POINT('Ctrl Pts',(-1.25787602833459,0.838930564299269,
-9.62160725357218));
#360697=CARTESIAN_POINT('Ctrl Pts',(-1.43125415993856,0.490979030161277,
-9.60227661278674));
#360698=CARTESIAN_POINT('Ctrl Pts',(-1.4836561814186,0.297137277323276,
-9.59150762651796));
#360699=CARTESIAN_POINT('Ctrl Pts',(-1.50954408604807,-0.0952173356098048,
-9.56971014802168));
#360700=CARTESIAN_POINT('Ctrl Pts',(-1.48451466629367,-0.289856099442056,
-9.55889688336433));
#360701=CARTESIAN_POINT('Ctrl Pts',(-1.36248851592326,-0.655967083629947,
-9.53855738424278));
#360702=CARTESIAN_POINT('Ctrl Pts',(-1.2677308612976,-0.824333298495162,
-9.52976224898876));
#360703=CARTESIAN_POINT('Ctrl Pts',(-1.01462826501303,-1.122691452766,-9.50929711813978));
#360704=CARTESIAN_POINT('Ctrl Pts',(-0.856271298649763,-1.24767507522504,
-9.49820639775275));
#360705=CARTESIAN_POINT('Ctrl Pts',(-0.506712953658665,-1.42483897430644,
-9.47646704461899));
#360706=CARTESIAN_POINT('Ctrl Pts',(-0.320184146078453,-1.47798021095492,
-9.46601652771752));
#360707=CARTESIAN_POINT('Ctrl Pts',(-0.0858209378369455,-1.4981608111566,
-9.45418015037584));
#360708=CARTESIAN_POINT('Ctrl Pts',(-0.0428867375032626,-1.49999999999999,
-9.45206338912018));
#360709=CARTESIAN_POINT('Ctrl Pts',(-2.47579081706926E-13,-1.5,-9.45000000000001));
#360710=CARTESIAN_POINT('Ctrl Pts',(-3.30985239216378E-14,-1.5,-9.38750000000001));
#360711=CARTESIAN_POINT('Ctrl Pts',(-0.0171879221613554,-1.5,-9.38832695429056));
#360712=CARTESIAN_POINT('Ctrl Pts',(-0.0343863909262785,-1.49970457697492,
-9.38916262219996));
#360713=CARTESIAN_POINT('Ctrl Pts',(-0.250311720287671,-1.49227409270073,
-9.39975773679355));
#360714=CARTESIAN_POINT('Ctrl Pts',(-0.445672776424722,-1.44599066373983,
-9.41044270079384));
#360715=CARTESIAN_POINT('Ctrl Pts',(-0.803397413409704,-1.28161610511915,
-9.43221969537712));
#360716=CARTESIAN_POINT('Ctrl Pts',(-0.962961932043072,-1.16649051245719,
-9.44309467998879));
#360717=CARTESIAN_POINT('Ctrl Pts',(-1.22631205474749,-0.884630222891906,
-9.46359457116292));
#360718=CARTESIAN_POINT('Ctrl Pts',(-1.32876836835458,-0.721653146130807,
-9.47240815854829));
#360719=CARTESIAN_POINT('Ctrl Pts',(-1.47057152631181,-0.357136234696439,
-9.49265909807242));
#360720=CARTESIAN_POINT('Ctrl Pts',(-1.50506196885152,-0.15779718640125,
-9.50373348964438));
#360721=CARTESIAN_POINT('Ctrl Pts',(-1.49395509078595,0.234965830650891,
-9.52555365725838));
#360722=CARTESIAN_POINT('Ctrl Pts',(-1.45146365973432,0.424713455348534,
-9.53609519196381));
#360723=CARTESIAN_POINT('Ctrl Pts',(-1.29592806047573,0.780212191090157,
-9.55584512172724));
#360724=CARTESIAN_POINT('Ctrl Pts',(-1.18343171231967,0.942156962082107,
-9.56506647525157));
#360725=CARTESIAN_POINT('Ctrl Pts',(-0.900853795573068,1.21556403974649,
-9.58625665265619));
#360726=CARTESIAN_POINT('Ctrl Pts',(-0.732871823156846,1.32364199490675,
-9.59734085449343));
#360727=CARTESIAN_POINT('Ctrl Pts',(-0.3714565780336,1.46571489439951,-9.61867592301221));
#360728=CARTESIAN_POINT('Ctrl Pts',(-0.182540101167985,1.50097459620851,
-9.62869046317083));
#360729=CARTESIAN_POINT('Ctrl Pts',(0.20664431190765,1.49894039450732,-9.64747161257811));
#360730=CARTESIAN_POINT('Ctrl Pts',(0.403235829399321,1.45838890762508,
-9.65805655656464));
#360731=CARTESIAN_POINT('Ctrl Pts',(0.766086052666307,1.30434472367595,
-9.67979320118089));
#360732=CARTESIAN_POINT('Ctrl Pts',(0.929355839681309,1.19352709430535,
-9.69072678995371));
#360733=CARTESIAN_POINT('Ctrl Pts',(1.200561091853,0.919167994853228,-9.71139624482852));
#360734=CARTESIAN_POINT('Ctrl Pts',(1.30735135435701,0.759632901639449,
-9.72029817213114));
#360735=CARTESIAN_POINT('Ctrl Pts',(1.45975713369087,0.399342269902501,
-9.74031431833875));
#360736=CARTESIAN_POINT('Ctrl Pts',(1.50005236242994,0.200474510687348,
-9.75136252718404));
#360737=CARTESIAN_POINT('Ctrl Pts',(1.49994954594571,-0.193552388316353,
-9.77325291046203));
#360738=CARTESIAN_POINT('Ctrl Pts',(1.46258844278961,-0.384917892848863,
-9.7838843273805));
#360739=CARTESIAN_POINT('Ctrl Pts',(1.31703360372687,-0.743666104827207,
-9.80381478360152));
#360740=CARTESIAN_POINT('Ctrl Pts',(1.20996724864347,-0.907524756776458,
-9.81282777796199));
#360741=CARTESIAN_POINT('Ctrl Pts',(0.93622857431212,-1.18862962920031,
-9.83380650474984));
#360742=CARTESIAN_POINT('Ctrl Pts',(0.770980617984793,-1.30190105127316,
-9.84490342914647));
#360743=CARTESIAN_POINT('Ctrl Pts',(0.412865291114638,-1.45464829026131,
-9.8663762397047));
#360744=CARTESIAN_POINT('Ctrl Pts',(0.224503174727305,-1.49535315172199,
-9.87656950685095));
#360745=CARTESIAN_POINT('Ctrl Pts',(0.0223606200870313,-1.49987505737306,
-9.88642070353594));
#360746=CARTESIAN_POINT('Ctrl Pts',(0.0111777862199557,-1.5,-9.88696220850975));
#360747=CARTESIAN_POINT('Ctrl Pts',(3.27515792264421E-14,-1.5,-9.8875));
#360748=CARTESIAN_POINT('Origin',(0.,1.30104260698261E-15,-17.7));
#360749=CARTESIAN_POINT('',(1.63031148958116E-14,-1.5,-10.45));
#360750=CARTESIAN_POINT('',(1.15223986389916E-13,-1.5,-10.3875));
#360751=CARTESIAN_POINT('',(-1.83697019872103E-16,-1.5,-17.7));
#360752=CARTESIAN_POINT('Ctrl Pts',(3.27899268114953E-14,-1.5,-10.45));
#360753=CARTESIAN_POINT('Ctrl Pts',(0.01800321797007,-1.5,-10.4491338197716));
#360754=CARTESIAN_POINT('Ctrl Pts',(0.036018717336121,-1.49967588627835,
-10.4482580454952));
#360755=CARTESIAN_POINT('Ctrl Pts',(0.245176324002544,-1.49213603731342,
-10.4379855052036));
#360756=CARTESIAN_POINT('Ctrl Pts',(0.433213044337886,-1.44875303070621,
-10.4277335007614));
#360757=CARTESIAN_POINT('Ctrl Pts',(0.789626966193958,-1.29072102809195,
-10.4061957501005));
#360758=CARTESIAN_POINT('Ctrl Pts',(0.953462163785975,-1.17489982808324,
-10.3950959699253));
#360759=CARTESIAN_POINT('Ctrl Pts',(1.22279469101575,-0.890029900886932,
-10.3742246491339));
#360760=CARTESIAN_POINT('Ctrl Pts',(1.32719200334045,-0.725215812482133,
-10.3652897673601));
#360761=CARTESIAN_POINT('Ctrl Pts',(1.4677522320276,-0.364869843745343,
-10.3452705468747));
#360762=CARTESIAN_POINT('Ctrl Pts',(1.50252159412429,-0.172745227268556,
-10.3345969570705));
#360763=CARTESIAN_POINT('Ctrl Pts',(1.49711892910183,0.219503631488235,
-10.3128053538062));
#360764=CARTESIAN_POINT('Ctrl Pts',(1.45486376302284,0.415856788035936,
-10.3018968451091));
#360765=CARTESIAN_POINT('Ctrl Pts',(1.29968754567509,0.772639620470973,
-10.2820755766405));
#360766=CARTESIAN_POINT('Ctrl Pts',(1.19139079377124,0.930997563987972,
-10.2731264395137));
#360767=CARTESIAN_POINT('Ctrl Pts',(0.91745975897177,1.20272674065901,-10.2523988937717));
#360768=CARTESIAN_POINT('Ctrl Pts',(0.752924634535686,1.31201491874155,
-10.2414469111818));
#360769=CARTESIAN_POINT('Ctrl Pts',(0.388240902110138,1.46246727905665,
-10.2197218246937));
#360770=CARTESIAN_POINT('Ctrl Pts',(0.191231504278741,1.50097064803793,
-10.2092275924849));
#360771=CARTESIAN_POINT('Ctrl Pts',(-0.198141883730837,1.49903212712652,
-10.1904400088166));
#360772=CARTESIAN_POINT('Ctrl Pts',(-0.386863356846977,1.46173524340097,
-10.1803241181599));
#360773=CARTESIAN_POINT('Ctrl Pts',(-0.747032332294729,1.31573401601126,
-10.1589398905994));
#360774=CARTESIAN_POINT('Ctrl Pts',(-0.914021954701355,1.2057289890355,
-10.1478499034516));
#360775=CARTESIAN_POINT('Ctrl Pts',(-1.19334053336476,0.929460378453624,
-10.1267370539982));
#360776=CARTESIAN_POINT('Ctrl Pts',(-1.30382251768123,0.766809790070398,
-10.1176005438928));
#360777=CARTESIAN_POINT('Ctrl Pts',(-1.45568345644507,0.41010588820822,
-10.097783660456));
#360778=CARTESIAN_POINT('Ctrl Pts',(-1.49629394058661,0.219747119591232,
-10.0872081733106));
#360779=CARTESIAN_POINT('Ctrl Pts',(-1.50335959946284,-0.17351577030611,
-10.065360234983));
#360780=CARTESIAN_POINT('Ctrl Pts',(-1.4667340049793,-0.372700342129076,
-10.0542944254373));
#360781=CARTESIAN_POINT('Ctrl Pts',(-1.32102533310306,-0.735675355437794,
-10.0341291469201));
#360782=CARTESIAN_POINT('Ctrl Pts',(-1.21697939084774,-0.897380503251673,
-10.0252913787072));
#360783=CARTESIAN_POINT('Ctrl Pts',(-0.950746497495352,-1.17650109767429,
-10.0047288928085));
#360784=CARTESIAN_POINT('Ctrl Pts',(-0.789812328683005,-1.29006299093454,
-9.99383144696635));
#360785=CARTESIAN_POINT('Ctrl Pts',(-0.430176479334777,-1.45067426469028,
-9.97206703482607));
#360786=CARTESIAN_POINT('Ctrl Pts',(-0.234344862574323,-1.49486307251423,
-9.9614176148877));
#360787=CARTESIAN_POINT('Ctrl Pts',(-0.0237105811411076,-1.49985951562273,
-9.95114467821085));
#360788=CARTESIAN_POINT('Ctrl Pts',(-0.0118526244172869,-1.5,-9.95057025965816));
#360789=CARTESIAN_POINT('Ctrl Pts',(-1.83697019872103E-16,-1.5,-9.95));
#360790=CARTESIAN_POINT('Ctrl Pts',(3.30985239216375E-14,-1.5,-9.8875));
#360791=CARTESIAN_POINT('Ctrl Pts',(-0.187391350651986,-1.5,-9.8965158705619));
#360792=CARTESIAN_POINT('Ctrl Pts',(-0.373271716031661,-1.46488681977112,
-9.90643440992845));
#360793=CARTESIAN_POINT('Ctrl Pts',(-0.730415627561203,-1.32472660344816,
-9.92751084372584));
#360794=CARTESIAN_POINT('Ctrl Pts',(-0.897065962568103,-1.21806574589348,
-9.93849161330598));
#360795=CARTESIAN_POINT('Ctrl Pts',(-1.17560811243111,-0.950818237745173,
-9.95931652063266));
#360796=CARTESIAN_POINT('Ctrl Pts',(-1.28645814636411,-0.794432345547403,
-9.96836486969182));
#360797=CARTESIAN_POINT('Ctrl Pts',(-1.44759303621033,-0.440494147717617,
-9.98802810290458));
#360798=CARTESIAN_POINT('Ctrl Pts',(-1.49317264952211,-0.244900486810878,
-9.9988944173994));
#360799=CARTESIAN_POINT('Ctrl Pts',(-1.50525018136636,0.147501105949109,
-10.0206945058861));
#360800=CARTESIAN_POINT('Ctrl Pts',(-1.47363789770394,0.340498678165481,
-10.0314165932314));
#360801=CARTESIAN_POINT('Ctrl Pts',(-1.33912346631036,0.702753338863711,
-10.0515418521591));
#360802=CARTESIAN_POINT('Ctrl Pts',(-1.23791519188803,0.868724225890744,
-10.0604053393911));
#360803=CARTESIAN_POINT('Ctrl Pts',(-0.973898850623588,1.15807608173006,
-10.0811453830838));
#360804=CARTESIAN_POINT('Ctrl Pts',(-0.811811210270145,1.27693851831173,
-10.0922455626658));
#360805=CARTESIAN_POINT('Ctrl Pts',(-0.457542083654513,1.44129593240477,
-10.1138558276921));
#360806=CARTESIAN_POINT('Ctrl Pts',(-0.269946185863268,1.48789423348432,
-10.124175936785));
#360807=CARTESIAN_POINT('Ctrl Pts',(0.120218128411184,1.50837654819066,
-10.1435166792942));
#360808=CARTESIAN_POINT('Ctrl Pts',(0.319199220425388,1.47911929755378,
-10.1534374991655));
#360809=CARTESIAN_POINT('Ctrl Pts',(0.691681259174506,1.34543867622126,
-10.1750719002031));
#360810=CARTESIAN_POINT('Ctrl Pts',(0.861831633536728,1.24333257808737,
-10.1860945444102));
#360811=CARTESIAN_POINT('Ctrl Pts',(1.1481697352069,0.983759282179983,-10.2070813620809));
#360812=CARTESIAN_POINT('Ctrl Pts',(1.26335525816127,0.830655508701343,
-10.2163524717388));
#360813=CARTESIAN_POINT('Ctrl Pts',(1.43444753592443,0.481571973138974,
-10.2357460014923));
#360814=CARTESIAN_POINT('Ctrl Pts',(1.48557727677494,0.287383561155462,
-10.2465342466025));
#360815=CARTESIAN_POINT('Ctrl Pts',(1.50887812224303,-0.105017066405158,
-10.268334281467));
#360816=CARTESIAN_POINT('Ctrl Pts',(1.48261031635569,-0.29936531384347,
-10.2791314063246));
#360817=CARTESIAN_POINT('Ctrl Pts',(1.35824595797596,-0.66476252932804,
-10.2994312516293));
#360818=CARTESIAN_POINT('Ctrl Pts',(1.26229343677386,-0.832680156076931,
-10.3082312163757));
#360819=CARTESIAN_POINT('Ctrl Pts',(1.00715502141771,-1.12937665709337,
-10.3287481385806));
#360820=CARTESIAN_POINT('Ctrl Pts',(0.848087752530656,-1.25323088458357,
-10.3398416613312));
#360821=CARTESIAN_POINT('Ctrl Pts',(0.497619683529373,-1.42802417610503,
-10.3615589333718));
#360822=CARTESIAN_POINT('Ctrl Pts',(0.31087547433655,-1.47995085278223,
-10.3719860760112));
#360823=CARTESIAN_POINT('Ctrl Pts',(0.0796161717872997,-1.49841710025498,
-10.3836254957115));
#360824=CARTESIAN_POINT('Ctrl Pts',(0.0397864392775881,-1.5,-10.3855857740478));
#360825=CARTESIAN_POINT('Ctrl Pts',(2.30631669799704E-13,-1.5,-10.3875));
#360826=CARTESIAN_POINT('Origin',(0.,1.30104260698261E-15,-17.7));
#360827=CARTESIAN_POINT('',(1.317107983056E-13,-1.5,-10.95));
#360828=CARTESIAN_POINT('',(5.75201446850214E-14,-1.5,-10.8875));
#360829=CARTESIAN_POINT('',(-1.83697019872103E-16,-1.5,-17.7));
#360830=CARTESIAN_POINT('Ctrl Pts',(2.63605293631073E-13,-1.5,-10.95));
#360831=CARTESIAN_POINT('Ctrl Pts',(0.0448692205490244,-1.5,-10.9478412286198));
#360832=CARTESIAN_POINT('Ctrl Pts',(0.0897883947290352,-1.49798685366247,
-10.9456241331128));
#360833=CARTESIAN_POINT('Ctrl Pts',(0.326130241143317,-1.47668935698625,
-10.9336615335956));
#360834=CARTESIAN_POINT('Ctrl Pts',(0.512517207445259,-1.42277176749051,
-10.9231962756789));
#360835=CARTESIAN_POINT('Ctrl Pts',(0.861485590365093,-1.24409415842851,
-10.9014432596091));
#360836=CARTESIAN_POINT('Ctrl Pts',(1.0193842596546,-1.11839026997729,-10.8903545816616));
#360837=CARTESIAN_POINT('Ctrl Pts',(1.27118292100986,-0.818972364535948,
-10.8699227488787));
#360838=CARTESIAN_POINT('Ctrl Pts',(1.36517744621195,-0.650317979971595,
-10.8611287766651));
#360839=CARTESIAN_POINT('Ctrl Pts',(1.48570385405768,-0.283751401839029,
-10.8407639667688));
#360840=CARTESIAN_POINT('Ctrl Pts',(1.50993769550051,-0.0889304081784544,
-10.8299405782321));
#360841=CARTESIAN_POINT('Ctrl Pts',(1.48239044708045,0.303385663179708,
-10.8081452409345));
#360842=CARTESIAN_POINT('Ctrl Pts',(1.42917377802666,0.497000591068319,
-10.7973888560518));
#360843=CARTESIAN_POINT('Ctrl Pts',(1.25433111678225,0.844223459760498,
-10.77809869668));
#360844=CARTESIAN_POINT('Ctrl Pts',(1.13748859571032,0.996094699681933,
-10.7687248150311));
#360845=CARTESIAN_POINT('Ctrl Pts',(0.848184943334172,1.25271538512326,
-10.747677334193));
#360846=CARTESIAN_POINT('Ctrl Pts',(0.676729486327462,1.35305218831829,
-10.7366410462495));
#360847=CARTESIAN_POINT('Ctrl Pts',(0.303241548629432,1.48237719193206,
-10.7150792382572));
#360848=CARTESIAN_POINT('Ctrl Pts',(0.104691386215296,1.5094409775268,-10.7052992160435));
#360849=CARTESIAN_POINT('Ctrl Pts',(-0.284735860779223,1.48515889892904,
-10.6858883867034));
#360850=CARTESIAN_POINT('Ctrl Pts',(-0.472041837113309,1.43663743886913,
-10.6755288053803));
#360851=CARTESIAN_POINT('Ctrl Pts',(-0.82497464331873,1.26850671189686,
-10.6538780198531));
#360852=CARTESIAN_POINT('Ctrl Pts',(-0.985990085787427,1.14783565807325,
-10.6427791870481));
#360853=CARTESIAN_POINT('Ctrl Pts',(-1.2468121626535,0.855821697819146,
-10.622118880128));
#360854=CARTESIAN_POINT('Ctrl Pts',(-1.34611994644716,0.689152655142687,
-10.613286258619));
#360855=CARTESIAN_POINT('Ctrl Pts',(-1.47699056819011,0.325761067320561,
-10.5930978370734));
#360856=CARTESIAN_POINT('Ctrl Pts',(-1.50669029213086,0.13226193594449,
-10.5823478853302));
#360857=CARTESIAN_POINT('Ctrl Pts',(-1.49058546546239,-0.260176469562684,
-10.560545751691));
#360858=CARTESIAN_POINT('Ctrl Pts',(-1.4430085552882,-0.455284347048996,
-10.5497064251639));
#360859=CARTESIAN_POINT('Ctrl Pts',(-1.27829239399112,-0.807490951113278,
-10.5301393916048));
#360860=CARTESIAN_POINT('Ctrl Pts',(-1.16589334752476,-0.962694609105648,
-10.5210192195837));
#360861=CARTESIAN_POINT('Ctrl Pts',(-0.884560332267287,-1.22720912557693,
-10.5001359531186));
#360862=CARTESIAN_POINT('Ctrl Pts',(-0.716645770489744,-1.33225560479891,
-10.4891392022422));
#360863=CARTESIAN_POINT('Ctrl Pts',(-0.362775121859122,-1.46685847888272,
-10.4683746239972));
#360864=CARTESIAN_POINT('Ctrl Pts',(-0.182059082850492,-1.5,-10.4587593217077));
#360865=CARTESIAN_POINT('Ctrl Pts',(3.46944695195361E-14,-1.5,-10.45));
#360866=CARTESIAN_POINT('Ctrl Pts',(2.30631669799704E-13,-1.5,-10.3875));
#360867=CARTESIAN_POINT('Ctrl Pts',(-0.156867334913038,-1.5,-10.3950472831699));
#360868=CARTESIAN_POINT('Ctrl Pts',(-0.312996144541852,-1.47539873316522,
-10.4032424025487));
#360869=CARTESIAN_POINT('Ctrl Pts',(-0.650223892518879,-1.36604243343655,
-10.4225049551306));
#360870=CARTESIAN_POINT('Ctrl Pts',(-0.823931750309691,-1.26885709450723,
-10.4335620710833));
#360871=CARTESIAN_POINT('Ctrl Pts',(-1.11843697167113,-1.01746168046079,
-10.4547146660983));
#360872=CARTESIAN_POINT('Ctrl Pts',(-1.23819841939332,-0.867732857684848,
-10.4642926190175));
#360873=CARTESIAN_POINT('Ctrl Pts',(-1.41957125919433,-0.523791050021272,
-10.483400497221));
#360874=CARTESIAN_POINT('Ctrl Pts',(-1.47641469054851,-0.331232362429373,
-10.4940982020873));
#360875=CARTESIAN_POINT('Ctrl Pts',(-1.51137640912421,0.0608252823475351,
-10.5158791823526));
#360876=CARTESIAN_POINT('Ctrl Pts',(-1.49070968039528,0.256421290917001,
-10.5267456272732));
#360877=CARTESIAN_POINT('Ctrl Pts',(-1.37688636532436,0.625002839747036,
-10.5472223799859));
#360878=CARTESIAN_POINT('Ctrl Pts',(-1.28627223103907,0.794950005365961,
-10.5560294763567));
#360879=CARTESIAN_POINT('Ctrl Pts',(-1.0402832110233,1.09904761991128,-10.57631178456));
#360880=CARTESIAN_POINT('Ctrl Pts',(-0.884457742076792,1.22793088704675,
-10.587389031684));
#360881=CARTESIAN_POINT('Ctrl Pts',(-0.538186167339719,1.41330793124745,
-10.6091983929301));
#360882=CARTESIAN_POINT('Ctrl Pts',(-0.352467598787901,1.4706692453251,
-10.6197271515612));
#360883=CARTESIAN_POINT('Ctrl Pts',(0.0334616791587361,1.51232318565235,
-10.6394522365017));
#360884=CARTESIAN_POINT('Ctrl Pts',(0.230106048856906,1.49509292939401,
-10.6487072899543));
#360885=CARTESIAN_POINT('Ctrl Pts',(0.607853032724975,1.38550236547394,
-10.6699258325206));
#360886=CARTESIAN_POINT('Ctrl Pts',(0.785003725931987,1.29339373943508,
-10.681007572167));
#360887=CARTESIAN_POINT('Ctrl Pts',(1.08768672851293,1.05033904654925,-10.7023219341654));
#360888=CARTESIAN_POINT('Ctrl Pts',(1.21207525087308,0.903933814333612,
-10.7122814547593));
#360889=CARTESIAN_POINT('Ctrl Pts',(1.40359638285787,0.565193125659586,
-10.7311003819078));
#360890=CARTESIAN_POINT('Ctrl Pts',(1.46605202366308,0.374420850721505,
-10.7416988416266));
#360891=CARTESIAN_POINT('Ctrl Pts',(1.51257644147676,-0.0169523031762115,
-10.7634417946209));
#360892=CARTESIAN_POINT('Ctrl Pts',(1.49751265962048,-0.213628692405403,
-10.7743682606892));
#360893=CARTESIAN_POINT('Ctrl Pts',(1.39415801382123,-0.585286893574757,
-10.7950159385319));
#360894=CARTESIAN_POINT('Ctrl Pts',(1.3087285026964,-0.757271802011755,
-10.803902431723));
#360895=CARTESIAN_POINT('Ctrl Pts',(1.07174988329698,-1.06849726548678,
-10.8239492226281));
#360896=CARTESIAN_POINT('Ctrl Pts',(0.919237776017449,-1.20221397668855,
-10.8350013178997));
#360897=CARTESIAN_POINT('Ctrl Pts',(0.577364012719776,-1.39783262154744,
-10.8568835782515));
#360898=CARTESIAN_POINT('Ctrl Pts',(0.392797634352501,-1.46048316846745,
-10.867503825241));
#360899=CARTESIAN_POINT('Ctrl Pts',(0.134513137431451,-1.49548113240844,
-10.8809027095581));
#360900=CARTESIAN_POINT('Ctrl Pts',(0.0672263389796428,-1.5,-10.8842655712578));
#360901=CARTESIAN_POINT('Ctrl Pts',(1.15223986389915E-13,-1.5,-10.8875));
#360902=CARTESIAN_POINT('Origin',(0.,1.30104260698261E-15,-17.7));
#360903=CARTESIAN_POINT('',(3.27899268114954E-14,-1.5,-11.45));
#360904=CARTESIAN_POINT('',(3.91179454725655E-8,-1.5,-11.3874999962359));
#360905=CARTESIAN_POINT('',(-1.83697019872103E-16,-1.5,-17.7));
#360906=CARTESIAN_POINT('Ctrl Pts',(6.5763550642863E-14,-1.5,-11.45));
#360907=CARTESIAN_POINT('Ctrl Pts',(0.0740159308911273,-1.5,-11.4464389068646));
#360908=CARTESIAN_POINT('Ctrl Pts',(0.148085783009549,-1.49452238116345,
-11.4427230633642));
#360909=CARTESIAN_POINT('Ctrl Pts',(0.412883068505858,-1.45496702756496,
-11.4288842382035));
#360910=CARTESIAN_POINT('Ctrl Pts',(0.596816517544713,-1.38967503608798,
-11.4182210695807));
#360911=CARTESIAN_POINT('Ctrl Pts',(0.934465047856721,-1.19009377843804,
-11.3964320232681));
#360912=CARTESIAN_POINT('Ctrl Pts',(1.08386040428747,-1.05584703782725,
-11.3855151597025));
#360913=CARTESIAN_POINT('Ctrl Pts',(1.3163827898316,-0.743849748068237,
-11.3656613298297));
#360914=CARTESIAN_POINT('Ctrl Pts',(1.39999632380265,-0.571134425145102,
-11.3567296902858));
#360915=CARTESIAN_POINT('Ctrl Pts',(1.49963117977393,-0.198403894113652,
-11.3360224385619));
#360916=CARTESIAN_POINT('Ctrl Pts',(1.51269633696756,-0.00138204992871142,
-11.3250767805516));
#360917=CARTESIAN_POINT('Ctrl Pts',(1.46205695157743,0.38978071904039,-11.3033455156089));
#360918=CARTESIAN_POINT('Ctrl Pts',(1.39757861373038,0.579872013608144,
-11.2928001431373));
#360919=CARTESIAN_POINT('Ctrl Pts',(1.20246123135251,0.916743535558502,
-11.2740550114243));
#360920=CARTESIAN_POINT('Ctrl Pts',(1.07637641317381,1.06194208376696,-11.2639554597755));
#360921=CARTESIAN_POINT('Ctrl Pts',(0.770855479402225,1.30190841028484,
-11.2425903457037));
#360922=CARTESIAN_POINT('Ctrl Pts',(0.59250422151623,1.39216640819344,-11.2315022501992));
#360923=CARTESIAN_POINT('Ctrl Pts',(0.213885504663574,1.49742599847879,
-11.2103620711834));
#360924=CARTESIAN_POINT('Ctrl Pts',(0.0176462582822069,1.51251835619341,
-11.2011967381139));
#360925=CARTESIAN_POINT('Ctrl Pts',(-0.367479610380647,1.46701539997117,
-11.1814033901124));
#360926=CARTESIAN_POINT('Ctrl Pts',(-0.552787639076062,1.40768754034473,
-11.1708397573241));
#360927=CARTESIAN_POINT('Ctrl Pts',(-0.897460445162141,1.2184958232013,
-11.1490013537333));
#360928=CARTESIAN_POINT('Ctrl Pts',(-1.05207235524188,1.08780840341489,
-11.137932378636));
#360929=CARTESIAN_POINT('Ctrl Pts',(-1.29472412660984,0.781052781557282,
-11.1177368003468));
#360930=CARTESIAN_POINT('Ctrl Pts',(-1.3834101935851,0.610355838142167,
-11.1089086576746));
#360931=CARTESIAN_POINT('Ctrl Pts',(-1.49336680388985,0.240627863692861,
-11.0883682146496));
#360932=CARTESIAN_POINT('Ctrl Pts',(-1.51196816894718,0.0446142718790937,
-11.0774785706599));
#360933=CARTESIAN_POINT('Ctrl Pts',(-1.47273239710866,-0.347230352946177,
-11.0557094248363));
#360934=CARTESIAN_POINT('Ctrl Pts',(-1.4138082514145,-0.539148472729819,
-11.0450473070706));
#360935=CARTESIAN_POINT('Ctrl Pts',(-1.22867993426292,-0.881179913042688,
-11.0260455603865));
#360936=CARTESIAN_POINT('Ctrl Pts',(-1.10721948916014,-1.02967824115973,
-11.016335615811));
#360937=CARTESIAN_POINT('Ctrl Pts',(-0.809701240101673,-1.27801893022418,
-10.9951229099051));
#360938=CARTESIAN_POINT('Ctrl Pts',(-0.634710650244654,-1.37335103067755,
-10.9840555573236));
#360939=CARTESIAN_POINT('Ctrl Pts',(-0.30154176022217,-1.47717946544105,
-10.9651418384408));
#360940=CARTESIAN_POINT('Ctrl Pts',(-0.151084567659519,-1.5,-10.9572690596507));
#360941=CARTESIAN_POINT('Ctrl Pts',(2.63605293631073E-13,-1.5,-10.95));
#360942=CARTESIAN_POINT('Ctrl Pts',(1.16087695012368E-13,-1.5,-10.8875));
#360943=CARTESIAN_POINT('Ctrl Pts',(-0.12607676064798,-1.5,-10.8935658709749));
#360944=CARTESIAN_POINT('Ctrl Pts',(-0.25189800249301,-1.48410901447996,
-10.9000608645601));
#360945=CARTESIAN_POINT('Ctrl Pts',(-0.566554888468781,-1.40297903034609,
-10.9174534117155));
#360946=CARTESIAN_POINT('Ctrl Pts',(-0.746880905326093,-1.31586358480684,
-10.9285492247339));
#360947=CARTESIAN_POINT('Ctrl Pts',(-1.05724907259812,-1.08104490954594,
-10.9500045611236));
#360948=CARTESIAN_POINT('Ctrl Pts',(-1.18612043822808,-0.937856887421639,
-10.9601823326524));
#360949=CARTESIAN_POINT('Ctrl Pts',(-1.38728387069208,-0.604106562997156,
-10.9791316551545));
#360950=CARTESIAN_POINT('Ctrl Pts',(-1.45506683222575,-0.415127521990897,
-10.9894373598894));
#360951=CARTESIAN_POINT('Ctrl Pts',(-1.51254045432257,-0.0245493613436996,
-11.011136146592));
#360952=CARTESIAN_POINT('Ctrl Pts',(-1.50281578535621,0.173003596323905,
-11.0221113109069));
#360953=CARTESIAN_POINT('Ctrl Pts',(-1.40938478588014,0.547497830146236,
-11.0429165461192));
#360954=CARTESIAN_POINT('Ctrl Pts',(-1.3287711275756,0.721439543544025,
-11.0519427899709));
#360955=CARTESIAN_POINT('Ctrl Pts',(-1.10171477651428,1.03720116470672,
-11.0716381998982));
#360956=CARTESIAN_POINT('Ctrl Pts',(-0.954641944826474,1.17396799633267,
-11.0825133234683));
#360957=CARTESIAN_POINT('Ctrl Pts',(-0.62019323119029,1.37944559625263,
-11.1043122058145));
#360958=CARTESIAN_POINT('Ctrl Pts',(-0.437075268034176,1.44792561276039,
-11.1150246956054));
#360959=CARTESIAN_POINT('Ctrl Pts',(-0.055816838742389,1.51130709733111,
-11.1351285971309));
#360960=CARTESIAN_POINT('Ctrl Pts',(0.138640459998841,1.50597001067819,
-11.1440045086118));
#360961=CARTESIAN_POINT('Ctrl Pts',(0.520991754899377,1.42061906677836,
-11.1647712534176));
#360962=CARTESIAN_POINT('Ctrl Pts',(0.704622020668317,1.33906284634774,
-11.1758716192662));
#360963=CARTESIAN_POINT('Ctrl Pts',(1.02321105261424,1.1134153046469,-11.1974677284819));
#360964=CARTESIAN_POINT('Ctrl Pts',(1.15684899515003,0.973846282386629,
-11.207774304275));
#360965=CARTESIAN_POINT('Ctrl Pts',(1.36868058691161,0.645339360696826,
-11.2270912487547));
#360966=CARTESIAN_POINT('Ctrl Pts',(1.44226174592408,0.457888647055234,
-11.2370617418303));
#360967=CARTESIAN_POINT('Ctrl Pts',(1.51128132170044,0.0680317382552205,
-11.2587204589858));
#360968=CARTESIAN_POINT('Ctrl Pts',(1.50719160437547,-0.130287409999096,
-11.2697381894444));
#360969=CARTESIAN_POINT('Ctrl Pts',(1.42419767371233,-0.507677808311096,
-11.290704322684));
#360970=CARTESIAN_POINT('Ctrl Pts',(1.34855478158873,-0.683707597950999,
-11.2999428388736));
#360971=CARTESIAN_POINT('Ctrl Pts',(1.13060284376123,-1.00562906491852,
-11.3193713193429));
#360972=CARTESIAN_POINT('Ctrl Pts',(0.987476097404956,-1.14648231893667,
-11.330170098527));
#360973=CARTESIAN_POINT('Ctrl Pts',(0.658560520626497,-1.36162150541419,
-11.3519711451064));
#360974=CARTESIAN_POINT('Ctrl Pts',(0.4769145726165,-1.43536720848172,-11.3627590816067));
#360975=CARTESIAN_POINT('Ctrl Pts',(0.191716665583194,-1.49081159186927,
-11.3780207940673));
#360976=CARTESIAN_POINT('Ctrl Pts',(0.0958654997424546,-1.49999999749403,
-11.3828876689235));
#360977=CARTESIAN_POINT('Ctrl Pts',(3.92107660876271E-8,-1.5,-11.3874999981135));
#360978=CARTESIAN_POINT('Origin',(0.,1.30104260698261E-15,-17.7));
#360979=CARTESIAN_POINT('',(-7.75932627375354E-15,-1.5,-11.95));
#360980=CARTESIAN_POINT('',(-5.78875387247644E-14,-1.5,-11.8875));
#360981=CARTESIAN_POINT('',(-1.83697019872103E-16,-1.5,-17.7));
#360982=CARTESIAN_POINT('Ctrl Pts',(-1.69829428298129E-14,-1.5,-11.95));
#360983=CARTESIAN_POINT('Ctrl Pts',(0.100881833600506,-1.5,-11.9451463205179));
#360984=CARTESIAN_POINT('Ctrl Pts',(0.201721389943112,-1.48982502247338,
-11.9400120368366));
#360985=CARTESIAN_POINT('Ctrl Pts',(0.491473166153889,-1.43047394711926,
-11.9244227070218));
#360986=CARTESIAN_POINT('Ctrl Pts',(0.672540326423178,-1.3547990422388,
-11.9136090285204));
#360987=CARTESIAN_POINT('Ctrl Pts',(0.999350570959909,-1.13614461453851,
-11.8918116291962));
#360988=CARTESIAN_POINT('Ctrl Pts',(1.140997017159,-0.993818203206639,-11.8810431499501));
#360989=CARTESIAN_POINT('Ctrl Pts',(1.35558757929163,-0.669655885635057,
-11.8617141478942));
#360990=CARTESIAN_POINT('Ctrl Pts',(1.42940163132548,-0.492839924587643,
-11.8523799958104));
#360991=CARTESIAN_POINT('Ctrl Pts',(1.50850787934159,-0.114393961960379,
-11.8313552201089));
#360992=CARTESIAN_POINT('Ctrl Pts',(1.51049547604303,0.0841697409274456,
-11.8203239032818));
#360993=CARTESIAN_POINT('Ctrl Pts',(1.43735398200173,0.472775402794805,
-11.7987346998447));
#360994=CARTESIAN_POINT('Ctrl Pts',(1.36214842931913,0.658807877229377,
-11.7889028447167));
#360995=CARTESIAN_POINT('Ctrl Pts',(1.1475035811994,0.984875713542306,-11.7695182997489));
#360996=CARTESIAN_POINT('Ctrl Pts',(1.01240051157657,1.12328481092082,-11.7591734531316));
#360997=CARTESIAN_POINT('Ctrl Pts',(0.691303249455659,1.34601671031323,
-11.7375376566995));
#360998=CARTESIAN_POINT('Ctrl Pts',(0.50667682107433,1.42581559724676,-11.7264381777742));
#360999=CARTESIAN_POINT('Ctrl Pts',(0.12363865838816,1.50722857034544,-11.7057477741045));
#361000=CARTESIAN_POINT('Ctrl Pts',(-0.0704840469712229,1.51064725154874,
-11.6969045916964));
#361001=CARTESIAN_POINT('Ctrl Pts',(-0.450942230229227,1.44369139174563,
-11.6767399038253));
#361002=CARTESIAN_POINT('Ctrl Pts',(-0.633566219118868,1.37338076711471,
-11.6660003301567));
#361003=CARTESIAN_POINT('Ctrl Pts',(-0.966126547831251,1.16453331691648,
-11.6441986958203));
#361004=CARTESIAN_POINT('Ctrl Pts',(-1.11184311893041,1.02633504569465,
-11.6333490631573));
#361005=CARTESIAN_POINT('Ctrl Pts',(-1.33574551993269,0.708424259098842,
-11.6137456986831));
#361006=CARTESIAN_POINT('Ctrl Pts',(-1.41463392551725,0.533765819933085,
-11.6046536566629));
#361007=CARTESIAN_POINT('Ctrl Pts',(-1.50446432303768,0.158262306638579,
-11.5837923503688));
#361008=CARTESIAN_POINT('Ctrl Pts',(-1.51224681783949,-0.0395730290779647,
-11.5728014983845));
#361009=CARTESIAN_POINT('Ctrl Pts',(-1.45052698303864,-0.431588209997764,
-11.5510228772223));
#361010=CARTESIAN_POINT('Ctrl Pts',(-1.37982744089299,-0.621556200146737,
-11.5407881953655));
#361011=CARTESIAN_POINT('Ctrl Pts',(-1.17295041156061,-0.954329063619033,
-11.521591128999));
#361012=CARTESIAN_POINT('Ctrl Pts',(-1.04190006093877,-1.09589150221479,
-11.5113536761039));
#361013=CARTESIAN_POINT('Ctrl Pts',(-0.727762512368969,-1.326576265309,
-11.4898318161655));
#361014=CARTESIAN_POINT('Ctrl Pts',(-0.545914193739363,-1.41117979458698,
-11.4787325368206));
#361015=CARTESIAN_POINT('Ctrl Pts',(-0.237063288725948,-1.48593301082516,
-11.461796462496));
#361016=CARTESIAN_POINT('Ctrl Pts',(-0.118619887738532,-1.5,-11.4557071020098));
#361017=CARTESIAN_POINT('Ctrl Pts',(6.81746326058885E-14,-1.5,-11.45));
#361018=CARTESIAN_POINT('Ctrl Pts',(3.92107660876271E-8,-1.5,-11.3874999981135));
#361019=CARTESIAN_POINT('Ctrl Pts',(-0.0950530796326291,-1.50000000248474,
-11.3920732434951));
#361020=CARTESIAN_POINT('Ctrl Pts',(-0.190095831220883,-1.49096664224319,
-11.3968969165483));
#361021=CARTESIAN_POINT('Ctrl Pts',(-0.479809379763385,-1.43513269158633,
-11.4123867092254));
#361022=CARTESIAN_POINT('Ctrl Pts',(-0.666252458474244,-1.35864583147218,
-11.4234815910354));
#361023=CARTESIAN_POINT('Ctrl Pts',(-0.991963171491764,-1.14142976957814,
-11.445186134519));
#361024=CARTESIAN_POINT('Ctrl Pts',(-1.129775168227,-1.00522676258199,-11.4556000341644));
#361025=CARTESIAN_POINT('Ctrl Pts',(-1.34963990277553,-0.683716883318096,
-11.475109111117));
#361026=CARTESIAN_POINT('Ctrl Pts',(-1.42783852471113,-0.500293352745201,
-11.4847059248475));
#361027=CARTESIAN_POINT('Ctrl Pts',(-1.50858351472943,-0.114056565279965,
-11.5061635241511));
#361028=CARTESIAN_POINT('Ctrl Pts',(-1.51050448345982,0.0849027709680435,
-11.5172168206094));
#361029=CARTESIAN_POINT('Ctrl Pts',(-1.43862290569877,0.465276123774864,
-11.5383486735431));
#361030=CARTESIAN_POINT('Ctrl Pts',(-1.36817728516983,0.643565573521427,
-11.5478836944957));
#361031=CARTESIAN_POINT('Ctrl Pts',(-1.15978950001239,0.971817636837456,
-11.5670278693537));
#361032=CARTESIAN_POINT('Ctrl Pts',(-1.02090607423869,1.11681147207431,
-11.5777375078261));
#361033=CARTESIAN_POINT('Ctrl Pts',(-0.698066542869175,1.3418770776122,
-11.5995219543972));
#361034=CARTESIAN_POINT('Ctrl Pts',(-0.518116473811858,1.42108953555501,
-11.6103801521854));
#361035=CARTESIAN_POINT('Ctrl Pts',(-0.141683055304006,1.50545774145914,
-11.6308348747528));
#361036=CARTESIAN_POINT('Ctrl Pts',(0.0509131338252352,1.51125195179322,
-11.6396370050768));
#361037=CARTESIAN_POINT('Ctrl Pts',(0.437041528852499,1.44881299277959,
-11.6599490316725));
#361038=CARTESIAN_POINT('Ctrl Pts',(0.62623629134813,1.37763484275265,-11.6710288397613));
#361039=CARTESIAN_POINT('Ctrl Pts',(0.959042063487257,1.169314430107,-11.692827643068));
#361040=CARTESIAN_POINT('Ctrl Pts',(1.10105809980976,1.03670005261147,-11.7033441255096));
#361041=CARTESIAN_POINT('Ctrl Pts',(1.32908189525078,0.722399107477091,
-11.7230455072922));
#361042=CARTESIAN_POINT('Ctrl Pts',(1.41191038943793,0.542991320198872,
-11.7323338155445));
#361043=CARTESIAN_POINT('Ctrl Pts',(1.50442295622243,0.160573439476918,
-11.7535792533624));
#361044=CARTESIAN_POINT('Ctrl Pts',(1.51246790529916,-0.0388527502376838,
-11.7646584861243));
#361045=CARTESIAN_POINT('Ctrl Pts',(1.45190806340713,-0.422154644343116,
-11.7859530357969));
#361046=CARTESIAN_POINT('Ctrl Pts',(1.38666899163276,-0.60278637597622,
-11.7958612563664));
#361047=CARTESIAN_POINT('Ctrl Pts',(1.18788554968428,-0.937259716387997,
-11.8147161552989));
#361048=CARTESIAN_POINT('Ctrl Pts',(1.05335607453411,-1.08625159653144,
-11.8253273710272));
#361049=CARTESIAN_POINT('Ctrl Pts',(0.73687657244448,-1.32104540776602,
-11.8470760484829));
#361050=CARTESIAN_POINT('Ctrl Pts',(0.558779034676864,-1.40567451730944,
-11.8579955788624));
#361051=CARTESIAN_POINT('Ctrl Pts',(0.248449127703398,-1.4845415311917,
-11.8751170838587));
#361052=CARTESIAN_POINT('Ctrl Pts',(0.124349321223437,-1.50000000000001,
-11.8815172404932));
#361053=CARTESIAN_POINT('Ctrl Pts',(-1.15081555396301E-13,-1.5,-11.8875));
#361054=CARTESIAN_POINT('Origin',(0.,1.30104260698261E-15,-17.7));
#361055=CARTESIAN_POINT('',(-7.43743506404469E-14,-1.5,-12.45));
#361056=CARTESIAN_POINT('',(-9.08611625561309E-14,-1.5,-12.3875));
#361057=CARTESIAN_POINT('',(-1.83697019872103E-16,-1.5,-17.7));
#361058=CARTESIAN_POINT('Ctrl Pts',(-1.49255607873044E-13,-1.5,-12.45));
#361059=CARTESIAN_POINT('Ctrl Pts',(0.129273918175039,-1.50000000000001,
-12.4437803057119));
#361060=CARTESIAN_POINT('Ctrl Pts',(0.25823729718224,-1.48329297796134,
-12.4371114683009));
#361061=CARTESIAN_POINT('Ctrl Pts',(0.572723955290597,-1.40007740134056,
-12.4196691781129));
#361062=CARTESIAN_POINT('Ctrl Pts',(0.750144096931693,-1.3135856707735,
-12.4087304994969));
#361063=CARTESIAN_POINT('Ctrl Pts',(1.06435712568823,-1.07547182691069,
-12.3869986446617));
#361064=CARTESIAN_POINT('Ctrl Pts',(1.19735454561133,-0.925129649588097,
-12.3764236317199));
#361065=CARTESIAN_POINT('Ctrl Pts',(1.39280290168056,-0.588526364225109,
-12.357670027044));
#361066=CARTESIAN_POINT('Ctrl Pts',(1.45623457230694,-0.407063441158707,
-12.3476146356199));
#361067=CARTESIAN_POINT('Ctrl Pts',(1.51282311873122,-0.0227616208969719,
-12.3262645344943));
#361068=CARTESIAN_POINT('Ctrl Pts',(1.50263225416625,0.176784345586005,
-12.3151786474674));
#361069=CARTESIAN_POINT('Ctrl Pts',(1.40603464232576,0.557833883882915,
-12.2940092286732));
#361070=CARTESIAN_POINT('Ctrl Pts',(1.3215977154996,0.735854831854552,-12.2848116544044));
#361071=CARTESIAN_POINT('Ctrl Pts',(1.09071795642565,1.04760785595713,-12.2650436405916));
#361072=CARTESIAN_POINT('Ctrl Pts',(0.947240611682627,1.17892568620947,
-12.2544928661171));
#361073=CARTESIAN_POINT('Ctrl Pts',(0.611987873045726,1.3840540163624,-12.232665002038));
#361074=CARTESIAN_POINT('Ctrl Pts',(0.421856785171934,1.45333657814123,
-12.2215928002026));
#361075=CARTESIAN_POINT('Ctrl Pts',(0.0351065239375032,1.51167222359196,
-12.2013648349873));
#361076=CARTESIAN_POINT('Ctrl Pts',(-0.157180541384606,1.50388936038236,
-12.1925456854651));
#361077=CARTESIAN_POINT('Ctrl Pts',(-0.532704648611216,1.41571270707977,
-12.1720289219516));
#361078=CARTESIAN_POINT('Ctrl Pts',(-0.71201086726083,1.33455944470295,
-12.1611477901963));
#361079=CARTESIAN_POINT('Ctrl Pts',(-1.03261081878757,1.10599576904317,
-12.139373926846));
#361080=CARTESIAN_POINT('Ctrl Pts',(-1.16995145118631,0.959557326068837,
-12.1286983880618));
#361081=CARTESIAN_POINT('Ctrl Pts',(-1.3749134520388,0.629070993015123,
-12.1096569732798));
#361082=CARTESIAN_POINT('Ctrl Pts',(-1.44350117252979,0.449954696299029,
-12.0999974831277));
#361083=CARTESIAN_POINT('Ctrl Pts',(-1.51136358881569,0.0685287076069453,
-12.0788071504226));
#361084=CARTESIAN_POINT('Ctrl Pts',(-1.50726802756032,-0.130617691366746,
-12.0677434615907));
#361085=CARTESIAN_POINT('Ctrl Pts',(-1.42232495427812,-0.515513190831157,
-12.0463603782871));
#361086=CARTESIAN_POINT('Ctrl Pts',(-1.34247474812846,-0.697500796762078,
-12.0368814909687));
#361087=CARTESIAN_POINT('Ctrl Pts',(-1.11971067389336,-1.01646080816819,
-12.0173037491331));
#361088=CARTESIAN_POINT('Ctrl Pts',(-0.980400167431732,-1.15140818962697,
-12.006852630892));
#361089=CARTESIAN_POINT('Ctrl Pts',(-0.652151238334278,-1.36550129028978,
-11.9851127163534));
#361090=CARTESIAN_POINT('Ctrl Pts',(-0.46471769226152,-1.44011995248529,
-11.9740220750469));
#361091=CARTESIAN_POINT('Ctrl Pts',(-0.179477568288609,-1.49194945314334,
-11.958858744832));
#361092=CARTESIAN_POINT('Ctrl Pts',(-0.0897329405635131,-1.5,-11.9543172781158));
#361093=CARTESIAN_POINT('Ctrl Pts',(-1.66705089355558E-14,-1.5,-11.95));
#361094=CARTESIAN_POINT('Ctrl Pts',(-1.15591380429657E-13,-1.5,-11.8875));
#361095=CARTESIAN_POINT('Ctrl Pts',(-0.0652848605868303,-1.49999999999999,
-11.8906410193195));
#361096=CARTESIAN_POINT('Ctrl Pts',(-0.130627004965125,-1.49573835196629,
-11.8939031738187));
#361097=CARTESIAN_POINT('Ctrl Pts',(-0.394661743495974,-1.46100883160568,
-11.9075712599982));
#361098=CARTESIAN_POINT('Ctrl Pts',(-0.586417356539178,-1.39513512522614,
-11.9186269314095));
#361099=CARTESIAN_POINT('Ctrl Pts',(-0.925959609152179,-1.19576722898065,
-11.940501162773));
#361100=CARTESIAN_POINT('Ctrl Pts',(-1.07201374331102,-1.06680038780183,
-11.9511106078341));
#361101=CARTESIAN_POINT('Ctrl Pts',(-1.30795895391836,-0.759598097932127,
-11.9709959240131));
#361102=CARTESIAN_POINT('Ctrl Pts',(-1.39523546176121,-0.584012000755381,
-11.980054888847));
#361103=CARTESIAN_POINT('Ctrl Pts',(-1.49903493494599,-0.20542738546847,
-12.001087367474));
#361104=CARTESIAN_POINT('Ctrl Pts',(-1.51303243828964,-0.00572450358818515,
-12.0121819720229));
#361105=CARTESIAN_POINT('Ctrl Pts',(-1.46351743699624,0.380165488829691,
-12.033620304935));
#361106=CARTESIAN_POINT('Ctrl Pts',(-1.40333733761183,0.563096032260082,
-12.0437831129034));
#361107=CARTESIAN_POINT('Ctrl Pts',(-1.2137649769442,0.903477291464536,
-12.0626931828592));
#361108=CARTESIAN_POINT('Ctrl Pts',(-1.08348466334011,1.05622395116131,
-12.0730437073621));
#361109=CARTESIAN_POINT('Ctrl Pts',(-0.773201313986828,1.30019840059802,
-12.0947492900082));
#361110=CARTESIAN_POINT('Ctrl Pts',(-0.597013697489189,1.38994075745238,
-12.1057189639052));
#361111=CARTESIAN_POINT('Ctrl Pts',(-0.225668498337577,1.49505966223445,
-12.1265052877069));
#361112=CARTESIAN_POINT('Ctrl Pts',(-0.0346407051353212,1.51159478969829,
-12.1355112708055));
#361113=CARTESIAN_POINT('Ctrl Pts',(0.352246354109036,1.47155875118354,
-12.1552374953032));
#361114=CARTESIAN_POINT('Ctrl Pts',(0.544033157216475,1.41193882215949,
-12.1661209513095));
#361115=CARTESIAN_POINT('Ctrl Pts',(0.888535142663614,1.22392451774981,
-12.1879184303793));
#361116=CARTESIAN_POINT('Ctrl Pts',(1.03894680127538,1.09913115010637,-12.1986215971129));
#361117=CARTESIAN_POINT('Ctrl Pts',(1.28355750724515,0.799809154688375,
-12.2187049350638));
#361118=CARTESIAN_POINT('Ctrl Pts',(1.37565998347666,0.628312544963968,
-12.227593747502));
#361119=CARTESIAN_POINT('Ctrl Pts',(1.4916507986338,0.254050617991306,-12.2483860767783));
#361120=CARTESIAN_POINT('Ctrl Pts',(1.51215487649894,0.0542431023100071,
-12.2594864943161));
#361121=CARTESIAN_POINT('Ctrl Pts',(1.47475977951007,-0.334237654454839,
-12.2810687585809));
#361122=CARTESIAN_POINT('Ctrl Pts',(1.4201240034924,-0.519519887009746,
-12.291362215945));
#361123=CARTESIAN_POINT('Ctrl Pts',(1.24035558751452,-0.866811580439447,
-12.3106561989133));
#361124=CARTESIAN_POINT('Ctrl Pts',(1.11411578699525,-1.02402320319891,
-12.3206755015169));
#361125=CARTESIAN_POINT('Ctrl Pts',(0.809936777076213,-1.27772235058463,
-12.3423575194936));
#361126=CARTESIAN_POINT('Ctrl Pts',(0.635863081781533,-1.37268067289867,
-12.3533703752388));
#361127=CARTESIAN_POINT('Ctrl Pts',(0.303076447178655,-1.47693942444835,
-12.3722776560933));
#361128=CARTESIAN_POINT('Ctrl Pts',(0.151876448244223,-1.50000000000002,
-12.3801928409769));
#361129=CARTESIAN_POINT('Ctrl Pts',(-1.83152104593631E-13,-1.5,-12.3875));
#361130=CARTESIAN_POINT('Origin',(0.,1.30104260698261E-15,-17.7));
#361131=CARTESIAN_POINT('',(-5.78875387247644E-14,-1.5,-12.95));
#361132=CARTESIAN_POINT('',(-1.83697019872103E-16,-1.5,-12.8875));
#361133=CARTESIAN_POINT('',(-1.83697019872103E-16,-1.5,-17.7));
#361134=CARTESIAN_POINT('Ctrl Pts',(-1.16399945238044E-13,-1.5,-12.95));
#361135=CARTESIAN_POINT('Ctrl Pts',(0.158876952576763,-1.50000000000001,
-12.9423560290551));
#361136=CARTESIAN_POINT('Ctrl Pts',(0.316934376671936,-1.47476380404689,
-12.9340504822496));
#361137=CARTESIAN_POINT('Ctrl Pts',(0.655117690859527,-1.36363573904858,
-12.914692739265));
#361138=CARTESIAN_POINT('Ctrl Pts',(0.828076727203405,-1.26608438701772,
-12.9036614839704));
#361139=CARTESIAN_POINT('Ctrl Pts',(1.12806327860616,-1.00845306391603,
-12.8820719486449));
#361140=CARTESIAN_POINT('Ctrl Pts',(1.25157899640202,-0.850310207670071,
-12.8722394559816));
#361141=CARTESIAN_POINT('Ctrl Pts',(1.42665630726749,-0.501394151761404,
-12.8528552306534));
#361142=CARTESIAN_POINT('Ctrl Pts',(1.47897883859234,-0.315190147192983,
-12.8425105637329));
#361143=CARTESIAN_POINT('Ctrl Pts',(1.51133966887728,0.0742508797942082,
-12.8208749511225));
#361144=CARTESIAN_POINT('Ctrl Pts',(1.48814391899043,0.274041623011249,
-12.8097754653882));
#361145=CARTESIAN_POINT('Ctrl Pts',(1.3671483554754,0.646475451295437,-12.7890846971502));
#361146=CARTESIAN_POINT('Ctrl Pts',(1.2730547677852,0.816305903343349,-12.7802413787577));
#361147=CARTESIAN_POINT('Ctrl Pts',(1.02485301882479,1.11232624886059,-12.7600769791676));
#361148=CARTESIAN_POINT('Ctrl Pts',(0.872656584289035,1.23533438080045,
-12.749337532243));
#361149=CARTESIAN_POINT('Ctrl Pts',(0.525518549519603,1.41893221299394,
-12.7275359059748));
#361150=CARTESIAN_POINT('Ctrl Pts',(0.33297967954763,1.47603634600655,-12.7166861493571));
#361151=CARTESIAN_POINT('Ctrl Pts',(-0.0542890167421315,1.51100424642432,
-12.6970823449523));
#361152=CARTESIAN_POINT('Ctrl Pts',(-0.244992999672171,1.49200322269456,
-12.6879906361045));
#361153=CARTESIAN_POINT('Ctrl Pts',(-0.615108227667013,1.38206416992609,
-12.6671295963181));
#361154=CARTESIAN_POINT('Ctrl Pts',(-0.790333414720495,1.2898950332486,
-12.6561388167787));
#361155=CARTESIAN_POINT('Ctrl Pts',(-1.09754102144741,1.04161475435297,
-12.6344616094948));
#361156=CARTESIAN_POINT('Ctrl Pts',(-1.2257837313118,0.887112892370766,
-12.6242840495761));
#361157=CARTESIAN_POINT('Ctrl Pts',(-1.41090380162242,0.543948766362077,
-12.605219375909));
#361158=CARTESIAN_POINT('Ctrl Pts',(-1.4686507071494,0.359961059105703,
-12.594997836617));
#361159=CARTESIAN_POINT('Ctrl Pts',(-1.51283723657042,-0.0271168915276431,
-12.5734935060262));
#361160=CARTESIAN_POINT('Ctrl Pts',(-1.49597450164886,-0.226891212692761,
-12.5623949326282));
#361161=CARTESIAN_POINT('Ctrl Pts',(-1.3867891322557,-0.603589178432375,
-12.5414672678648));
#361162=CARTESIAN_POINT('Ctrl Pts',(-1.29738422067913,-0.77736340783658,
-12.5324936660921));
#361163=CARTESIAN_POINT('Ctrl Pts',(-1.05762498672902,-1.08111224118951,
-12.5125207769772));
#361164=CARTESIAN_POINT('Ctrl Pts',(-0.909644569683913,-1.20826568059143,
-12.5018690258592));
#361165=CARTESIAN_POINT('Ctrl Pts',(-0.568774928134204,-1.40215707843199,
-12.4800830554213));
#361166=CARTESIAN_POINT('Ctrl Pts',(-0.378052343015115,-1.46514290080414,
-12.4691573045894));
#361167=CARTESIAN_POINT('Ctrl Pts',(-0.12054655675434,-1.49637094630723,
-12.455900605963));
#361168=CARTESIAN_POINT('Ctrl Pts',(-0.0602444439907949,-1.49999999999999,
-12.4528985121629));
#361169=CARTESIAN_POINT('Ctrl Pts',(-1.48565004261022E-13,-1.5,-12.45));
#361170=CARTESIAN_POINT('Ctrl Pts',(-1.8153862809239E-13,-1.5,-12.3875));
#361171=CARTESIAN_POINT('Ctrl Pts',(-0.0374929816783926,-1.5,-12.3893038819221));
#361172=CARTESIAN_POINT('Ctrl Pts',(-0.0750234464464321,-1.49859432408929,
-12.3911486138032));
#361173=CARTESIAN_POINT('Ctrl Pts',(-0.310834813771295,-1.48085636003662,
-12.4029868147272));
#361174=CARTESIAN_POINT('Ctrl Pts',(-0.504193695961855,-1.42664676038125,
-12.4137956204967));
#361175=CARTESIAN_POINT('Ctrl Pts',(-0.854282208926748,-1.2481551406557,
-12.435597362478));
#361176=CARTESIAN_POINT('Ctrl Pts',(-1.00849825756739,-1.12722328348696,
-12.4463763038324));
#361177=CARTESIAN_POINT('Ctrl Pts',(-1.26079688771879,-0.834996038406131,
-12.4666324508097));
#361178=CARTESIAN_POINT('Ctrl Pts',(-1.35715776934335,-0.667045853726193,
-12.4754418970152));
#361179=CARTESIAN_POINT('Ctrl Pts',(-1.48382942208322,-0.296722390016991,
-12.4960154227769));
#361180=CARTESIAN_POINT('Ctrl Pts',(-1.51009088547731,-0.0969934152972635,
-12.507111476928));
#361181=CARTESIAN_POINT('Ctrl Pts',(-1.48347839072346,0.293462146888296,
-12.5288034526049));
#361182=CARTESIAN_POINT('Ctrl Pts',(-1.43380448896476,0.480679727579932,
-12.53920442931));
#361183=CARTESIAN_POINT('Ctrl Pts',(-1.26405217312614,0.831418736778474,
-12.5586899298211));
#361184=CARTESIAN_POINT('Ctrl Pts',(-1.14359126239354,0.990608365372646,
-12.568329172106));
#361185=CARTESIAN_POINT('Ctrl Pts',(-0.848358771487759,1.25263385222588,
-12.5898120376934));
#361186=CARTESIAN_POINT('Ctrl Pts',(-0.67670373428794,1.35309855913209,
-12.6008614808243));
#361187=CARTESIAN_POINT('Ctrl Pts',(-0.310977376334873,1.47966238232852,
-12.6219731601809));
#361188=CARTESIAN_POINT('Ctrl Pts',(-0.121276295927422,1.50710633513481,
-12.6314676932935));
#361189=CARTESIAN_POINT('Ctrl Pts',(0.267112603342264,1.48936011891211,
-12.6506470133728));
#361190=CARTESIAN_POINT('Ctrl Pts',(0.461952664132715,1.44087424484157,
-12.6613680900036));
#361191=CARTESIAN_POINT('Ctrl Pts',(0.817619890410771,1.27255732995747,
-12.6831556072643));
#361192=CARTESIAN_POINT('Ctrl Pts',(0.97572465732348,1.15580070930254,-12.6940056658717));
#361193=CARTESIAN_POINT('Ctrl Pts',(1.23602733972881,0.871060496173528,
-12.7144389348828));
#361194=CARTESIAN_POINT('Ctrl Pts',(1.33680365595805,0.706727529185695,
-12.7232373594897));
#361195=CARTESIAN_POINT('Ctrl Pts',(1.47445973273482,0.340592604871063,
-12.7435781886183));
#361196=CARTESIAN_POINT('Ctrl Pts',(1.50668752861793,0.141113819903124,
-12.7546603433388));
#361197=CARTESIAN_POINT('Ctrl Pts',(1.49130621154247,-0.251075049662532,
-12.7764486138702));
#361198=CARTESIAN_POINT('Ctrl Pts',(1.44682930119438,-0.440154664538035,
-12.7869530369188));
#361199=CARTESIAN_POINT('Ctrl Pts',(1.28739409514771,-0.794363222880267,
-12.8066312901601));
#361200=CARTESIAN_POINT('Ctrl Pts',(1.1727403962829,-0.955556720159954,
-12.8159530769364));
#361201=CARTESIAN_POINT('Ctrl Pts',(0.88669793180305,-1.22589150798183,
-12.8372246010871));
#361202=CARTESIAN_POINT('Ctrl Pts',(0.717681680755148,-1.33190577252514,
-12.8483012399388));
#361203=CARTESIAN_POINT('Ctrl Pts',(0.362630102147741,-1.46687280253244,
-12.8691327511461));
#361204=CARTESIAN_POINT('Ctrl Pts',(0.182013319335047,-1.5,-12.8787428800905));
#361205=CARTESIAN_POINT('Ctrl Pts',(-1.59594559789866E-15,-1.5,-12.8875));
#361206=CARTESIAN_POINT('Origin',(0.,1.30104260698261E-15,-17.7));
#361207=CARTESIAN_POINT('',(6.17379976491385E-9,-1.5,-13.4499999994059));
#361208=CARTESIAN_POINT('',(3.27899268114955E-14,-1.5,-13.3875));
#361209=CARTESIAN_POINT('',(-1.83697019872103E-16,-1.5,-17.7));
#361210=CARTESIAN_POINT('Ctrl Pts',(1.23475991584132E-8,-1.5,-13.4499999994059));
#361211=CARTESIAN_POINT('Ctrl Pts',(0.189148975563307,-1.49999999844298,
-13.4408995656269));
#361212=CARTESIAN_POINT('Ctrl Pts',(0.376690429974303,-1.46422167503491,
-13.4308826308776));
#361213=CARTESIAN_POINT('Ctrl Pts',(0.736633814777829,-1.32156048455152,
-13.409602035855));
#361214=CARTESIAN_POINT('Ctrl Pts',(0.904354826486513,-1.21297087800871,
-13.3985161769573));
#361215=CARTESIAN_POINT('Ctrl Pts',(1.18606966936468,-0.938803382033804,
-13.3773464014827));
#361216=CARTESIAN_POINT('Ctrl Pts',(1.29803119767387,-0.776671648115806,
-13.3681484248953));
#361217=CARTESIAN_POINT('Ctrl Pts',(1.45259433871836,-0.42085298006497,
-13.3483807211147));
#361218=CARTESIAN_POINT('Ctrl Pts',(1.49458892567519,-0.23094188314,-13.3378301046189));
#361219=CARTESIAN_POINT('Ctrl Pts',(1.50462756389352,0.161957317004072,
-13.3160023712775));
#361220=CARTESIAN_POINT('Ctrl Pts',(1.46957234297039,0.3612576400713,-13.3049301311071));
#361221=CARTESIAN_POINT('Ctrl Pts',(1.32673541454486,0.725368121781877,
-13.2847017710121));
#361222=CARTESIAN_POINT('Ctrl Pts',(1.22385906373864,0.888008057584638,
-13.2758827228365));
#361223=CARTESIAN_POINT('Ctrl Pts',(0.959747099080752,1.16914578135365,
-13.2553662487964));
#361224=CARTESIAN_POINT('Ctrl Pts',(0.799819539093315,1.28386008899408,
-13.2444852219334));
#361225=CARTESIAN_POINT('Ctrl Pts',(0.441586475710377,1.44724329476693,
-13.2227113032527));
#361226=CARTESIAN_POINT('Ctrl Pts',(0.246098944072605,1.49297421001171,
-13.2120356018003));
#361227=CARTESIAN_POINT('Ctrl Pts',(-0.142590608807902,1.50525249012568,
-13.1929937036315));
#361228=CARTESIAN_POINT('Ctrl Pts',(-0.332004710784623,1.47510255039801,
-13.1833348200824));
#361229=CARTESIAN_POINT('Ctrl Pts',(-0.696265710086782,1.34317897081802,
-13.162144760705));
#361230=CARTESIAN_POINT('Ctrl Pts',(-0.866688171311859,1.24006818470157,
-13.151081117713));
#361231=CARTESIAN_POINT('Ctrl Pts',(-1.1575612640928,0.974071462272501,
-13.1296976816664));
#361232=CARTESIAN_POINT('Ctrl Pts',(-1.27525175459758,0.813928698898369,
-13.1202182610499));
#361233=CARTESIAN_POINT('Ctrl Pts',(-1.44011441929941,0.461535143221553,
-13.1006408412901));
#361234=CARTESIAN_POINT('Ctrl Pts',(-1.48733570237035,0.273418130482792,
-13.0901898961379));
#361235=CARTESIAN_POINT('Ctrl Pts',(-1.50864005363079,-0.117897423145407,
-13.0684501431586));
#361236=CARTESIAN_POINT('Ctrl Pts',(-1.47955490051629,-0.317529377045197,
-13.057359479053));
#361237=CARTESIAN_POINT('Ctrl Pts',(-1.34767507955946,-0.685884446848146,
-13.0368953085084));
#361238=CARTESIAN_POINT('Ctrl Pts',(-1.24922625664541,-0.852115139450408,
-13.028100227978));
#361239=CARTESIAN_POINT('Ctrl Pts',(-0.993144863791779,-1.14081747479882,
-13.0077599969045));
#361240=CARTESIAN_POINT('Ctrl Pts',(-0.83708138983694,-1.25979574668122,
-12.9969464375163));
#361241=CARTESIAN_POINT('Ctrl Pts',(-0.484325304368011,-1.43351148257176,
-12.9751490153329));
#361242=CARTESIAN_POINT('Ctrl Pts',(-0.290246273872271,-1.48502724998096,
-12.9643803900853));
#361243=CARTESIAN_POINT('Ctrl Pts',(-0.061166760094827,-1.49906552881572,
-12.95296884465));
#361244=CARTESIAN_POINT('Ctrl Pts',(-0.0305694474716846,-1.5,-12.9514707732272));
#361245=CARTESIAN_POINT('Ctrl Pts',(-1.15591380429657E-13,-1.5,-12.95));
#361246=CARTESIAN_POINT('Ctrl Pts',(-1.83697019872103E-16,-1.5,-12.8875));
#361247=CARTESIAN_POINT('Ctrl Pts',(-0.00807884865481996,-1.5,-12.8878886937871));
#361248=CARTESIAN_POINT('Ctrl Pts',(-0.0161602766706464,-1.49993473226773,
-12.8882793246664));
#361249=CARTESIAN_POINT('Ctrl Pts',(-0.223037962130807,-1.49659066907362,
-12.8983256225932));
#361250=CARTESIAN_POINT('Ctrl Pts',(-0.419188387790651,-1.4538860378266,
-12.9089491541048));
#361251=CARTESIAN_POINT('Ctrl Pts',(-0.780151786748742,-1.29594949218373,
-12.9307031400023));
#361252=CARTESIAN_POINT('Ctrl Pts',(-0.942045516713052,-1.18350295005882,
-12.9416157707759));
#361253=CARTESIAN_POINT('Ctrl Pts',(-1.21031233322143,-0.906324473969546,
-12.9622221661166));
#361254=CARTESIAN_POINT('Ctrl Pts',(-1.31548035152035,-0.745510580599391,
-12.9710827455223));
#361255=CARTESIAN_POINT('Ctrl Pts',(-1.46393442269762,-0.383629870391432,
-12.9911872294227));
#361256=CARTESIAN_POINT('Ctrl Pts',(-1.50206316794945,-0.184567223381819,
-13.0022462653677));
#361257=CARTESIAN_POINT('Ctrl Pts',(-1.49784697651995,0.209023161470686,
-13.0241123978595));
#361258=CARTESIAN_POINT('Ctrl Pts',(-1.4585649562512,0.399800978318997,
-13.0347111654622));
#361259=CARTESIAN_POINT('Ctrl Pts',(-1.30928839502881,0.757346329732696,
-13.0545747960963));
#361260=CARTESIAN_POINT('Ctrl Pts',(-1.20021246007597,0.920492389190269,
-13.0636573174573));
#361261=CARTESIAN_POINT('Ctrl Pts',(-0.923182794605771,1.19875428317566,
-13.0847154105068));
#361262=CARTESIAN_POINT('Ctrl Pts',(-0.75690113054832,1.31010422518364,
-13.0958086947436));
#361263=CARTESIAN_POINT('Ctrl Pts',(-0.397560799802422,1.45887984296568,
-13.117230120517));
#361264=CARTESIAN_POINT('Ctrl Pts',(-0.208979560478688,1.49757686314416,
-13.1273781568515));
#361265=CARTESIAN_POINT('Ctrl Pts',(0.180529207953534,1.50229867163426,
-13.1462495675573));
#361266=CARTESIAN_POINT('Ctrl Pts',(0.377822901886829,1.46519477880051,
-13.1566448245426));
#361267=CARTESIAN_POINT('Ctrl Pts',(0.743702509879271,1.31728437099402,
-13.1783568378287));
#361268=CARTESIAN_POINT('Ctrl Pts',(0.909111631589959,1.20907086766095,
-13.1893210185557));
#361269=CARTESIAN_POINT('Ctrl Pts',(1.18493942771686,0.939180171635513,
-13.2100887533629));
#361270=CARTESIAN_POINT('Ctrl Pts',(1.29428564810427,0.781636310928492,
-13.219075760504));
#361271=CARTESIAN_POINT('Ctrl Pts',(1.45191928137376,0.426021078425527,
-13.2388321623097));
#361272=CARTESIAN_POINT('Ctrl Pts',(1.49554556850097,0.229973772428518,
-13.2497236793096));
#361273=CARTESIAN_POINT('Ctrl Pts',(1.50369690667037,-0.162351848758911,
-13.2715195471533));
#361274=CARTESIAN_POINT('Ctrl Pts',(1.47022567902877,-0.354842241618453,
-13.2822134578677));
#361275=CARTESIAN_POINT('Ctrl Pts',(1.33215624580652,-0.71597793363767,
-13.3022765518688));
#361276=CARTESIAN_POINT('Ctrl Pts',(1.22907824959446,-0.88126846710937,
-13.3111789581204));
#361277=CARTESIAN_POINT('Ctrl Pts',(0.961938307621396,-1.1679948129568,
-13.3319963552892));
#361278=CARTESIAN_POINT('Ctrl Pts',(0.798818223935141,-1.28507501721829,
-13.3430967018709));
#361279=CARTESIAN_POINT('Ctrl Pts',(0.44327680231076,-1.44572266131707,
-13.3646651310528));
#361280=CARTESIAN_POINT('Ctrl Pts',(0.255415543169415,-1.4904339350922,
-13.3749455899245));
#361281=CARTESIAN_POINT('Ctrl Pts',(0.0427931613907333,-1.49954254591616,
-13.3854284060048));
#361282=CARTESIAN_POINT('Ctrl Pts',(0.0213882799085289,-1.5,-13.3864709559031));
#361283=CARTESIAN_POINT('Ctrl Pts',(6.5763550642863E-14,-1.5,-13.3875));
#361284=CARTESIAN_POINT('Origin',(0.,1.30104260698261E-15,-17.7));
#361285=CARTESIAN_POINT('',(6.1641847663942E-14,-1.5,-13.95));
#361286=CARTESIAN_POINT('',(1.23467392347757E-13,-1.5,-13.8875));
#361287=CARTESIAN_POINT('',(-1.83697019872103E-16,-1.5,-17.7));
#361288=CARTESIAN_POINT('Ctrl Pts',(1.23467392347756E-13,-1.5,-13.95));
#361289=CARTESIAN_POINT('Ctrl Pts',(0.0273727606550288,-1.5,-13.9486830274389));
#361290=CARTESIAN_POINT('Ctrl Pts',(0.0547705664019769,-1.4992507445935,
-13.9473440372451));
#361291=CARTESIAN_POINT('Ctrl Pts',(0.27349293350586,-1.48725212293488,
-13.9364874574053));
#361292=CARTESIAN_POINT('Ctrl Pts',(0.461021133040364,-1.44019285401277,
-13.926157800784));
#361293=CARTESIAN_POINT('Ctrl Pts',(0.814973605767246,-1.27493031347283,
-13.9045376283737));
#361294=CARTESIAN_POINT('Ctrl Pts',(0.976806088535854,-1.15563365119737,
-13.8934376632419));
#361295=CARTESIAN_POINT('Ctrl Pts',(1.24005780212886,-0.865642475645971,
-13.8727166488343));
#361296=CARTESIAN_POINT('Ctrl Pts',(1.34081010114396,-0.699504708701909,
-13.8638613727056));
#361297=CARTESIAN_POINT('Ctrl Pts',(1.47445308365235,-0.336977220166086,
-13.8437209566758));
#361298=CARTESIAN_POINT('Ctrl Pts',(1.5056086078487,-0.143858005698238,
-13.8329921114276));
#361299=CARTESIAN_POINT('Ctrl Pts',(1.4925681575455,0.248556174862625,-13.8111913236187));
#361300=CARTESIAN_POINT('Ctrl Pts',(1.44651041138113,0.444035568848532,
-13.8003313572862));
#361301=CARTESIAN_POINT('Ctrl Pts',(1.28451834308037,0.797560797550709,
-13.7806910668027));
#361302=CARTESIAN_POINT('Ctrl Pts',(1.17329856752123,0.953663525102152,
-13.7716263668414));
#361303=CARTESIAN_POINT('Ctrl Pts',(0.894089756253627,1.22025961834643,
-13.7507874796114));
#361304=CARTESIAN_POINT('Ctrl Pts',(0.727136316356959,1.32653649589924,
-13.7398027930016));
#361305=CARTESIAN_POINT('Ctrl Pts',(0.359161671993576,1.46988350906151,
-13.7181167431934));
#361306=CARTESIAN_POINT('Ctrl Pts',(0.161383474980832,1.50448162004382,
-13.7078890555059));
#361307=CARTESIAN_POINT('Ctrl Pts',(-0.228318046516828,1.49478151140755,
-13.6888700848487));
#361308=CARTESIAN_POINT('Ctrl Pts',(-0.416623010527941,1.45358281099932,
-13.6786658496989));
#361309=CARTESIAN_POINT('Ctrl Pts',(-0.774430407259481,1.29985998622534,
-13.6571807548312));
#361310=CARTESIAN_POINT('Ctrl Pts',(-0.939420778107782,1.18611726233594,
-13.6460831318046));
#361311=CARTESIAN_POINT('Ctrl Pts',(-1.21234841839429,0.904315851918118,
-13.6251240776328));
#361312=CARTESIAN_POINT('Ctrl Pts',(-1.31892166504881,0.740281487577644,
-13.6161267493098));
#361313=CARTESIAN_POINT('Ctrl Pts',(-1.46355819493749,0.381238092972433,
-13.596179894054));
#361314=CARTESIAN_POINT('Ctrl Pts',(-1.50044394700116,0.189730464566316,
-13.5855405813648));
#361315=CARTESIAN_POINT('Ctrl Pts',(-1.49953010905219,-0.204397744186537,
-13.5636445697674));
#361316=CARTESIAN_POINT('Ctrl Pts',(-1.45870003340395,-0.403213907571023,
-13.5525992273571));
#361317=CARTESIAN_POINT('Ctrl Pts',(-1.30531953657094,-0.763109642954445,
-13.5326050198358));
#361318=CARTESIAN_POINT('Ctrl Pts',(-1.19812778701953,-0.922330037194102,
-13.5236913378856));
#361319=CARTESIAN_POINT('Ctrl Pts',(-0.926195786334519,-1.19598932968987,
-13.5030063563888));
#361320=CARTESIAN_POINT('Ctrl Pts',(-0.762587572873664,-1.30640090443331,
-13.4920677643612));
#361321=CARTESIAN_POINT('Ctrl Pts',(-0.399276435807626,-1.45947733686857,
-13.4703358260059));
#361322=CARTESIAN_POINT('Ctrl Pts',(-0.202579407806616,-1.49949470960994,
-13.4597606421466));
#361323=CARTESIAN_POINT('Ctrl Pts',(-0.00251767479581147,-1.499998415418,
-13.4501211757012));
#361324=CARTESIAN_POINT('Ctrl Pts',(-0.0012587977324238,-1.50000000001036,
-13.4500605639338));
#361325=CARTESIAN_POINT('Ctrl Pts',(1.23475997724286E-8,-1.5,-13.4499999994059));
#361326=CARTESIAN_POINT('Ctrl Pts',(6.20337115009306E-14,-1.5,-13.3875));
#361327=CARTESIAN_POINT('Ctrl Pts',(-0.178100903696597,-1.5,-13.3960688837243));
#361328=CARTESIAN_POINT('Ctrl Pts',(-0.354967221346645,-1.46828470868815,
-13.4054593487141));
#361329=CARTESIAN_POINT('Ctrl Pts',(-0.70633803961609,-1.33777107321515,
-13.4259900638533));
#361330=CARTESIAN_POINT('Ctrl Pts',(-0.875184458485685,-1.23393656197652,
-13.4369979829477));
#361331=CARTESIAN_POINT('Ctrl Pts',(-1.15859240296114,-0.97146419681889,
-13.457924353066));
#361332=CARTESIAN_POINT('Ctrl Pts',(-1.27214519917268,-0.817134168424963,
-13.4671036573098));
#361333=CARTESIAN_POINT('Ctrl Pts',(-1.4395118380733,-0.466219582375254,
-13.4865989120903));
#361334=CARTESIAN_POINT('Ctrl Pts',(-1.48856622007895,-0.271485424393246,
-13.4974174764227));
#361335=CARTESIAN_POINT('Ctrl Pts',(-1.50765853111819,0.120953412385961,
-13.5192196340215));
#361336=CARTESIAN_POINT('Ctrl Pts',(-1.47938132936033,0.314812388806881,
-13.529989577156));
#361337=CARTESIAN_POINT('Ctrl Pts',(-1.35121242124249,0.679040400354931,
-13.5502244666864));
#361338=CARTESIAN_POINT('Ctrl Pts',(-1.25330353095733,0.846227866481236,
-13.55904006871));
#361339=CARTESIAN_POINT('Ctrl Pts',(-0.994844835122127,1.14019695876635,
-13.5796409766303));
#361340=CARTESIAN_POINT('Ctrl Pts',(-0.834633214314774,1.26219703017889,
-13.5907380527029));
#361341=CARTESIAN_POINT('Ctrl Pts',(-0.482711808255667,1.433106098456,-13.6124173533652));
#361342=CARTESIAN_POINT('Ctrl Pts',(-0.295632313906198,1.48304608128885,
-13.6228054414791));
#361343=CARTESIAN_POINT('Ctrl Pts',(0.0932458580179198,1.51012548968155,
-13.6422675570379));
#361344=CARTESIAN_POINT('Ctrl Pts',(0.291481610423482,1.48466644261322,
-13.6519498476698));
#361345=CARTESIAN_POINT('Ctrl Pts',(0.665692555798307,1.35853927436543,
-13.673457612625));
#361346=CARTESIAN_POINT('Ctrl Pts',(0.838095336951256,1.25951242582141,
-13.6845030910935));
#361347=CARTESIAN_POINT('Ctrl Pts',(1.12957335331216,1.00506872077059,-13.7055947143901));
#361348=CARTESIAN_POINT('Ctrl Pts',(1.24763399480712,0.854095972651749,
-13.7150502237416));
#361349=CARTESIAN_POINT('Ctrl Pts',(1.42521375094207,0.508242002316863,
-13.7342643332047));
#361350=CARTESIAN_POINT('Ctrl Pts',(1.47995176671291,0.31506087755952,-13.7449966179134));
#361351=CARTESIAN_POINT('Ctrl Pts',(1.51060379458671,-0.077164127040108,
-13.7667868959467));
#361352=CARTESIAN_POINT('Ctrl Pts',(1.48786123370151,-0.272317462827342,
-13.7776287479349));
#361353=CARTESIAN_POINT('Ctrl Pts',(1.37014123212598,-0.639731899664652,
-13.7980406610925));
#361354=CARTESIAN_POINT('Ctrl Pts',(1.27756797068767,-0.808926535266669,
-13.8068364972199));
#361355=CARTESIAN_POINT('Ctrl Pts',(1.02820533535891,-1.11031494337791,
-13.8272058628313));
#361356=CARTESIAN_POINT('Ctrl Pts',(0.87116979906505,-1.23735790462876,
-13.8382902097397));
#361357=CARTESIAN_POINT('Ctrl Pts',(0.523318710027666,-1.41885361090174,
-13.8600677504607));
#361358=CARTESIAN_POINT('Ctrl Pts',(0.337204794027228,-1.47421825389061,
-13.8705600671689));
#361359=CARTESIAN_POINT('Ctrl Pts',(0.0971864689633863,-1.49764146682935,
-13.8827585990216));
#361360=CARTESIAN_POINT('Ctrl Pts',(0.0485661678850943,-1.5,-13.8851633591582));
#361361=CARTESIAN_POINT('Ctrl Pts',(2.47118481715386E-13,-1.5,-13.8875));
#361362=CARTESIAN_POINT('Origin',(0.,1.30104260698261E-15,-17.7));
#361363=CARTESIAN_POINT('',(1.15223986389915E-13,-1.5,-14.45));
#361364=CARTESIAN_POINT('',(2.04248178747325E-14,-1.5,-14.3875));
#361365=CARTESIAN_POINT('',(-1.83697019872103E-16,-1.5,-17.7));
#361366=CARTESIAN_POINT('Ctrl Pts',(2.30631669799703E-13,-1.5,-14.45));
#361367=CARTESIAN_POINT('Ctrl Pts',(0.0548934545880663,-1.5,-14.4473589374347));
#361368=CARTESIAN_POINT('Ctrl Pts',(0.109846375959735,-1.49698693850033,
-14.4446313176197));
#361369=CARTESIAN_POINT('Ctrl Pts',(0.356114797475588,-1.46979646143151,
-14.4320274316354));
#361370=CARTESIAN_POINT('Ctrl Pts',(0.541735609813599,-1.41195761642243,
-14.4214901115543));
#361371=CARTESIAN_POINT('Ctrl Pts',(0.887622898574594,-1.22565352496498,
-14.3996734879631));
#361372=CARTESIAN_POINT('Ctrl Pts',(1.04315567077518,-1.09633139380361,
-14.3885981325504));
#361373=CARTESIAN_POINT('Ctrl Pts',(1.28833566498435,-0.791587430127308,
-14.3683367944769));
#361374=CARTESIAN_POINT('Ctrl Pts',(1.3784815054932,-0.621459006709495,
-14.3595255003727));
#361375=CARTESIAN_POINT('Ctrl Pts',(1.4913685586622,-0.252598796378145,
-14.3390332664654));
#361376=CARTESIAN_POINT('Ctrl Pts',(1.51153567546017,-0.0568996909763287,
-14.3281610939431));
#361377=CARTESIAN_POINT('Ctrl Pts',(1.47553879372479,0.335110661665423,
-14.3063827410185));
#361378=CARTESIAN_POINT('Ctrl Pts',(1.41819075254881,0.527516332674454,
-14.2956935370736));
#361379=CARTESIAN_POINT('Ctrl Pts',(1.23590781493958,0.870996745486203,
-14.2766112919174));
#361380=CARTESIAN_POINT('Ctrl Pts',(1.11573602959479,1.02042728393899,-14.2670023390876));
#361381=CARTESIAN_POINT('Ctrl Pts',(0.820502075920879,1.27108579679313,
-14.2458351524004));
#361382=CARTESIAN_POINT('Ctrl Pts',(0.646482477624955,1.36782476586137,
-14.2347754369885));
#361383=CARTESIAN_POINT('Ctrl Pts',(0.271051159733503,1.48841962626682,
-14.2133626320511));
#361384=CARTESIAN_POINT('Ctrl Pts',(0.0733547619086724,1.51111323541884,
-14.2038379836117));
#361385=CARTESIAN_POINT('Ctrl Pts',(-0.314557462546743,1.47917868967553,
-14.1842874772956));
#361386=CARTESIAN_POINT('Ctrl Pts',(-0.501217439520081,1.42677172190501,
-14.1738510458615));
#361387=CARTESIAN_POINT('Ctrl Pts',(-0.851327691872639,1.25104062313835,
-14.1521249390812));
#361388=CARTESIAN_POINT('Ctrl Pts',(-1.01011504827038,1.12673940669524,
-14.1410324672666));
#361389=CARTESIAN_POINT('Ctrl Pts',(-1.26444900369502,0.829385260622806,
-14.12053598174));
#361390=CARTESIAN_POINT('Ctrl Pts',(-1.35992886792741,0.661290561105772,
-14.1117383645058));
#361391=CARTESIAN_POINT('Ctrl Pts',(-1.48336975502415,0.295610939923114,
-14.0914228299957));
#361392=CARTESIAN_POINT('Ctrl Pts',(-1.50914875596412,0.101147022240177,
-14.0806192790133));
#361393=CARTESIAN_POINT('Ctrl Pts',(-1.48482616482199,-0.291237481210953,
-14.0588201399327));
#361394=CARTESIAN_POINT('Ctrl Pts',(-1.43319362671366,-0.485289998468957,
-14.0480394445295));
#361395=CARTESIAN_POINT('Ctrl Pts',(-1.26119818391366,-0.833927043460052,
-14.0286707198077));
#361396=CARTESIAN_POINT('Ctrl Pts',(-1.14561487565883,-0.986733837248934,
-14.0193758148138));
#361397=CARTESIAN_POINT('Ctrl Pts',(-0.858564070758227,-1.24559925824427,
-13.998374370385));
#361398=CARTESIAN_POINT('Ctrl Pts',(-0.68809869252659,-1.34728197701362,
-13.9873483310851));
#361399=CARTESIAN_POINT('Ctrl Pts',(-0.341228236903536,-1.47071578820734,
-13.9672308015301));
#361400=CARTESIAN_POINT('Ctrl Pts',(-0.171142290594654,-1.5,-13.9582340872954));
#361401=CARTESIAN_POINT('Ctrl Pts',(1.24067423001861E-13,-1.5,-13.95));
#361402=CARTESIAN_POINT('Ctrl Pts',(2.47118481715386E-13,-1.5,-13.8875));
#361403=CARTESIAN_POINT('Ctrl Pts',(-0.146901164955814,-1.5,-13.8945677855943));
#361404=CARTESIAN_POINT('Ctrl Pts',(-0.29324926487615,-1.47842590781795,
-13.9022082421731));
#361405=CARTESIAN_POINT('Ctrl Pts',(-0.623428532768038,-1.37853225627447,
-13.9208688232603));
#361406=CARTESIAN_POINT('Ctrl Pts',(-0.799335806249486,-1.28455193913573,
-13.9319427302667));
#361407=CARTESIAN_POINT('Ctrl Pts',(-1.09903141191604,-1.03843192947599,
-13.9531985087522));
#361408=CARTESIAN_POINT('Ctrl Pts',(-1.22172374531855,-0.890818384453344,
-13.9630100897527));
#361409=CARTESIAN_POINT('Ctrl Pts',(-1.40955390799974,-0.550171809059182,
-13.9819348994968));
#361410=CARTESIAN_POINT('Ctrl Pts',(-1.46997231997795,-0.358729462154206,
-13.9925705854359));
#361411=CARTESIAN_POINT('Ctrl Pts',(-1.51228676565712,0.032932669464555,
-14.0143295927481));
#361412=CARTESIAN_POINT('Ctrl Pts',(-1.49517726595293,0.229233814621506,
-14.0252352119235));
#361413=CARTESIAN_POINT('Ctrl Pts',(-1.38800785053078,0.599780881822918,
-14.0458211601013));
#361414=CARTESIAN_POINT('Ctrl Pts',(-1.30070197071466,0.771020319677233,
-14.0546705116916));
#361415=CARTESIAN_POINT('Ctrl Pts',(-1.06044914873033,1.07967342382362,
-14.0748033783162));
#361416=CARTESIAN_POINT('Ctrl Pts',(-0.906719571382535,1.21164763042927,
-14.0858656462383));
#361417=CARTESIAN_POINT('Ctrl Pts',(-0.563218003842742,1.40356600641679,
-14.1077234391118));
#361418=CARTESIAN_POINT('Ctrl Pts',(-0.378216913316017,1.46430207383723,
-14.1183114212137));
#361419=CARTESIAN_POINT('Ctrl Pts',(0.00632781424123031,1.51255890297912,
-14.1381533055208));
#361420=CARTESIAN_POINT('Ctrl Pts',(0.202281576293156,1.49898759168369,
-14.1472603993304));
#361421=CARTESIAN_POINT('Ctrl Pts',(0.581508724714796,1.39681711699902,
-14.1683440427571));
#361422=CARTESIAN_POINT('Ctrl Pts',(0.760705115394362,1.30788860290628,
-14.179435869626));
#361423=CARTESIAN_POINT('Ctrl Pts',(1.06829485686206,1.07009670557278,-14.2008401184439));
#361424=CARTESIAN_POINT('Ctrl Pts',(1.19556689497506,0.925745529551606,
-14.2109732521221));
#361425=CARTESIAN_POINT('Ctrl Pts',(1.39325787996739,0.590186443266003,
-14.2298057498024));
#361426=CARTESIAN_POINT('Ctrl Pts',(1.45914179626626,0.400560887356709,
-14.2402466173691));
#361427=CARTESIAN_POINT('Ctrl Pts',(1.51268440697242,0.00963277955025047,
-14.2619648455806));
#361428=CARTESIAN_POINT('Ctrl Pts',(1.5010363637033,-0.187621421187203,
-14.2729234122882));
#361429=CARTESIAN_POINT('Ctrl Pts',(1.40403520475586,-0.561104485393219,
-14.2936724714108));
#361430=CARTESIAN_POINT('Ctrl Pts',(1.32169950767049,-0.734339156382434,
-14.3026413460211));
#361431=CARTESIAN_POINT('Ctrl Pts',(1.09150246145397,-1.04794409308597,
-14.3224279548129));
#361432=CARTESIAN_POINT('Ctrl Pts',(0.943090741730096,-1.18326898371886,
-14.3333274417471));
#361433=CARTESIAN_POINT('Ctrl Pts',(0.606792062293365,-1.38536725397004,
-14.3551214603459));
#361434=CARTESIAN_POINT('Ctrl Pts',(0.423199204933112,-1.45201782338356,
-14.36580598052));
#361435=CARTESIAN_POINT('Ctrl Pts',(0.155076678190878,-1.49399241577041,
-14.3798719925021));
#361436=CARTESIAN_POINT('Ctrl Pts',(0.0775142586163279,-1.5,-14.3837705934935));
#361437=CARTESIAN_POINT('Ctrl Pts',(4.1033332769337E-14,-1.5,-14.3875));
#361438=CARTESIAN_POINT('Origin',(0.,1.30104260698261E-15,-17.7));
#361439=CARTESIAN_POINT('',(3.9380059590488E-15,-1.5,-14.95));
#361440=CARTESIAN_POINT('',(-4.305399998793E-15,-1.5,-14.8875));
#361441=CARTESIAN_POINT('',(-1.83697019872103E-16,-1.5,-17.7));
#361442=CARTESIAN_POINT('Ctrl Pts',(8.0597089379697E-15,-1.5,-14.95));
#361443=CARTESIAN_POINT('Ctrl Pts',(0.0833426479163508,-1.5,-14.9459901749825));
#361444=CARTESIAN_POINT('Ctrl Pts',(0.166719807561326,-1.49305513625313,
-14.9417857766368));
#361445=CARTESIAN_POINT('Ctrl Pts',(0.440334138154219,-1.44694357835383,
-14.92734062441));
#361446=CARTESIAN_POINT('Ctrl Pts',(0.623337762253202,-1.37803356404355,
-14.9166216913762));
#361447=CARTESIAN_POINT('Ctrl Pts',(0.957346261788502,-1.17176336052225,
-14.8948219720741));
#361448=CARTESIAN_POINT('Ctrl Pts',(1.10410200439716,-1.03465926441528,
-14.8839527360016));
#361449=CARTESIAN_POINT('Ctrl Pts',(1.33041854393489,-0.718392039016014,
-14.8642788757107));
#361450=CARTESIAN_POINT('Ctrl Pts',(1.41062716737482,-0.544282817543551,
-14.8552379343079));
#361451=CARTESIAN_POINT('Ctrl Pts',(1.50321498327612,-0.169551281775696,
-14.8344195156541));
#361452=CARTESIAN_POINT('Ctrl Pts',(1.51248503780511,0.0280695077048375,
-14.8234405829052));
#361453=CARTESIAN_POINT('Ctrl Pts',(1.45408384547968,0.418559633800821,
-14.801746687011));
#361454=CARTESIAN_POINT('Ctrl Pts',(1.38585349562832,0.607383413780491,
-14.7914718125692));
#361455=CARTESIAN_POINT('Ctrl Pts',(1.18387280610371,0.940701591758596,
-14.7724951738364));
#361456=CARTESIAN_POINT('Ctrl Pts',(1.0546254503485,1.0836125085627,-14.7623070098443));
#361457=CARTESIAN_POINT('Ctrl Pts',(0.743605532358566,1.31772476639197,
-14.74083993879));
#361458=CARTESIAN_POINT('Ctrl Pts',(0.563015447126632,1.40441023945795,
-14.7297433644558));
#361459=CARTESIAN_POINT('Ctrl Pts',(0.18279417496058,1.50140926982081,-14.7087555424593));
#361460=CARTESIAN_POINT('Ctrl Pts',(-0.0126886225498201,1.51244081182594,
-14.6997350964691));
#361461=CARTESIAN_POINT('Ctrl Pts',(-0.39624513432888,1.45955748315514,
-14.6798122438401));
#361462=CARTESIAN_POINT('Ctrl Pts',(-0.580705695498423,1.39645389961965,
-14.6691845036325));
#361463=CARTESIAN_POINT('Ctrl Pts',(-0.9221882556015,1.19996076135229,-14.6472967735696));
#361464=CARTESIAN_POINT('Ctrl Pts',(-1.07440923072296,1.0658328764283,-14.6362472639081));
#361465=CARTESIAN_POINT('Ctrl Pts',(-1.31061083652864,0.753999860652955,
-14.6162209806342));
#361466=CARTESIAN_POINT('Ctrl Pts',(-1.39559625713445,0.581837152560039,
-14.6073242862533));
#361467=CARTESIAN_POINT('Ctrl Pts',(-1.49804375618007,0.209916424324193,
-14.5866620235735));
#361468=CARTESIAN_POINT('Ctrl Pts',(-1.51262046441537,0.0131539254397011,
-14.5757307736355));
#361469=CARTESIAN_POINT('Ctrl Pts',(-1.46509565708434,-0.378143856838375,
-14.5539920079534));
#361470=CARTESIAN_POINT('Ctrl Pts',(-1.40215696456351,-0.568753598411832,
-14.5434025778659));
#361471=CARTESIAN_POINT('Ctrl Pts',(-1.20975930776716,-0.907039313885584,
-14.5246089270063));
#361472=CARTESIAN_POINT('Ctrl Pts',(-1.08496567168402,-1.05315762768056,
-14.5146127233373));
#361473=CARTESIAN_POINT('Ctrl Pts',(-0.781571052774216,-1.29547893043548,
-14.4932844956303));
#361474=CARTESIAN_POINT('Ctrl Pts',(-0.604126639955704,-1.38713882161312,
-14.4822010892498));
#361475=CARTESIAN_POINT('Ctrl Pts',(-0.27913311540433,-1.48046544168253,
-14.4639724248964));
#361476=CARTESIAN_POINT('Ctrl Pts',(-0.139785614626517,-1.5,-14.4567254385195));
#361477=CARTESIAN_POINT('Ctrl Pts',(2.31446806164826E-13,-1.5,-14.45));
#361478=CARTESIAN_POINT('Ctrl Pts',(4.10782519111308E-14,-1.5,-14.3875));
#361479=CARTESIAN_POINT('Ctrl Pts',(-0.114802638392122,-1.5,-14.393023444515));
#361480=CARTESIAN_POINT('Ctrl Pts',(-0.229464033139329,-1.48682369573369,
-14.3989061018938));
#361481=CARTESIAN_POINT('Ctrl Pts',(-0.535294746130471,-1.41526322525725,
-14.4156081797797));
#361482=CARTESIAN_POINT('Ctrl Pts',(-0.717909801300955,-1.33195624756892,
-14.4267083334316));
#361483=CARTESIAN_POINT('Ctrl Pts',(-1.03395736808419,-1.10341176165394,
-14.4482626370203));
#361484=CARTESIAN_POINT('Ctrl Pts',(-1.16611604840162,-0.962694650490352,
-14.4585299331351));
#361485=CARTESIAN_POINT('Ctrl Pts',(-1.37511325312879,-0.631742654647489,
-14.4777784268315));
#361486=CARTESIAN_POINT('Ctrl Pts',(-1.44704926475347,-0.442854836839777,
-14.487896953509));
#361487=CARTESIAN_POINT('Ctrl Pts',(-1.51189910921728,-0.0517560135145772,
-14.5096246659159));
#361488=CARTESIAN_POINT('Ctrl Pts',(-1.50569525189539,0.146294635185502,
-14.5206274797326));
#361489=CARTESIAN_POINT('Ctrl Pts',(-1.41878873104838,0.522609896388955,
-14.5415338831328));
#361490=CARTESIAN_POINT('Ctrl Pts',(-1.34129312954439,0.697853135661597,
-14.5506851468736));
#361491=CARTESIAN_POINT('Ctrl Pts',(-1.11994179463028,1.01749033453342,
-14.5702137290199));
#361492=CARTESIAN_POINT('Ctrl Pts',(-0.975330636366259,1.1568341836933,
-14.5810419990925));
#361493=CARTESIAN_POINT('Ctrl Pts',(-0.644319867728664,1.36838967916601,
-14.6028443036649));
#361494=CARTESIAN_POINT('Ctrl Pts',(-0.462107846438292,1.44017602864903,
-14.6136050488901));
#361495=CARTESIAN_POINT('Ctrl Pts',(-0.0823016076968858,1.51001412847041,
-14.6338184322888));
#361496=CARTESIAN_POINT('Ctrl Pts',(0.11155694551423,1.5081352756803,-14.6426413061636));
#361497=CARTESIAN_POINT('Ctrl Pts',(0.495135269222907,1.42988726169609,
-14.6632697828117));
#361498=CARTESIAN_POINT('Ctrl Pts',(0.680550509755873,1.35150894848779,
-14.674367753098));
#361499=CARTESIAN_POINT('Ctrl Pts',(1.00364455605091,1.13113958357526,-14.6960339938958));
#361500=CARTESIAN_POINT('Ctrl Pts',(1.13991781438308,0.993673545026912,
-14.706408945165));
#361501=CARTESIAN_POINT('Ctrl Pts',(1.35681439160581,0.669566740973199,
-14.7258473533814));
#361502=CARTESIAN_POINT('Ctrl Pts',(1.43331430411777,0.484663366150857,
-14.7355742574361));
#361503=CARTESIAN_POINT('Ctrl Pts',(1.5097428860136,0.0970721898109013,
-14.7571071005661));
#361504=CARTESIAN_POINT('Ctrl Pts',(1.50944017341581,-0.101671470041182,
-14.7681484150024));
#361505=CARTESIAN_POINT('Ctrl Pts',(1.43344868231728,-0.480953874011405,
-14.7892196596674));
#361506=CARTESIAN_POINT('Ctrl Pts',(1.36109153695783,-0.658403087718725,
-14.7986367608878));
#361507=CARTESIAN_POINT('Ctrl Pts',(1.14918218367097,-0.98434035303761,
-14.8178860673269));
#361508=CARTESIAN_POINT('Ctrl Pts',(1.0087251700937,-1.12782793490334,-14.8286295747064));
#361509=CARTESIAN_POINT('Ctrl Pts',(0.683617804911299,-1.34926578512871,
-14.8504223615019));
#361510=CARTESIAN_POINT('Ctrl Pts',(0.503025762151212,-1.4264734675165,
-14.8612557580544));
#361511=CARTESIAN_POINT('Ctrl Pts',(0.209684998456008,-1.4890033745908,
-14.8771060639912));
#361512=CARTESIAN_POINT('Ctrl Pts',(0.104876703558311,-1.5,-14.8824541172474));
#361513=CARTESIAN_POINT('Ctrl Pts',(-7.91033905045424E-15,-1.5,-14.8875));
#361514=CARTESIAN_POINT('Origin',(0.,1.30104260698261E-15,-17.7));
#361515=CARTESIAN_POINT('',(-1.25488059566348E-14,-1.5,-15.45));
#361516=CARTESIAN_POINT('',(-9.08611625561304E-14,-1.5,-15.3875));
#361517=CARTESIAN_POINT('',(-1.83697019872103E-16,-1.5,-17.7));
#361518=CARTESIAN_POINT('Ctrl Pts',(-2.42514341941558E-14,-1.5,-15.45));
#361519=CARTESIAN_POINT('Ctrl Pts',(0.111323301433604,-1.5,-15.4446439551625));
#361520=CARTESIAN_POINT('Ctrl Pts',(0.222528418840014,-1.487610191846,-15.438949435119));
#361521=CARTESIAN_POINT('Ctrl Pts',(0.521588263685572,-1.41982534379392,
-15.4226779991793));
#361522=CARTESIAN_POINT('Ctrl Pts',(0.701387188966607,-1.34015125019033,
-15.4118142500866));
#361523=CARTESIAN_POINT('Ctrl Pts',(1.02369796438871,-1.11425235425986,
-15.3900320963425));
#361524=CARTESIAN_POINT('Ctrl Pts',(1.16221616046766,-0.968913692312363,
-15.3793304514723));
#361525=CARTESIAN_POINT('Ctrl Pts',(1.36979060342105,-0.640129619772863,
-15.3602106305254));
#361526=CARTESIAN_POINT('Ctrl Pts',(1.4397950022009,-0.461644714260468,
-15.3506469285699));
#361527=CARTESIAN_POINT('Ctrl Pts',(1.51072425414865,-0.0810206637609527,
-15.3295011479866));
#361528=CARTESIAN_POINT('Ctrl Pts',(1.50828800418927,0.117985125174841,
-15.3184452708235));
#361529=CARTESIAN_POINT('Ctrl Pts',(1.4265462362482,0.503905578853235,-15.2970052456192));
#361530=CARTESIAN_POINT('Ctrl Pts',(1.34795543831095,0.686987858184746,
-15.2874372068696));
#361531=CARTESIAN_POINT('Ctrl Pts',(1.12740342360153,1.00789447542627,-15.2679118204132));
#361532=CARTESIAN_POINT('Ctrl Pts',(0.989235785780901,1.14380179508466,
-15.2574890235153));
#361533=CARTESIAN_POINT('Ctrl Pts',(0.662921772954764,1.36028138369372,
-15.2357759113474));
#361534=CARTESIAN_POINT('Ctrl Pts',(0.476242679886323,1.43632722737674,
-15.2246819247477));
#361535=CARTESIAN_POINT('Ctrl Pts',(0.0918050218253722,1.50941276067965,
-15.2041555055975));
#361536=CARTESIAN_POINT('Ctrl Pts',(-0.101630965929904,1.50878309871131,
-15.195354252836));
#361537=CARTESIAN_POINT('Ctrl Pts',(-0.480357226858617,1.43422493859728,
-15.1750617171081));
#361538=CARTESIAN_POINT('Ctrl Pts',(-0.661868306335575,1.36002328041678,
-15.1642676040534));
#361539=CARTESIAN_POINT('Ctrl Pts',(-0.990290105863839,1.14405209277072,
-15.1424672031994));
#361540=CARTESIAN_POINT('Ctrl Pts',(-1.13306867305426,1.0028494976295,-15.1316754718731));
#361541=CARTESIAN_POINT('Ctrl Pts',(-1.35022747427309,0.680397702134618,
-15.1122704198588));
#361542=CARTESIAN_POINT('Ctrl Pts',(-1.42543857932541,0.504183174466805,
-15.1030101763592));
#361543=CARTESIAN_POINT('Ctrl Pts',(-1.5075168947896,0.126543024855669,
-15.0820301680475));
#361544=CARTESIAN_POINT('Ctrl Pts',(-1.51111163732494,-0.0718357148492454,
-15.0710091269527));
#361545=CARTESIAN_POINT('Ctrl Pts',(-1.44111936884653,-0.461399458746197,
-15.0493666967362));
#361546=CARTESIAN_POINT('Ctrl Pts',(-1.3671547321,-0.648515270510511,-15.0394296163137));
#361547=CARTESIAN_POINT('Ctrl Pts',(-1.15466029410091,-0.976448604471469,
-15.020096713622));
#361548=CARTESIAN_POINT('Ctrl Pts',(-1.02067685168224,-1.11574616139637,
-15.0097810556618));
#361549=CARTESIAN_POINT('Ctrl Pts',(-0.701495530341301,-1.34071034466502,
-14.9881754320879));
#361550=CARTESIAN_POINT('Ctrl Pts',(-0.517629508292398,-1.42185426682779,
-14.9770751761397));
#361551=CARTESIAN_POINT('Ctrl Pts',(-0.216870396831998,-1.4882347989933,
-14.9607609929715));
#361552=CARTESIAN_POINT('Ctrl Pts',(-0.108480333794644,-1.5,-14.9552192624932));
#361553=CARTESIAN_POINT('Ctrl Pts',(8.01442245901285E-15,-1.5,-14.95));
#361554=CARTESIAN_POINT('Ctrl Pts',(-8.4271029777139E-15,-1.5,-14.8875));
#361555=CARTESIAN_POINT('Ctrl Pts',(-0.0855201633304099,-1.5,-14.8916145907767));
#361556=CARTESIAN_POINT('Ctrl Pts',(-0.171066049806968,-1.4926875449768,
-14.8959335429095));
#361557=CARTESIAN_POINT('Ctrl Pts',(-0.4527262879348,-1.44395797271794,
-14.9108385266642));
#361558=CARTESIAN_POINT('Ctrl Pts',(-0.640931643232649,-1.37082770443278,
-14.9219249573841));
#361559=CARTESIAN_POINT('Ctrl Pts',(-0.971170408162794,-1.15922855412728,
-14.943691331545));
#361560=CARTESIAN_POINT('Ctrl Pts',(-1.11165987404137,-1.02528720584264,
-14.9541712271315));
#361561=CARTESIAN_POINT('Ctrl Pts',(-1.3367117285935,-0.708348419626942,
-14.9738028947048));
#361562=CARTESIAN_POINT('Ctrl Pts',(-1.41786008418202,-0.527486975061614,
-14.9831951680522));
#361563=CARTESIAN_POINT('Ctrl Pts',(-1.50610295132645,-0.143662247154666,
-15.0045187640471));
#361564=CARTESIAN_POINT('Ctrl Pts',(-1.51191577587105,0.0556152855864015,
-15.0155897380882));
#361565=CARTESIAN_POINT('Ctrl Pts',(-1.44722790883372,0.437862624097292,
-15.0368257013388));
#361566=CARTESIAN_POINT('Ctrl Pts',(-1.38010005197985,0.61763562974742,
-15.0465897838943));
#361567=CARTESIAN_POINT('Ctrl Pts',(-1.17783126149847,0.949866536949361,
-15.0655500819249));
#361568=CARTESIAN_POINT('Ctrl Pts',(-1.04171156367606,1.09742626632624,
-15.0761980253114));
#361569=CARTESIAN_POINT('Ctrl Pts',(-0.722895001951393,1.32871820587405,
-15.0979618703878));
#361570=CARTESIAN_POINT('Ctrl Pts',(-0.544108190648435,1.41139051879915,
-15.108860207994));
#361571=CARTESIAN_POINT('Ctrl Pts',(-0.16930443437504,1.50255234182842,
-15.1294252349874));
#361572=CARTESIAN_POINT('Ctrl Pts',(0.0227470043379086,1.51188809314083,
-15.1382641909471));
#361573=CARTESIAN_POINT('Ctrl Pts',(0.409971699885314,1.45675699794972,
-15.1584259671089));
#361574=CARTESIAN_POINT('Ctrl Pts',(0.600820985146348,1.38896201249828,
-15.1694914016676));
#361575=CARTESIAN_POINT('Ctrl Pts',(0.93796296179849,1.18634431453642,-15.19134042197));
#361576=CARTESIAN_POINT('Ctrl Pts',(1.08257277860081,1.05604938901551,-15.2019172685116));
#361577=CARTESIAN_POINT('Ctrl Pts',(1.31567390201647,0.746287006525185,
-15.2217368621657));
#361578=CARTESIAN_POINT('Ctrl Pts',(1.40135803625885,0.569337778598538,
-15.2308701234113));
#361579=CARTESIAN_POINT('Ctrl Pts',(1.50112075384638,0.189363321238377,
-15.2519798154869));
#361580=CARTESIAN_POINT('Ctrl Pts',(1.51298098203424,-0.0102601896058358,
-15.2630700105338));
#361581=CARTESIAN_POINT('Ctrl Pts',(1.45950018878855,-0.395215606541005,
-15.2844564225857));
#361582=CARTESIAN_POINT('Ctrl Pts',(1.39751363149503,-0.577335386345449,
-15.2945741881304));
#361583=CARTESIAN_POINT('Ctrl Pts',(1.20464107988243,-0.915599695925714,
-15.3133666497738));
#361584=CARTESIAN_POINT('Ctrl Pts',(1.07285325728569,-1.06701811961393,
-15.3238550491371));
#361585=CARTESIAN_POINT('Ctrl Pts',(0.760308243858021,-1.30775115601977,
-15.3455794068958));
#361586=CARTESIAN_POINT('Ctrl Pts',(0.583422679771014,-1.39567368120654,
-15.3565321099322));
#361587=CARTESIAN_POINT('Ctrl Pts',(0.265773861282844,-1.4822979631247,
-15.3742212258907));
#361588=CARTESIAN_POINT('Ctrl Pts',(0.133067928039146,-1.50000000000002,
-15.3810977663272));
#361589=CARTESIAN_POINT('Ctrl Pts',(-1.81243908770057E-13,-1.5,-15.3875));
#361590=CARTESIAN_POINT('Origin',(0.,1.30104260698261E-15,-17.7));
#361591=CARTESIAN_POINT('',(-9.91045685139722E-14,-1.5,-15.95));
#361592=CARTESIAN_POINT('',(-5.78875387247641E-14,-1.5,-15.8875));
#361593=CARTESIAN_POINT('',(-1.83697019872103E-16,-1.5,-17.7));
#361594=CARTESIAN_POINT('Ctrl Pts',(-1.9824419883463E-13,-1.5,-15.95));
#361595=CARTESIAN_POINT('Ctrl Pts',(0.139005423550127,-1.50000000000002,
-15.9433120984412));
#361596=CARTESIAN_POINT('Ctrl Pts',(0.277560387205389,-1.48068294817197,
-15.9361092848711));
#361597=CARTESIAN_POINT('Ctrl Pts',(0.600085978486933,-1.38862312983871,
-15.9180345479496));
#361598=CARTESIAN_POINT('Ctrl Pts',(0.776112872049263,-1.29846904643623,
-15.9070611699898));
#361599=CARTESIAN_POINT('Ctrl Pts',(1.08587924465258,-1.0537627108278,-15.8853601302278));
#361600=CARTESIAN_POINT('Ctrl Pts',(1.2158160773737,-0.900716948777619,
-15.8750398304875));
#361601=CARTESIAN_POINT('Ctrl Pts',(1.40463721490438,-0.559860276301527,
-15.8561033486833));
#361602=CARTESIAN_POINT('Ctrl Pts',(1.46440645046521,-0.376748429685064,
-15.8459304683157));
#361603=CARTESIAN_POINT('Ctrl Pts',(1.51302063951444,0.00934783112624828,
-15.8244806760484));
#361604=CARTESIAN_POINT('Ctrl Pts',(1.49853823464877,0.209065615577763,
-15.8133852435789));
#361605=CARTESIAN_POINT('Ctrl Pts',(1.39382524437842,0.587332821171853,
-15.7923703988237));
#361606=CARTESIAN_POINT('Ctrl Pts',(1.30618806903924,0.762611041822026,
-15.7833270293886));
#361607=CARTESIAN_POINT('Ctrl Pts',(1.06959752065909,1.06923064121564,-15.7634268502281));
#361608=CARTESIAN_POINT('Ctrl Pts',(0.923216581814794,1.19789325795466,
-15.7528101324482));
#361609=CARTESIAN_POINT('Ctrl Pts',(0.583132675200652,1.39651825520832,
-15.7309304768275));
#361610=CARTESIAN_POINT('Ctrl Pts',(0.39117351318407,1.46195342463353,-15.7198771937437));
#361611=CARTESIAN_POINT('Ctrl Pts',(0.00321980990958416,1.5120275866676,
-15.6998208135468));
#361612=CARTESIAN_POINT('Ctrl Pts',(-0.18847028855034,1.50024098128145,
-15.6909389129386));
#361613=CARTESIAN_POINT('Ctrl Pts',(-0.56211869449964,1.40434869273489,
-15.6702980709437));
#361614=CARTESIAN_POINT('Ctrl Pts',(-0.740055987160223,1.31927374142842,
-15.6593738658672));
#361615=CARTESIAN_POINT('Ctrl Pts',(-1.05599671268407,1.08368405233533,
-15.6376290025927));
#361616=CARTESIAN_POINT('Ctrl Pts',(-1.19016110651751,0.934367809352227,
-15.6270263417686));
#361617=CARTESIAN_POINT('Ctrl Pts',(-1.38814783449007,0.599384255812547,
-15.6081956021682));
#361618=CARTESIAN_POINT('Ctrl Pts',(-1.45295516418789,0.418554810098528,
-15.5982530450054));
#361619=CARTESIAN_POINT('Ctrl Pts',(-1.51256821159738,0.0350132169417762,
-15.5769451787189));
#361620=CARTESIAN_POINT('Ctrl Pts',(-1.50401150674298,-0.164443593428988,
-15.5658642448094));
#361621=CARTESIAN_POINT('Ctrl Pts',(-1.41052302220585,-0.54653655484083,
-15.5446368580643));
#361622=CARTESIAN_POINT('Ctrl Pts',(-1.32731037887536,-0.725612665524742,
-15.5353710096694));
#361623=CARTESIAN_POINT('Ctrl Pts',(-1.09860541639505,-1.0393070754435,
-15.5156537034228));
#361624=CARTESIAN_POINT('Ctrl Pts',(-0.956240325103892,-1.17161411743875,
-15.5051289641634));
#361625=CARTESIAN_POINT('Ctrl Pts',(-0.622849133757918,-1.3791768632517,
-15.4833230411629));
#361626=CARTESIAN_POINT('Ctrl Pts',(-0.433429747115656,-1.44990464399728,
-15.4722449360977));
#361627=CARTESIAN_POINT('Ctrl Pts',(-0.157575290483857,-1.49379678385447,
-15.4577536562577));
#361628=CARTESIAN_POINT('Ctrl Pts',(-0.0787664422449298,-1.5,-15.4537896522194));
#361629=CARTESIAN_POINT('Ctrl Pts',(-2.49139148933975E-14,-1.5,-15.45));
#361630=CARTESIAN_POINT('Ctrl Pts',(-1.81538628092389E-13,-1.5,-15.3875));
#361631=CARTESIAN_POINT('Ctrl Pts',(-0.0563819164787718,-1.49999999999999,
-15.3902126762214));
#361632=CARTESIAN_POINT('Ctrl Pts',(-0.112820272486968,-1.49682133988549,
-15.3930163640053));
#361633=CARTESIAN_POINT('Ctrl Pts',(-0.366693800802395,-1.46802622167381,
-15.4060307242262));
#361634=CARTESIAN_POINT('Ctrl Pts',(-0.557892872152436,-1.4065213599787,
-15.416938262216));
#361635=CARTESIAN_POINT('Ctrl Pts',(-0.900375697723385,-1.21521133216021,
-15.4387301422834));
#361636=CARTESIAN_POINT('Ctrl Pts',(-1.04943199886932,-1.08909227907259,
-15.4494049239462));
#361637=CARTESIAN_POINT('Ctrl Pts',(-1.29133268505232,-0.787292734249682,
-15.4694266968261));
#361638=CARTESIAN_POINT('Ctrl Pts',(-1.38192952606011,-0.614527613446004,
-15.4783595770309));
#361639=CARTESIAN_POINT('Ctrl Pts',(-1.49412509971429,-0.238900033630599,
-15.4992277759095));
#361640=CARTESIAN_POINT('Ctrl Pts',(-1.51259570348729,-0.0391031199996457,
-15.5103276044446));
#361641=CARTESIAN_POINT('Ctrl Pts',(-1.47140529217722,0.348608984033488,
-15.5318671657798));
#361642=CARTESIAN_POINT('Ctrl Pts',(-1.41502953905832,0.533175050865238,
-15.5421208361593));
#361643=CARTESIAN_POINT('Ctrl Pts',(-1.23170628994585,0.879224217244925,
-15.5613457898471));
#361644=CARTESIAN_POINT('Ctrl Pts',(-1.10338153525748,1.03572364197227,
-15.5715169656327));
#361645=CARTESIAN_POINT('Ctrl Pts',(-0.796023642645709,1.28640426416543,
-15.5932680797523));
#361646=CARTESIAN_POINT('Ctrl Pts',(-0.62112711033994,1.37938163956646,
-15.6042654979584));
#361647=CARTESIAN_POINT('Ctrl Pts',(-0.251426690538926,1.49092995580701,
-15.6251512820394));
#361648=CARTESIAN_POINT('Ctrl Pts',(-0.0608274576246367,1.5107522237239,
-15.6342747646995));
#361649=CARTESIAN_POINT('Ctrl Pts',(0.326562741336238,1.47746883594747,
-15.6538376228864));
#361650=CARTESIAN_POINT('Ctrl Pts',(0.519344095745307,1.42120313751349,
-15.6646757561926));
#361651=CARTESIAN_POINT('Ctrl Pts',(0.867345798213808,1.23908164937997,
-15.6864779261351));
#361652=CARTESIAN_POINT('Ctrl Pts',(1.02013094421681,1.11667248839913,-15.6972290593712));
#361653=CARTESIAN_POINT('Ctrl Pts',(1.26952313129237,0.821751391166321,
-15.7174201992672));
#361654=CARTESIAN_POINT('Ctrl Pts',(1.36427593646597,0.652469554342664,
-15.7262516914256));
#361655=CARTESIAN_POINT('Ctrl Pts',(1.48692449351355,0.28064626582611,-15.7469085407876));
#361656=CARTESIAN_POINT('Ctrl Pts',(1.51101166939509,0.0808688019443721,
-15.758007288781));
#361657=CARTESIAN_POINT('Ctrl Pts',(1.48032070916219,-0.30887591067725,
-15.7796597728155));
#361658=CARTESIAN_POINT('Ctrl Pts',(1.42876679947988,-0.4953786169298,-15.790021034274));
#361659=CARTESIAN_POINT('Ctrl Pts',(1.25523973112578,-0.844827663861237,
-15.8094348702146));
#361660=CARTESIAN_POINT('Ctrl Pts',(1.13261743009202,-1.00327631324769,
-15.8192090382999));
#361661=CARTESIAN_POINT('Ctrl Pts',(0.834015518184608,-1.26219443505352,
-15.8407676995351));
#361662=CARTESIAN_POINT('Ctrl Pts',(0.66143190822918,-1.36059728730173,
-15.851804544903));
#361663=CARTESIAN_POINT('Ctrl Pts',(0.321498956392526,-1.47402512943341,
-15.8713103500663));
#361664=CARTESIAN_POINT('Ctrl Pts',(0.161184406212371,-1.50000000000001,
-15.8797450116404));
#361665=CARTESIAN_POINT('Ctrl Pts',(-1.15324416682938E-13,-1.5,-15.8875));
#361666=CARTESIAN_POINT('Origin',(0.,1.30104260698261E-15,-17.7));
#361667=CARTESIAN_POINT('',(-3.52181723406995E-14,-1.5,-16.45));
#361668=CARTESIAN_POINT('',(-3.28061311267145E-9,-1.5,-16.3875000003157));
#361669=CARTESIAN_POINT('',(-1.83697019872103E-16,-1.5,-17.7));
#361670=CARTESIAN_POINT('Ctrl Pts',(-7.03256897160998E-14,-1.5,-16.45));
#361671=CARTESIAN_POINT('Ctrl Pts',(0.168036425573696,-1.50000000000001,
-16.4419153437051));
#361672=CARTESIAN_POINT('Ctrl Pts',(0.335044197307986,-1.4717685684019,
-16.4330959721079));
#361673=CARTESIAN_POINT('Ctrl Pts',(0.680086032609039,-1.35140886275186,
-16.4131518139098));
#361674=CARTESIAN_POINT('Ctrl Pts',(0.851531443639169,-1.2504870512757,
-16.4020997590736));
#361675=CARTESIAN_POINT('Ctrl Pts',(1.14601371920132,-0.987774246726167,
-16.3806338960805));
#361676=CARTESIAN_POINT('Ctrl Pts',(1.26599579666737,-0.82842018359447,
-16.371023343533));
#361677=CARTESIAN_POINT('Ctrl Pts',(1.43490714469483,-0.477395294625578,
-16.3515219608125));
#361678=CARTESIAN_POINT('Ctrl Pts',(1.4841605975908,-0.290020872063163,
-16.3411122706702));
#361679=CARTESIAN_POINT('Ctrl Pts',(1.50986212260163,0.100587505098709,
-16.3194118052723));
#361680=CARTESIAN_POINT('Ctrl Pts',(1.48311557158905,0.300302548213859,
-16.3083165250992));
#361681=CARTESIAN_POINT('Ctrl Pts',(1.35554797880811,0.670289337794323,
-16.2877617034559));
#361682=CARTESIAN_POINT('Ctrl Pts',(1.25882822940715,0.83794366300827,-16.2789558552313));
#361683=CARTESIAN_POINT('Ctrl Pts',(1.00588056946405,1.1295673883459,-16.2586852462309));
#361684=CARTESIAN_POINT('Ctrl Pts',(0.85134626809255,1.25016646854075,-16.2479002367397));
#361685=CARTESIAN_POINT('Ctrl Pts',(0.500796045646876,1.42784262728117,
-16.2260989324447));
#361686=CARTESIAN_POINT('Ctrl Pts',(0.307311031573199,1.48159135488892,
-16.2152968601533));
#361687=CARTESIAN_POINT('Ctrl Pts',(-0.0804273149057107,1.5098304912482,
-16.1958573698059));
#361688=CARTESIAN_POINT('Ctrl Pts',(-0.270721495045628,1.48754355738367,
-16.1866288937016));
#361689=CARTESIAN_POINT('Ctrl Pts',(-0.639161421773415,1.37115465935108,
-16.1656692945166));
#361690=CARTESIAN_POINT('Ctrl Pts',(-0.813047372594786,1.27575252329573,
-16.1546531434721));
#361691=CARTESIAN_POINT('Ctrl Pts',(-1.11651136080784,1.02137886522145,
-16.1329867905853));
#361692=CARTESIAN_POINT('Ctrl Pts',(-1.24228452751426,0.864007809213955,
-16.1230004338451));
#361693=CARTESIAN_POINT('Ctrl Pts',(-1.42125313546844,0.516437942199717,
-16.1036909967887));
#361694=CARTESIAN_POINT('Ctrl Pts',(-1.47549587742737,0.330996665444978,
-16.0933887036357));
#361695=CARTESIAN_POINT('Ctrl Pts',(-1.51203470326867,-0.0576521809014891,
-16.0717971010609));
#361696=CARTESIAN_POINT('Ctrl Pts',(-1.4910723524167,-0.257459318260953,
-16.0606967045409));
#361697=CARTESIAN_POINT('Ctrl Pts',(-1.37422796518395,-0.631411640728053,
-16.039921575515));
#361698=CARTESIAN_POINT('Ctrl Pts',(-1.28178637871755,-0.802623545105735,
-16.031041544091));
#361699=CARTESIAN_POINT('Ctrl Pts',(-1.03656461337122,-1.10138523312758,
-16.0109443706265));
#361700=CARTESIAN_POINT('Ctrl Pts',(-0.885848333753066,-1.22587711713333,
-16.0002349223534));
#361701=CARTESIAN_POINT('Ctrl Pts',(-0.540894576375725,-1.41314385564441,
-15.9784364731159));
#361702=CARTESIAN_POINT('Ctrl Pts',(-0.348977633880678,-1.47233713149717,
-15.9675586072523));
#361703=CARTESIAN_POINT('Ctrl Pts',(-0.100798107708362,-1.49746273757136,
-15.95492013073));
#361704=CARTESIAN_POINT('Ctrl Pts',(-0.0503728797114157,-1.49999999999999,
-15.9524235663051));
#361705=CARTESIAN_POINT('Ctrl Pts',(-1.98025440008072E-13,-1.5,-15.95));
#361706=CARTESIAN_POINT('Ctrl Pts',(-1.15591380429656E-13,-1.5,-15.8875));
#361707=CARTESIAN_POINT('Ctrl Pts',(-0.0282996953382467,-1.5,-15.8888615697268));
#361708=CARTESIAN_POINT('Ctrl Pts',(-0.0566240871054407,-1.49919914153783,
-15.8902465737296));
#361709=CARTESIAN_POINT('Ctrl Pts',(-0.283485129586087,-1.48633215611448,
-15.9015188469868));
#361710=CARTESIAN_POINT('Ctrl Pts',(-0.477791833083697,-1.43570158758071,
-15.9122738372991));
#361711=CARTESIAN_POINT('Ctrl Pts',(-0.831408146007146,-1.26356018264295,
-15.9340689157798));
#361712=CARTESIAN_POINT('Ctrl Pts',(-0.988071982085702,-1.14522831828112,
-15.9448934043398));
#361713=CARTESIAN_POINT('Ctrl Pts',(-1.24539023513224,-0.857683675651588,
-15.9652609857459));
#361714=CARTESIAN_POINT('Ctrl Pts',(-1.34452115083349,-0.692011402109955,
-15.9740549221051));
#361715=CARTESIAN_POINT('Ctrl Pts',(-1.47809729028292,-0.324304246911353,
-15.994483097394));
#361716=CARTESIAN_POINT('Ctrl Pts',(-1.50810420074621,-0.124712286570321,
-16.0055715396351));
#361717=CARTESIAN_POINT('Ctrl Pts',(-1.48853544451949,0.266868562855922,
-16.0273260312699));
#361718=CARTESIAN_POINT('Ctrl Pts',(-1.4421174985353,0.455272106590349,
-16.0377928948107));
#361719=CARTESIAN_POINT('Ctrl Pts',(-1.2788482198455,0.808200849278024,
-16.0574000471822));
#361720=CARTESIAN_POINT('Ctrl Pts',(-1.16205342557626,0.968652795358693,
-16.066831033921));
#361721=CARTESIAN_POINT('Ctrl Pts',(-0.872599471298887,1.23593064859787,
-16.0881817786015));
#361722=CARTESIAN_POINT('Ctrl Pts',(-0.702585751391358,1.33989755061812,
-16.099249537015));
#361723=CARTESIAN_POINT('Ctrl Pts',(-0.338806177850127,1.47356192521677,
-16.1204647892019));
#361724=CARTESIAN_POINT('Ctrl Pts',(-0.149481621918083,1.50458947598212,
-16.1301805766684));
#361725=CARTESIAN_POINT('Ctrl Pts',(0.239299609749548,1.49407842338806,
-16.1491777960815));
#361726=CARTESIAN_POINT('Ctrl Pts',(0.434987759787139,1.44923946858524,
-16.1598383731123));
#361727=CARTESIAN_POINT('Ctrl Pts',(0.794035116108409,1.28745866283198,
-16.1816069583685));
#361728=CARTESIAN_POINT('Ctrl Pts',(0.954546097189385,1.17341011083296,
-16.1924975618797));
#361729=CARTESIAN_POINT('Ctrl Pts',(1.2198857778125,0.893439019887669,-16.2130406979644));
#361730=CARTESIAN_POINT('Ctrl Pts',(1.32343910677365,0.731340871006502,
-16.2218699516109));
#361731=CARTESIAN_POINT('Ctrl Pts',(1.46793947870625,0.367886953782886,
-16.2420618359011));
#361732=CARTESIAN_POINT('Ctrl Pts',(1.50390407689632,0.168652212602878,
-16.2531304326333));
#361733=CARTESIAN_POINT('Ctrl Pts',(1.49558655333712,-0.224460277777845,
-16.2749700154322));
#361734=CARTESIAN_POINT('Ctrl Pts',(1.45439300750538,-0.414631844673234,
-16.285535102482));
#361735=CARTESIAN_POINT('Ctrl Pts',(1.30139496490231,-0.770963910381184,
-16.3053313283546));
#361736=CARTESIAN_POINT('Ctrl Pts',(1.19029155446738,-0.933396272503928,
-16.3144930784542));
#361737=CARTESIAN_POINT('Ctrl Pts',(0.909964975941346,-1.20878284364848,
-16.3356299242282));
#361738=CARTESIAN_POINT('Ctrl Pts',(0.742666467555146,-1.31819339066415,
-16.3467182593274));
#361739=CARTESIAN_POINT('Ctrl Pts',(0.382138693371518,-1.46296970865467,
-16.3680857243389));
#361740=CARTESIAN_POINT('Ctrl Pts',(0.193358648206561,-1.49964906173907,
-16.3781872794157));
#361741=CARTESIAN_POINT('Ctrl Pts',(0.00182787874326844,-1.49999916475107,
-16.3874120329417));
#361742=CARTESIAN_POINT('Ctrl Pts',(0.000913917476143004,-1.500000000004,
-16.387456029125));
#361743=CARTESIAN_POINT('Ctrl Pts',(-6.56122786601575E-9,-1.5,-16.3875000003157));
#361744=CARTESIAN_POINT('Origin',(0.,1.30104260698261E-15,-17.7));
#361745=CARTESIAN_POINT('',(-3.27497425406278E-15,-1.5,-16.95));
#361746=CARTESIAN_POINT('',(7.40069566007051E-14,-1.5,-16.8875));
#361747=CARTESIAN_POINT('',(-1.83697019872103E-16,-1.5,-17.7));
#361748=CARTESIAN_POINT('Ctrl Pts',(-6.36625148825346E-15,-1.5,-16.95));
#361749=CARTESIAN_POINT('Ctrl Pts',(0.00717878911557301,-1.5,-16.9496546103476));
#361750=CARTESIAN_POINT('Ctrl Pts',(0.0143597453507418,-1.49994846502973,
-16.9493076849027));
#361751=CARTESIAN_POINT('Ctrl Pts',(0.212376106994468,-1.49710435039622,
-16.9397016150769));
#361752=CARTESIAN_POINT('Ctrl Pts',(0.400911243289437,-1.45796825101003,
-16.9295436002308));
#361753=CARTESIAN_POINT('Ctrl Pts',(0.759987383851973,-1.3083234108683,
-16.9081107402479));
#361754=CARTESIAN_POINT('Ctrl Pts',(0.926044855054272,-1.1965525530469,
-16.897016550389));
#361755=CARTESIAN_POINT('Ctrl Pts',(1.20235571743438,-0.917667416345093,
-16.8759757284716));
#361756=CARTESIAN_POINT('Ctrl Pts',(1.31099152978271,-0.754365753138052,
-16.8669092085077));
#361757=CARTESIAN_POINT('Ctrl Pts',(1.45945581927049,-0.396556979756925,
-16.8470309433198));
#361758=CARTESIAN_POINT('Ctrl Pts',(1.4983193728066,-0.205649305285253,
-16.8364249614047));
#361759=CARTESIAN_POINT('Ctrl Pts',(1.50163878727677,0.188039890760164,
-16.8145533394022));
#361760=CARTESIAN_POINT('Ctrl Pts',(1.46303737424034,0.387061948217881,
-16.8034965584324));
#361761=CARTESIAN_POINT('Ctrl Pts',(1.31372064674803,0.748597044662741,
-16.7834112752965));
#361762=CARTESIAN_POINT('Ctrl Pts',(1.20819922581391,0.909131369903976,
-16.7745425298575));
#361763=CARTESIAN_POINT('Ctrl Pts',(0.939292039335553,1.18569679716197,
-16.7539223538365));
#361764=CARTESIAN_POINT('Ctrl Pts',(0.777097385352746,1.29779011578116,
-16.7430050566133));
#361765=CARTESIAN_POINT('Ctrl Pts',(0.415719640656572,1.45488122333486,
-16.7212546198885));
#361766=CARTESIAN_POINT('Ctrl Pts',(0.219471117337767,1.49711751151553,
-16.7106393781808));
#361767=CARTESIAN_POINT('Ctrl Pts',(-0.169562171286055,1.50247953702935,
-16.6917730602017));
#361768=CARTESIAN_POINT('Ctrl Pts',(-0.358634652400107,1.46888588907569,
-16.6818809013823));
#361769=CARTESIAN_POINT('Ctrl Pts',(-0.72098912092783,1.33012556726985,
-16.6605926605033));
#361770=CARTESIAN_POINT('Ctrl Pts',(-0.889782806071457,1.22366226856375,
-16.6495142566874));
#361771=CARTESIAN_POINT('Ctrl Pts',(-1.17507366301727,0.952658247764962,
-16.6282603044662));
#361772=CARTESIAN_POINT('Ctrl Pts',(-1.28925790013609,0.791301639710218,
-16.6189612022061));
#361773=CARTESIAN_POINT('Ctrl Pts',(-1.44784764442517,0.436812377816807,
-16.5992673543232));
#361774=CARTESIAN_POINT('Ctrl Pts',(-1.49189503873834,0.247586245339542,
-16.5887547914078));
#361775=CARTESIAN_POINT('Ctrl Pts',(-1.5063509150992,-0.144730905312155,
-16.5669593941493));
#361776=CARTESIAN_POINT('Ctrl Pts',(-1.47363286889394,-0.344181505946763,
-16.5558788052252));
#361777=CARTESIAN_POINT('Ctrl Pts',(-1.33507745593545,-0.709967243911615,
-16.5355573753382));
#361778=CARTESIAN_POINT('Ctrl Pts',(-1.23393748040781,-0.874005706767427,
-16.526756575074));
#361779=CARTESIAN_POINT('Ctrl Pts',(-0.972975121217884,-1.15812390953611,
-16.5063088454143));
#361780=CARTESIAN_POINT('Ctrl Pts',(-0.814553352492015,-1.27452938786755,
-16.4954532890034));
#361781=CARTESIAN_POINT('Ctrl Pts',(-0.458437576191844,-1.44199606386582,
-16.4736678086166));
#361782=CARTESIAN_POINT('Ctrl Pts',(-0.263482699756925,-1.49000622960536,
-16.4629544220358));
#361783=CARTESIAN_POINT('Ctrl Pts',(-0.0432058286522188,-1.49953365893944,
-16.4520916953186));
#361784=CARTESIAN_POINT('Ctrl Pts',(-0.0215950339203933,-1.5,-16.4510389915539));
#361785=CARTESIAN_POINT('Ctrl Pts',(-7.0252647661527E-14,-1.5,-16.45));
#361786=CARTESIAN_POINT('Ctrl Pts',(-6.56122874781451E-9,-1.5,-16.3875000003157));
#361787=CARTESIAN_POINT('Ctrl Pts',(-0.197760835115308,-1.49999999913496,
-16.3970147726398));
#361788=CARTESIAN_POINT('Ctrl Pts',(-0.393674363985098,-1.46088922717867,
-16.4075270770246));
#361789=CARTESIAN_POINT('Ctrl Pts',(-0.756980891744115,-1.30966991596929,
-16.4292072069137));
#361790=CARTESIAN_POINT('Ctrl Pts',(-0.921128318171999,-1.19990983310728,
-16.4401536448406));
#361791=CARTESIAN_POINT('Ctrl Pts',(-1.19422167497537,-0.9273709277071,
-16.460863380246));
#361792=CARTESIAN_POINT('Ctrl Pts',(-1.30205526275989,-0.768652145532881,
-16.4697971030261));
#361793=CARTESIAN_POINT('Ctrl Pts',(-1.45614334856541,-0.411354813164807,
-16.4896469548243));
#361794=CARTESIAN_POINT('Ctrl Pts',(-1.49779139671246,-0.214869528570988,
-16.5005628039684));
#361795=CARTESIAN_POINT('Ctrl Pts',(-1.50197888629897,0.177339198454728,
-16.522352177692));
#361796=CARTESIAN_POINT('Ctrl Pts',(-1.46663648684746,0.36929929400795,
-16.533016627445));
#361797=CARTESIAN_POINT('Ctrl Pts',(-1.32497448529002,0.729294436104746,
-16.5530163575615));
#361798=CARTESIAN_POINT('Ctrl Pts',(-1.21999111521496,0.893897793943286,
-16.5619669777115));
#361799=CARTESIAN_POINT('Ctrl Pts',(-0.949687696780064,1.17794207999332,
-16.5828620760514));
#361800=CARTESIAN_POINT('Ctrl Pts',(-0.785538396757973,1.2932036942435,
-16.593961424438));
#361801=CARTESIAN_POINT('Ctrl Pts',(-0.42874359030238,1.45007444994965,
-16.6154852435592));
#361802=CARTESIAN_POINT('Ctrl Pts',(-0.240632039256655,1.49286834004424,
-16.625724483948));
#361803=CARTESIAN_POINT('Ctrl Pts',(0.150965629028709,1.50580608204866,
-16.6449246172702));
#361804=CARTESIAN_POINT('Ctrl Pts',(0.350813587754195,1.47214577207638,
-16.655152255164));
#361805=CARTESIAN_POINT('Ctrl Pts',(0.721214931117633,1.32977784672249,
-16.6769278626988));
#361806=CARTESIAN_POINT('Ctrl Pts',(0.888712464670945,1.22419508548818,
-16.687919446018));
#361807=CARTESIAN_POINT('Ctrl Pts',(1.16912185117981,0.958774356216467,
-16.708783446952));
#361808=CARTESIAN_POINT('Ctrl Pts',(1.28100791450679,0.803180363582307,
-16.71787886869));
#361809=CARTESIAN_POINT('Ctrl Pts',(1.44454094300695,0.450399892657063,
-16.7374777837414));
#361810=CARTESIAN_POINT('Ctrl Pts',(1.49145811670285,0.2551290911654,-16.7483261616021));
#361811=CARTESIAN_POINT('Ctrl Pts',(1.50623123857247,-0.137301746650813,
-16.7701278748141));
#361812=CARTESIAN_POINT('Ctrl Pts',(1.47589844403143,-0.330637120387082,
-16.7808687289105));
#361813=CARTESIAN_POINT('Ctrl Pts',(1.34382317997907,-0.693653962162479,
-16.8010363312314));
#361814=CARTESIAN_POINT('Ctrl Pts',(1.24388886091701,-0.86009207853055,
-16.809878149235));
#361815=CARTESIAN_POINT('Ctrl Pts',(0.982011607657436,-1.15122916903297,
-16.8305648658598));
#361816=CARTESIAN_POINT('Ctrl Pts',(0.820640162711084,-1.27130434030765,
-16.841664274549));
#361817=CARTESIAN_POINT('Ctrl Pts',(0.467262008540732,-1.4381909115658,
-16.8633019270092));
#361818=CARTESIAN_POINT('Ctrl Pts',(0.279858196352626,-1.4860778314542,
-16.8736485893462));
#361819=CARTESIAN_POINT('Ctrl Pts',(0.0589934646081979,-1.49913079072886,
-16.8846375309088));
#361820=CARTESIAN_POINT('Ctrl Pts',(0.0294826483031038,-1.5,-16.8860815154222));
#361821=CARTESIAN_POINT('Ctrl Pts',(1.48197610221282E-13,-1.5,-16.8875));
#361822=CARTESIAN_POINT('Origin',(0.,0.,0.));
#361823=CARTESIAN_POINT('',(1.,-0.577350269189625,0.));
#361824=CARTESIAN_POINT('',(1.,0.577350269189625,0.));
#361825=CARTESIAN_POINT('Ctrl Pts',(1.,0.577350269189567,-2.89100513080514E-14));
#361826=CARTESIAN_POINT('Ctrl Pts',(1.,0.,-0.288675134594789));
#361827=CARTESIAN_POINT('Ctrl Pts',(1.,-0.577350269189567,-2.89669235401328E-14));
#361828=CARTESIAN_POINT('Origin',(0.,0.,0.));
#361829=CARTESIAN_POINT('Origin',(-9.08513196663917E-30,1.30104260698261E-15,
-2.72083333333333));
#361830=CARTESIAN_POINT('',(1.92031473636372E-14,-2.75,-1.275));
#361831=CARTESIAN_POINT('Origin',(0.,0.,-1.275));
#361832=CARTESIAN_POINT('',(1.48387956900833E-14,-1.5,0.));
#361833=CARTESIAN_POINT('Origin',(0.,0.,0.));
#361834=CARTESIAN_POINT('Origin',(0.,-6.07153216591882E-15,-1.275));
#361835=CARTESIAN_POINT('',(3.5,-6.5001585456204E-15,-1.7));
#361836=CARTESIAN_POINT('Origin',(0.,-6.07153216591882E-15,-1.7));
#361837=CARTESIAN_POINT('',(3.5,-6.5001585456204E-15,-1.275));
#361838=CARTESIAN_POINT('',(3.5,-6.5001585456204E-15,-1.275));
#361839=CARTESIAN_POINT('Origin',(0.,-6.07153216591882E-15,-1.275));
#361840=CARTESIAN_POINT('Origin',(0.,1.30104260698261E-15,-17.7));
#361841=CARTESIAN_POINT('',(-0.190653686693216,-1.15967294634856,-17.6497595264192));
#361842=CARTESIAN_POINT('Origin',(1.61565205658576E-12,-4.96575003339217E-12,
-17.6497595264242));
#361843=CARTESIAN_POINT('',(1.5,1.19400060681869E-14,-17.325));
#361844=CARTESIAN_POINT('Ctrl Pts',(-0.190653686693157,-1.15967294634849,
-17.6497595264193));
#361845=CARTESIAN_POINT('Ctrl Pts',(-0.0284998709946839,-1.21316624422583,
-17.6232802583166));
#361846=CARTESIAN_POINT('Ctrl Pts',(0.132812584998293,-1.22453742267452,
-17.6019314805365));
#361847=CARTESIAN_POINT('Ctrl Pts',(0.43460101025012,-1.20145302480442,
-17.556617792806));
#361848=CARTESIAN_POINT('Ctrl Pts',(0.585964437952993,-1.1617261501811,
-17.5329612724316));
#361849=CARTESIAN_POINT('Ctrl Pts',(0.869448526794397,-1.02932298167968,
-17.4866550394236));
#361850=CARTESIAN_POINT('Ctrl Pts',(0.998920187452606,-0.936988886374714,
-17.4643879452696));
#361851=CARTESIAN_POINT('Ctrl Pts',(1.23902574358817,-0.688927643824148,
-17.4195390704608));
#361852=CARTESIAN_POINT('Ctrl Pts',(1.32213723929246,-0.544619521972593,
-17.4001916451074));
#361853=CARTESIAN_POINT('Ctrl Pts',(1.43760569485959,-0.296763466124491,
-17.364807974774));
#361854=CARTESIAN_POINT('Ctrl Pts',(1.48023624450735,-0.15035662689787,
-17.3447637554926));
#361855=CARTESIAN_POINT('Ctrl Pts',(1.5,-5.5719318048375E-14,-17.325));
#361856=CARTESIAN_POINT('',(1.05094390383305,-1.07028823734362,-17.325));
#361857=CARTESIAN_POINT('Origin',(0.,1.27054942088145E-15,-17.325));
#361858=CARTESIAN_POINT('',(1.21319421105025E-11,1.30188293868178,-17.5231170613182));
#361859=CARTESIAN_POINT('Ctrl Pts',(1.05094390383306,-1.07028823734362,
-17.325));
#361860=CARTESIAN_POINT('Ctrl Pts',(0.935385993427474,-1.17626791798079,
-17.330344050598));
#361861=CARTESIAN_POINT('Ctrl Pts',(0.803785254470359,-1.26328904652287,
-17.3359002371836));
#361862=CARTESIAN_POINT('Ctrl Pts',(0.516934873238126,-1.39355888591543,
-17.3470910935073));
#361863=CARTESIAN_POINT('Ctrl Pts',(0.363306541543587,-1.43555902061286,
-17.3526546969488));
#361864=CARTESIAN_POINT('Ctrl Pts',(0.0426040379259422,-1.47015363976017,
-17.3634241785173));
#361865=CARTESIAN_POINT('Ctrl Pts',(-0.153813269939513,-1.46406932942307,
-17.3692656832653));
#361866=CARTESIAN_POINT('Ctrl Pts',(-0.544498419837906,-1.34782426630485,
-17.3835915070066));
#361867=CARTESIAN_POINT('Ctrl Pts',(-0.712708756400491,-1.25901794320711,
-17.3905532160389));
#361868=CARTESIAN_POINT('Ctrl Pts',(-0.994597414971914,-1.02998098075363,
-17.4038861495252));
#361869=CARTESIAN_POINT('Ctrl Pts',(-1.10896900381996,-0.895834524037364,
-17.4101516283496));
#361870=CARTESIAN_POINT('Ctrl Pts',(-1.31543167012074,-0.538181445013064,
-17.4238015714036));
#361871=CARTESIAN_POINT('Ctrl Pts',(-1.3550125850498,-0.35227324511601,
-17.4305084599621));
#361872=CARTESIAN_POINT('Ctrl Pts',(-1.39356381858887,-0.0519947242753176,
-17.4418520811531));
#361873=CARTESIAN_POINT('Ctrl Pts',(-1.38187430699883,0.12723752056229,
-17.4487219473622));
#361874=CARTESIAN_POINT('Ctrl Pts',(-1.29309014390597,0.463770583356018,
-17.4618139578014));
#361875=CARTESIAN_POINT('Ctrl Pts',(-1.21939859014006,0.619852828413784,
-17.4676355285718));
#361876=CARTESIAN_POINT('Ctrl Pts',(-1.01621515776853,0.898746785102145,
-17.4797586572927));
#361877=CARTESIAN_POINT('Ctrl Pts',(-0.88577741068908,1.01869874939368,
-17.4864917330467));
#361878=CARTESIAN_POINT('Ctrl Pts',(-0.592305977603864,1.19696902839803,
-17.5000787478208));
#361879=CARTESIAN_POINT('Ctrl Pts',(-0.4335679262802,1.25612063590089,-17.5067931009191));
#361880=CARTESIAN_POINT('Ctrl Pts',(-0.19744601600065,1.29605054472226,
-17.5159479725373));
#361881=CARTESIAN_POINT('Ctrl Pts',(-0.106030063883377,1.30560924308118,
-17.5193907569208));
#361882=CARTESIAN_POINT('Ctrl Pts',(2.42640436556823E-11,1.30188293868178,
-17.5231170613182));
#361883=CARTESIAN_POINT('',(-1.37772764904077E-16,1.125,-17.7));
#361884=CARTESIAN_POINT('',(-1.37772764904077E-16,1.125,-17.7));
#361885=CARTESIAN_POINT('Origin',(0.,1.30104260698261E-15,-17.7));
#361886=CARTESIAN_POINT('Ctrl Pts',(2.42640436556823E-11,1.30188293868178,
-17.5231170613182));
#361887=CARTESIAN_POINT('Ctrl Pts',(0.0760719339486668,1.2992094782347,
-17.5257905217639));
#361888=CARTESIAN_POINT('Ctrl Pts',(0.159648962549911,1.28947675310995,
-17.5288785177485));
#361889=CARTESIAN_POINT('Ctrl Pts',(0.40269613660347,1.2320476915949,-17.5385272441259));
#361890=CARTESIAN_POINT('Ctrl Pts',(0.548816268504338,1.16713624115107,
-17.5450297256207));
#361891=CARTESIAN_POINT('Ctrl Pts',(0.818207535128496,0.981215796564792,
-17.5585876105205));
#361892=CARTESIAN_POINT('Ctrl Pts',(0.936716607513114,0.858672224092071,
-17.5655185585548));
#361893=CARTESIAN_POINT('Ctrl Pts',(1.11591095938415,0.579498508975487,
-17.5781734173653));
#361894=CARTESIAN_POINT('Ctrl Pts',(1.17608370721062,0.42793868292318,-17.5841070452516));
#361895=CARTESIAN_POINT('Ctrl Pts',(1.23202197995131,0.11483696308775,-17.5973875990212));
#361896=CARTESIAN_POINT('Ctrl Pts',(1.22996230656325,-0.0417057257492802,
-17.6041323253085));
#361897=CARTESIAN_POINT('Ctrl Pts',(1.16140063641678,-0.374600983755444,
-17.6187180909218));
#361898=CARTESIAN_POINT('Ctrl Pts',(1.08806635420093,-0.523009838130679,
-17.6251950806039));
#361899=CARTESIAN_POINT('Ctrl Pts',(0.926670564829111,-0.759859567065848,
-17.636382069517));
#361900=CARTESIAN_POINT('Ctrl Pts',(0.816778283270273,-0.867993743880628,
-17.6429384269021));
#361901=CARTESIAN_POINT('Ctrl Pts',(0.689217670442692,-0.95192918512462,
-17.6497595264192));
#361902=CARTESIAN_POINT('Origin',(0.,1.30104260698261E-15,-17.7));
#361903=CARTESIAN_POINT('',(0.,1.5,-17.1375));
#361904=CARTESIAN_POINT('Ctrl Pts',(1.48214773787458E-13,-1.5,-16.8875));
#361905=CARTESIAN_POINT('Ctrl Pts',(-0.168700874931512,-1.5,-16.8956166246295));
#361906=CARTESIAN_POINT('Ctrl Pts',(-0.336404258415459,-1.4715456896381,
-16.9044756549396));
#361907=CARTESIAN_POINT('Ctrl Pts',(-0.681664294759072,-1.3505624135401,
-16.9244476327415));
#361908=CARTESIAN_POINT('Ctrl Pts',(-0.852691790631952,-1.24964098115487,
-16.935479570095));
#361909=CARTESIAN_POINT('Ctrl Pts',(-1.14101924136252,-0.992046267738318,
-16.9565071397422));
#361910=CARTESIAN_POINT('Ctrl Pts',(-1.25731577449887,-0.839770223914915,
-16.9658460986716));
#361911=CARTESIAN_POINT('Ctrl Pts',(-1.43092610724364,-0.491934042916581,
-16.9851703309492));
#361912=CARTESIAN_POINT('Ctrl Pts',(-1.48345731807414,-0.298128007144441,
-16.9959373329364));
#361913=CARTESIAN_POINT('Ctrl Pts',(-1.50960821845787,0.0942209676885727,
-17.0177344982049));
#361914=CARTESIAN_POINT('Ctrl Pts',(-1.48470482643099,0.288888827938097,
-17.0285493793299));
#361915=CARTESIAN_POINT('Ctrl Pts',(-1.36291637315436,0.655072135992765,
-17.0488928964441));
#361916=CARTESIAN_POINT('Ctrl Pts',(-1.26827983757057,0.823483999572315,
-17.0576877467413));
#361917=CARTESIAN_POINT('Ctrl Pts',(-1.0153840018506,1.12201042967563,-17.0781476041466));
#361918=CARTESIAN_POINT('Ctrl Pts',(-0.857099532258911,1.24710842449888,
-17.0892380135412));
#361919=CARTESIAN_POINT('Ctrl Pts',(-0.572347677865173,1.39166121246558,
-17.1069534987447));
#361920=CARTESIAN_POINT('Ctrl Pts',(-0.4596082437036,1.4328525882471,-17.1135218821827));
#361921=CARTESIAN_POINT('Ctrl Pts',(-0.23070953814774,1.48664703132354,
-17.1260290663739));
#361922=CARTESIAN_POINT('Ctrl Pts',(-0.115555336796759,1.5,-17.1319403412662));
#361923=CARTESIAN_POINT('Ctrl Pts',(0.,1.5,-17.1375));
#361924=CARTESIAN_POINT('Ctrl Pts',(1.05094390383305,-1.07028823734362,
-17.325));
#361925=CARTESIAN_POINT('Ctrl Pts',(1.19681767290924,-0.927050983124833,
-17.3140028323958));
#361926=CARTESIAN_POINT('Ctrl Pts',(1.29903810567665,-0.749999999999992,
-17.3041666666667));
#361927=CARTESIAN_POINT('Ctrl Pts',(1.73205080756887,5.56731272112934E-15,
-17.2625));
#361928=CARTESIAN_POINT('Ctrl Pts',(1.29903810567665,0.750000000000003,
-17.2208333333333));
#361929=CARTESIAN_POINT('Ctrl Pts',(0.866025403784432,1.50000000000001,
-17.1791666666667));
#361930=CARTESIAN_POINT('Ctrl Pts',(0.,1.5,-17.1375));
#361931=CARTESIAN_POINT('Ctrl Pts',(1.5,-9.16905440462301E-13,-17.325));
#361932=CARTESIAN_POINT('Ctrl Pts',(1.50000000000007,0.113382160049262,
-17.3187009911084));
#361933=CARTESIAN_POINT('Ctrl Pts',(1.48714599278535,0.226394075227564,
-17.3124225513762));
#361934=CARTESIAN_POINT('Ctrl Pts',(1.43685459231838,0.444596795408891,
-17.3003001780328));
#361935=CARTESIAN_POINT('Ctrl Pts',(1.40019786486094,0.549243517321112,
-17.2944864712599));
#361936=CARTESIAN_POINT('Ctrl Pts',(1.27022036812056,0.820121616189383,
-17.2794376879895));
#361937=CARTESIAN_POINT('Ctrl Pts',(1.15630836828071,0.974180856589762,
-17.2702389996247));
#361938=CARTESIAN_POINT('Ctrl Pts',(0.872255139316108,1.23601632287667,
-17.2492992748773));
#361939=CARTESIAN_POINT('Ctrl Pts',(0.703120346224601,1.33947189512315,
-17.2382880074548));
#361940=CARTESIAN_POINT('Ctrl Pts',(0.331429097945265,1.47650377647961,
-17.2165985627852));
#361941=CARTESIAN_POINT('Ctrl Pts',(0.132114621180555,1.50745501208499,
-17.2065634513442));
#361942=CARTESIAN_POINT('Ctrl Pts',(-0.258608395317897,1.48988839341874,
-17.1872768198185));
#361943=CARTESIAN_POINT('Ctrl Pts',(-0.446412994821231,1.44476268630561,
-17.1769875749477));
#361944=CARTESIAN_POINT('Ctrl Pts',(-0.801678290027555,1.28329967090816,
-17.1554097817016));
#361945=CARTESIAN_POINT('Ctrl Pts',(-0.96457328759709,1.16582740490308,
-17.1443093739767));
#361946=CARTESIAN_POINT('Ctrl Pts',(-1.23102809938628,0.878523264761282,
-17.1235088903078));
#361947=CARTESIAN_POINT('Ctrl Pts',(-1.33369501556255,0.713083676857493,
-17.1146157598254));
#361948=CARTESIAN_POINT('Ctrl Pts',(-1.47098536711031,0.351701939382808,
-17.0945389966324));
#361949=CARTESIAN_POINT('Ctrl Pts',(-1.50404981696719,0.159098896944735,
-17.083838827608));
#361950=CARTESIAN_POINT('Ctrl Pts',(-1.49503834317181,-0.233246755242361,
-17.062041846931));
#361951=CARTESIAN_POINT('Ctrl Pts',(-1.45098360774137,-0.429196364751628,
-17.0511557575138));
#361952=CARTESIAN_POINT('Ctrl Pts',(-1.29258205682888,-0.784445130722396,
-17.0314197149599));
#361953=CARTESIAN_POINT('Ctrl Pts',(-1.18290688373643,-0.941734829338834,
-17.022419999831));
#361954=CARTESIAN_POINT('Ctrl Pts',(-0.906484956369989,-1.21104821023222,
-17.0016397164027));
#361955=CARTESIAN_POINT('Ctrl Pts',(-0.740803185746063,-1.31892334248899,
-16.9906718170453));
#361956=CARTESIAN_POINT('Ctrl Pts',(-0.381222093318042,-1.46335566825523,
-16.9693594546205));
#361957=CARTESIAN_POINT('Ctrl Pts',(-0.19142984944887,-1.5,-16.9592101729258));
#361958=CARTESIAN_POINT('Ctrl Pts',(-4.23272528138341E-15,-1.5,-16.95));
#361959=CARTESIAN_POINT('Origin',(-1.04744440165294E-14,-1.5,-17.7));
#361960=CARTESIAN_POINT('Origin',(1.92031473636372E-14,-2.75,-1.7));
#361961=CARTESIAN_POINT('Ctrl Pts',(-0.823407874165082,-0.838564036615827,
-1.7));
#361962=CARTESIAN_POINT('Ctrl Pts',(-0.906490492544621,-0.774359745626708,
-1.7));
#361963=CARTESIAN_POINT('Ctrl Pts',(-0.98024328853839,-0.698926148377459,
-1.7));
#361964=CARTESIAN_POINT('Ctrl Pts',(-1.08660188806759,-0.554873516577794,
-1.7));
#361965=CARTESIAN_POINT('Ctrl Pts',(-1.1486524092587,-0.460342302886378,
-1.7));
#361966=CARTESIAN_POINT('Ctrl Pts',(-1.26101256383043,-0.17907236672097,
-1.7));
#361967=CARTESIAN_POINT('Ctrl Pts',(-1.29189854216959,-0.0173431812158739,
-1.7));
#361968=CARTESIAN_POINT('Ctrl Pts',(-1.29108788069115,0.299928246129644,
-1.7));
#361969=CARTESIAN_POINT('Ctrl Pts',(-1.26280625062506,0.452633561520656,
-1.7));
#361970=CARTESIAN_POINT('Ctrl Pts',(-1.1540332144262,0.739009154469549,
-1.7));
#361971=CARTESIAN_POINT('Ctrl Pts',(-1.06946235041198,0.885676341398372,
-1.70000000000001));
#361972=CARTESIAN_POINT('Ctrl Pts',(-0.838259841587371,1.15024128579277,
-1.70000000000001));
#361973=CARTESIAN_POINT('Ctrl Pts',(-0.700104404477312,1.25940267622837,
-1.7));
#361974=CARTESIAN_POINT('Ctrl Pts',(-0.464671189528445,1.38344546062926,
-1.7));
#361975=CARTESIAN_POINT('Ctrl Pts',(-0.379819280861329,1.41817253578376,
-1.69999999991087));
#361976=CARTESIAN_POINT('Ctrl Pts',(-0.197016232181906,1.47315729177752,
-1.69999999991087));
#361977=CARTESIAN_POINT('Ctrl Pts',(-0.0990761231255047,1.4917436564062,
-1.7));
#361978=CARTESIAN_POINT('Ctrl Pts',(0.,1.49999999999999,-1.7));
#361979=CARTESIAN_POINT('Ctrl Pts',(1.05094390383303,1.07028823734365,-1.7));
#361980=CARTESIAN_POINT('Ctrl Pts',(1.15645058505027,0.945436326977039,
-1.7));
#361981=CARTESIAN_POINT('Ctrl Pts',(1.25865636483395,0.783904299885076,
-1.7));
#361982=CARTESIAN_POINT('Ctrl Pts',(1.37926580863893,0.431617173084607,
-1.7));
#361983=CARTESIAN_POINT('Ctrl Pts',(1.40434751926454,0.262443514736457,
-1.7));
#361984=CARTESIAN_POINT('Ctrl Pts',(1.39184293889025,-0.0842766397941932,
-1.7));
#361985=CARTESIAN_POINT('Ctrl Pts',(1.35147890198672,-0.258564301101902,
-1.69999999999998));
#361986=CARTESIAN_POINT('Ctrl Pts',(1.22264360102688,-0.547784828945173,
-1.69999999999998));
#361987=CARTESIAN_POINT('Ctrl Pts',(1.1307158712709,-0.704303629990696,
-1.69999999996056));
#361988=CARTESIAN_POINT('Ctrl Pts',(0.870778252488567,-0.949211899826218,
-1.69999999996056));
#361989=CARTESIAN_POINT('Ctrl Pts',(0.741392706431225,-1.03250755194956,
-1.7));
#361990=CARTESIAN_POINT('Ctrl Pts',(0.507423555842253,-1.12806524548885,
-1.7));
#361991=CARTESIAN_POINT('Ctrl Pts',(0.410508853202597,-1.15454268439211,
-1.7));
#361992=CARTESIAN_POINT('Ctrl Pts',(0.208302465257298,-1.18420948820834,
-1.7));
#361993=CARTESIAN_POINT('Ctrl Pts',(0.103673587510497,-1.18626732189837,
-1.7));
#361994=CARTESIAN_POINT('Ctrl Pts',(-1.38777878078145E-16,-1.17524047358083,
-1.7));
#361995=CARTESIAN_POINT('Origin',(0.,-6.07153216591882E-15,-1.275));
#361996=CARTESIAN_POINT('Origin',(1.04744440165294E-14,-1.5,0.));
#361997=CARTESIAN_POINT('',(-0.999999999999999,0.577350269189625,0.));
#361998=CARTESIAN_POINT('',(-0.999999999999999,-0.577350269189627,0.));
#361999=CARTESIAN_POINT('Origin',(0.,0.,0.));
#362000=CARTESIAN_POINT('',(3.25260651745651E-16,1.15470053837925,0.));
#362001=CARTESIAN_POINT('Origin',(0.,0.,0.));
#362002=CARTESIAN_POINT('Origin',(0.,0.,0.));
#362003=CARTESIAN_POINT('',(5.42101086242752E-16,-1.15470053837925,0.));
#362004=CARTESIAN_POINT('Origin',(0.,0.,0.));
#362005=CARTESIAN_POINT('Origin',(0.,0.,0.));
#362006=CARTESIAN_POINT('Origin',(0.,0.,0.));
#362007=CARTESIAN_POINT('Ctrl Pts',(0.999999999999951,0.577350269189654,
-2.7791564077117E-14));
#362008=CARTESIAN_POINT('Ctrl Pts',(0.500000000000001,0.866025403784438,
-0.28867513459479));
#362009=CARTESIAN_POINT('Ctrl Pts',(5.09575199449458E-14,1.15470053837922,
-2.90996254149895E-14));
#362010=CARTESIAN_POINT('Origin',(0.,0.,0.));
#362011=CARTESIAN_POINT('Ctrl Pts',(-4.99717345888679E-14,1.15470053837922,
-2.93650291647028E-14));
#362012=CARTESIAN_POINT('Ctrl Pts',(-0.5,0.866025403784438,-0.288675134594791));
#362013=CARTESIAN_POINT('Ctrl Pts',(-0.999999999999949,0.577350269189654,
-2.94219013967842E-14));
#362014=CARTESIAN_POINT('Origin',(0.,0.,0.));
#362015=CARTESIAN_POINT('Ctrl Pts',(-0.999999999999999,0.577350269189567,
-2.99337514855168E-14));
#362016=CARTESIAN_POINT('Ctrl Pts',(-0.999999999999999,-1.33226762955019E-15,
-0.288675134594791));
#362017=CARTESIAN_POINT('Ctrl Pts',(-0.999999999999999,-0.57735026918957,
-2.85119456834816E-14));
#362018=CARTESIAN_POINT('Origin',(0.,0.,0.));
#362019=CARTESIAN_POINT('Ctrl Pts',(-0.999999999999948,-0.577350269189654,
-2.99906237175983E-14));
#362020=CARTESIAN_POINT('Ctrl Pts',(-0.499999999999999,-0.866025403784438,
-0.288675134594791));
#362021=CARTESIAN_POINT('Ctrl Pts',(-4.92134381611157E-14,-1.15470053837922,
-2.91564976470709E-14));
#362022=CARTESIAN_POINT('Origin',(0.,0.,0.));
#362023=CARTESIAN_POINT('Ctrl Pts',(5.0350882802744E-14,-1.15470053837922,
-2.93650291647027E-14));
#362024=CARTESIAN_POINT('Ctrl Pts',(0.5,-0.866025403784437,-0.288675134594791));
#362025=CARTESIAN_POINT('Ctrl Pts',(0.99999999999995,-0.577350269189653,
-2.91944124684585E-14));
#362026=CARTESIAN_POINT('Origin',(1.,-0.577350269189624,-1.19));
#362027=CARTESIAN_POINT('',(1.9352544089507E-16,-1.15470053837925,-1.19));
#362028=CARTESIAN_POINT('',(1.,-0.577350269189624,-1.19));
#362029=CARTESIAN_POINT('',(1.9352544089507E-16,-1.15470053837925,-1.19));
#362030=CARTESIAN_POINT('',(1.,0.577350269189626,-1.19));
#362031=CARTESIAN_POINT('',(1.,-0.577350269189624,-1.19));
#362032=CARTESIAN_POINT('',(3.85779730129493E-16,1.15470053837925,-1.19));
#362033=CARTESIAN_POINT('',(1.,0.577350269189626,-1.19));
#362034=CARTESIAN_POINT('',(-0.999999999999999,0.577350269189625,-1.19));
#362035=CARTESIAN_POINT('',(3.85779730129493E-16,1.15470053837925,-1.19));
#362036=CARTESIAN_POINT('',(-0.999999999999999,-0.577350269189625,-1.19));
#362037=CARTESIAN_POINT('',(-0.999999999999999,0.577350269189625,-1.19));
#362038=CARTESIAN_POINT('',(-0.999999999999999,-0.577350269189625,-1.19));
#362039=CARTESIAN_POINT('Origin',(1.,-0.577350269189624,-1.19));
#362040=CARTESIAN_POINT('',(1.,-0.577350269189624,-1.19));
#362041=CARTESIAN_POINT('',(1.,0.577350269189626,-1.19));
#362042=CARTESIAN_POINT('Origin',(1.,0.577350269189626,-1.19));
#362043=CARTESIAN_POINT('',(3.85779730129493E-16,1.15470053837925,-1.19));
#362044=CARTESIAN_POINT('Origin',(3.85779730129493E-16,1.15470053837925,
-1.19));
#362045=CARTESIAN_POINT('',(-0.999999999999999,0.577350269189625,-1.19));
#362046=CARTESIAN_POINT('Origin',(-0.999999999999999,0.577350269189625,
-1.19));
#362047=CARTESIAN_POINT('',(-0.999999999999999,-0.577350269189625,-1.19));
#362048=CARTESIAN_POINT('Origin',(-0.999999999999999,-0.577350269189625,
-1.19));
#362049=CARTESIAN_POINT('',(1.9352544089507E-16,-1.15470053837925,-1.19));
#362050=CARTESIAN_POINT('Origin',(1.9352544089507E-16,-1.15470053837925,
-1.19));
#362051=CARTESIAN_POINT('Ctrl Pts',(0.,1.17524047358083,-17.95));
#362052=CARTESIAN_POINT('Ctrl Pts',(-0.678525403784434,1.17524047358083,
-17.9083333333333));
#362053=CARTESIAN_POINT('Ctrl Pts',(-1.01778810567665,0.58762023679042,
-17.8666666666667));
#362054=CARTESIAN_POINT('Ctrl Pts',(-1.35705080756887,6.21444700856507E-15,
-17.825));
#362055=CARTESIAN_POINT('Ctrl Pts',(-1.01778810567665,-0.587620236790408,
-17.7833333333333));
#362056=CARTESIAN_POINT('Ctrl Pts',(-0.678525403784435,-1.17524047358082,
-17.7416666666667));
#362057=CARTESIAN_POINT('Ctrl Pts',(-1.43925448419918E-16,-1.17524047358082,
-17.7));
#362058=CARTESIAN_POINT('Ctrl Pts',(0.678525403784434,-1.17524047358082,
-17.6583333333333));
#362059=CARTESIAN_POINT('Ctrl Pts',(1.01778810567665,-0.587620236790409,
-17.6166666666667));
#362060=CARTESIAN_POINT('Ctrl Pts',(1.35705080756887,5.77279150326459E-15,
-17.575));
#362061=CARTESIAN_POINT('Ctrl Pts',(1.01778810567665,0.587620236790419,
-17.5333333333333));
#362062=CARTESIAN_POINT('Ctrl Pts',(0.678525403784435,1.17524047358083,
-17.4916666666667));
#362063=CARTESIAN_POINT('Ctrl Pts',(0.,1.17524047358083,-17.45));
#362064=CARTESIAN_POINT('Ctrl Pts',(-0.678525403784434,1.17524047358083,
-17.4083333333333));
#362065=CARTESIAN_POINT('Ctrl Pts',(-1.01778810567665,0.58762023679042,
-17.3666666666667));
#362066=CARTESIAN_POINT('Ctrl Pts',(-1.35705080756887,5.99589916907193E-15,
-17.325));
#362067=CARTESIAN_POINT('Ctrl Pts',(-1.01778810567665,-0.587620236790408,
-17.2833333333333));
#362068=CARTESIAN_POINT('Ctrl Pts',(-0.678525403784435,-1.17524047358082,
-17.2416666666667));
#362069=CARTESIAN_POINT('Ctrl Pts',(-1.43925448419918E-16,-1.17524047358082,
-17.2));
#362070=CARTESIAN_POINT('Ctrl Pts',(0.678525403784434,-1.17524047358082,
-17.1583333333333));
#362071=CARTESIAN_POINT('Ctrl Pts',(1.01778810567665,-0.587620236790409,
-17.1166666666667));
#362072=CARTESIAN_POINT('Ctrl Pts',(1.35705080756887,5.55424366377145E-15,
-17.075));
#362073=CARTESIAN_POINT('Ctrl Pts',(1.01778810567665,0.587620236790419,
-17.0333333333333));
#362074=CARTESIAN_POINT('Ctrl Pts',(0.678525403784435,1.17524047358083,
-16.9916666666667));
#362075=CARTESIAN_POINT('Ctrl Pts',(0.,1.17524047358083,-16.95));
#362076=CARTESIAN_POINT('Ctrl Pts',(-0.678525403784434,1.17524047358083,
-16.9083333333333));
#362077=CARTESIAN_POINT('Ctrl Pts',(-1.01778810567665,0.58762023679042,
-16.8666666666667));
#362078=CARTESIAN_POINT('Ctrl Pts',(-1.35705080756887,5.77735132957879E-15,
-16.825));
#362079=CARTESIAN_POINT('Ctrl Pts',(-1.01778810567665,-0.587620236790408,
-16.7833333333333));
#362080=CARTESIAN_POINT('Ctrl Pts',(-0.678525403784435,-1.17524047358082,
-16.7416666666667));
#362081=CARTESIAN_POINT('Ctrl Pts',(-1.43925448419918E-16,-1.17524047358082,
-16.7));
#362082=CARTESIAN_POINT('Ctrl Pts',(0.678525403784434,-1.17524047358082,
-16.6583333333333));
#362083=CARTESIAN_POINT('Ctrl Pts',(1.01778810567665,-0.587620236790409,
-16.6166666666667));
#362084=CARTESIAN_POINT('Ctrl Pts',(1.35705080756887,5.33569582427831E-15,
-16.575));
#362085=CARTESIAN_POINT('Ctrl Pts',(1.01778810567665,0.587620236790419,
-16.5333333333333));
#362086=CARTESIAN_POINT('Ctrl Pts',(0.678525403784435,1.17524047358083,
-16.4916666666667));
#362087=CARTESIAN_POINT('Ctrl Pts',(0.,1.17524047358083,-16.45));
#362088=CARTESIAN_POINT('Ctrl Pts',(-0.678525403784434,1.17524047358083,
-16.4083333333333));
#362089=CARTESIAN_POINT('Ctrl Pts',(-1.01778810567665,0.58762023679042,
-16.3666666666667));
#362090=CARTESIAN_POINT('Ctrl Pts',(-1.35705080756887,5.55880349008565E-15,
-16.325));
#362091=CARTESIAN_POINT('Ctrl Pts',(-1.01778810567665,-0.587620236790408,
-16.2833333333333));
#362092=CARTESIAN_POINT('Ctrl Pts',(-0.678525403784435,-1.17524047358082,
-16.2416666666667));
#362093=CARTESIAN_POINT('Ctrl Pts',(-1.43925448419918E-16,-1.17524047358082,
-16.2));
#362094=CARTESIAN_POINT('Ctrl Pts',(0.678525403784434,-1.17524047358082,
-16.1583333333333));
#362095=CARTESIAN_POINT('Ctrl Pts',(1.01778810567665,-0.587620236790409,
-16.1166666666667));
#362096=CARTESIAN_POINT('Ctrl Pts',(1.35705080756887,5.11714798478517E-15,
-16.075));
#362097=CARTESIAN_POINT('Ctrl Pts',(1.01778810567665,0.587620236790419,
-16.0333333333333));
#362098=CARTESIAN_POINT('Ctrl Pts',(0.678525403784435,1.17524047358083,
-15.9916666666667));
#362099=CARTESIAN_POINT('Ctrl Pts',(0.,1.17524047358083,-15.95));
#362100=CARTESIAN_POINT('Ctrl Pts',(-0.678525403784434,1.17524047358083,
-15.9083333333333));
#362101=CARTESIAN_POINT('Ctrl Pts',(-1.01778810567665,0.58762023679042,
-15.8666666666667));
#362102=CARTESIAN_POINT('Ctrl Pts',(-1.35705080756887,5.34025565059251E-15,
-15.825));
#362103=CARTESIAN_POINT('Ctrl Pts',(-1.01778810567665,-0.587620236790409,
-15.7833333333333));
#362104=CARTESIAN_POINT('Ctrl Pts',(-0.678525403784435,-1.17524047358082,
-15.7416666666667));
#362105=CARTESIAN_POINT('Ctrl Pts',(-1.43925448419918E-16,-1.17524047358082,
-15.7));
#362106=CARTESIAN_POINT('Ctrl Pts',(0.678525403784434,-1.17524047358082,
-15.6583333333333));
#362107=CARTESIAN_POINT('Ctrl Pts',(1.01778810567665,-0.587620236790409,
-15.6166666666667));
#362108=CARTESIAN_POINT('Ctrl Pts',(1.35705080756887,4.89860014529203E-15,
-15.575));
#362109=CARTESIAN_POINT('Ctrl Pts',(1.01778810567665,0.587620236790418,
-15.5333333333333));
#362110=CARTESIAN_POINT('Ctrl Pts',(0.678525403784435,1.17524047358083,
-15.4916666666667));
#362111=CARTESIAN_POINT('Ctrl Pts',(0.,1.17524047358083,-15.45));
#362112=CARTESIAN_POINT('Ctrl Pts',(-0.678525403784434,1.17524047358083,
-15.4083333333333));
#362113=CARTESIAN_POINT('Ctrl Pts',(-1.01778810567665,0.587620236790419,
-15.3666666666667));
#362114=CARTESIAN_POINT('Ctrl Pts',(-1.35705080756887,5.12170781109936E-15,
-15.325));
#362115=CARTESIAN_POINT('Ctrl Pts',(-1.01778810567665,-0.587620236790409,
-15.2833333333333));
#362116=CARTESIAN_POINT('Ctrl Pts',(-0.678525403784435,-1.17524047358082,
-15.2416666666667));
#362117=CARTESIAN_POINT('Ctrl Pts',(-1.43925448419918E-16,-1.17524047358082,
-15.2));
#362118=CARTESIAN_POINT('Ctrl Pts',(0.678525403784434,-1.17524047358082,
-15.1583333333333));
#362119=CARTESIAN_POINT('Ctrl Pts',(1.01778810567665,-0.58762023679041,
-15.1166666666667));
#362120=CARTESIAN_POINT('Ctrl Pts',(1.35705080756887,4.68005230579889E-15,
-15.075));
#362121=CARTESIAN_POINT('Ctrl Pts',(1.01778810567665,0.587620236790418,
-15.0333333333333));
#362122=CARTESIAN_POINT('Ctrl Pts',(0.678525403784435,1.17524047358083,
-14.9916666666667));
#362123=CARTESIAN_POINT('Ctrl Pts',(0.,1.17524047358083,-14.95));
#362124=CARTESIAN_POINT('Ctrl Pts',(-0.678525403784434,1.17524047358083,
-14.9083333333333));
#362125=CARTESIAN_POINT('Ctrl Pts',(-1.01778810567665,0.587620236790419,
-14.8666666666667));
#362126=CARTESIAN_POINT('Ctrl Pts',(-1.35705080756887,4.90315997160622E-15,
-14.825));
#362127=CARTESIAN_POINT('Ctrl Pts',(-1.01778810567665,-0.587620236790409,
-14.7833333333333));
#362128=CARTESIAN_POINT('Ctrl Pts',(-0.678525403784435,-1.17524047358082,
-14.7416666666667));
#362129=CARTESIAN_POINT('Ctrl Pts',(-1.43925448419918E-16,-1.17524047358082,
-14.7));
#362130=CARTESIAN_POINT('Ctrl Pts',(0.678525403784434,-1.17524047358082,
-14.6583333333333));
#362131=CARTESIAN_POINT('Ctrl Pts',(1.01778810567665,-0.58762023679041,
-14.6166666666667));
#362132=CARTESIAN_POINT('Ctrl Pts',(1.35705080756887,4.46150446630575E-15,
-14.575));
#362133=CARTESIAN_POINT('Ctrl Pts',(1.01778810567665,0.587620236790418,
-14.5333333333333));
#362134=CARTESIAN_POINT('Ctrl Pts',(0.678525403784435,1.17524047358083,
-14.4916666666667));
#362135=CARTESIAN_POINT('Ctrl Pts',(0.,1.17524047358083,-14.45));
#362136=CARTESIAN_POINT('Ctrl Pts',(-0.678525403784434,1.17524047358083,
-14.4083333333333));
#362137=CARTESIAN_POINT('Ctrl Pts',(-1.01778810567665,0.587620236790419,
-14.3666666666667));
#362138=CARTESIAN_POINT('Ctrl Pts',(-1.35705080756887,4.68461213211308E-15,
-14.325));
#362139=CARTESIAN_POINT('Ctrl Pts',(-1.01778810567665,-0.587620236790409,
-14.2833333333333));
#362140=CARTESIAN_POINT('Ctrl Pts',(-0.678525403784435,-1.17524047358082,
-14.2416666666667));
#362141=CARTESIAN_POINT('Ctrl Pts',(-1.43925448419918E-16,-1.17524047358082,
-14.2));
#362142=CARTESIAN_POINT('Ctrl Pts',(0.678525403784434,-1.17524047358082,
-14.1583333333333));
#362143=CARTESIAN_POINT('Ctrl Pts',(1.01778810567665,-0.58762023679041,
-14.1166666666667));
#362144=CARTESIAN_POINT('Ctrl Pts',(1.35705080756887,4.2429566268126E-15,
-14.075));
#362145=CARTESIAN_POINT('Ctrl Pts',(1.01778810567665,0.587620236790418,
-14.0333333333333));
#362146=CARTESIAN_POINT('Ctrl Pts',(0.678525403784435,1.17524047358083,
-13.9916666666667));
#362147=CARTESIAN_POINT('Ctrl Pts',(0.,1.17524047358083,-13.95));
#362148=CARTESIAN_POINT('Ctrl Pts',(-0.678525403784434,1.17524047358083,
-13.9083333333333));
#362149=CARTESIAN_POINT('Ctrl Pts',(-1.01778810567665,0.587620236790419,
-13.8666666666667));
#362150=CARTESIAN_POINT('Ctrl Pts',(-1.35705080756887,4.46606429261994E-15,
-13.825));
#362151=CARTESIAN_POINT('Ctrl Pts',(-1.01778810567665,-0.58762023679041,
-13.7833333333333));
#362152=CARTESIAN_POINT('Ctrl Pts',(-0.678525403784435,-1.17524047358082,
-13.7416666666667));
#362153=CARTESIAN_POINT('Ctrl Pts',(-1.43925448419918E-16,-1.17524047358082,
-13.7));
#362154=CARTESIAN_POINT('Ctrl Pts',(0.678525403784434,-1.17524047358082,
-13.6583333333333));
#362155=CARTESIAN_POINT('Ctrl Pts',(1.01778810567665,-0.58762023679041,
-13.6166666666667));
#362156=CARTESIAN_POINT('Ctrl Pts',(1.35705080756887,4.02440878731946E-15,
-13.575));
#362157=CARTESIAN_POINT('Ctrl Pts',(1.01778810567665,0.587620236790417,
-13.5333333333333));
#362158=CARTESIAN_POINT('Ctrl Pts',(0.678525403784435,1.17524047358083,
-13.4916666666667));
#362159=CARTESIAN_POINT('Ctrl Pts',(0.,1.17524047358083,-13.45));
#362160=CARTESIAN_POINT('Ctrl Pts',(-0.678525403784434,1.17524047358083,
-13.4083333333333));
#362161=CARTESIAN_POINT('Ctrl Pts',(-1.01778810567665,0.587620236790418,
-13.3666666666667));
#362162=CARTESIAN_POINT('Ctrl Pts',(-1.35705080756887,4.2475164531268E-15,
-13.325));
#362163=CARTESIAN_POINT('Ctrl Pts',(-1.01778810567665,-0.58762023679041,
-13.2833333333333));
#362164=CARTESIAN_POINT('Ctrl Pts',(-0.678525403784435,-1.17524047358082,
-13.2416666666667));
#362165=CARTESIAN_POINT('Ctrl Pts',(-1.43925448419918E-16,-1.17524047358082,
-13.2));
#362166=CARTESIAN_POINT('Ctrl Pts',(0.678525403784434,-1.17524047358082,
-13.1583333333333));
#362167=CARTESIAN_POINT('Ctrl Pts',(1.01778810567665,-0.587620236790411,
-13.1166666666667));
#362168=CARTESIAN_POINT('Ctrl Pts',(1.35705080756887,3.80586094782632E-15,
-13.075));
#362169=CARTESIAN_POINT('Ctrl Pts',(1.01778810567665,0.587620236790417,
-13.0333333333333));
#362170=CARTESIAN_POINT('Ctrl Pts',(0.678525403784435,1.17524047358083,
-12.9916666666667));
#362171=CARTESIAN_POINT('Ctrl Pts',(0.,1.17524047358083,-12.95));
#362172=CARTESIAN_POINT('Ctrl Pts',(-0.678525403784434,1.17524047358083,
-12.9083333333333));
#362173=CARTESIAN_POINT('Ctrl Pts',(-1.01778810567665,0.587620236790418,
-12.8666666666667));
#362174=CARTESIAN_POINT('Ctrl Pts',(-1.35705080756887,4.02896861363366E-15,
-12.825));
#362175=CARTESIAN_POINT('Ctrl Pts',(-1.01778810567665,-0.58762023679041,
-12.7833333333333));
#362176=CARTESIAN_POINT('Ctrl Pts',(-0.678525403784435,-1.17524047358082,
-12.7416666666667));
#362177=CARTESIAN_POINT('Ctrl Pts',(-1.43925448419918E-16,-1.17524047358082,
-12.7));
#362178=CARTESIAN_POINT('Ctrl Pts',(0.678525403784434,-1.17524047358082,
-12.6583333333333));
#362179=CARTESIAN_POINT('Ctrl Pts',(1.01778810567665,-0.587620236790411,
-12.6166666666667));
#362180=CARTESIAN_POINT('Ctrl Pts',(1.35705080756887,3.58731310833318E-15,
-12.575));
#362181=CARTESIAN_POINT('Ctrl Pts',(1.01778810567665,0.587620236790417,
-12.5333333333333));
#362182=CARTESIAN_POINT('Ctrl Pts',(0.678525403784435,1.17524047358083,
-12.4916666666667));
#362183=CARTESIAN_POINT('Ctrl Pts',(0.,1.17524047358083,-12.45));
#362184=CARTESIAN_POINT('Ctrl Pts',(-0.678525403784434,1.17524047358083,
-12.4083333333333));
#362185=CARTESIAN_POINT('Ctrl Pts',(-1.01778810567665,0.587620236790418,
-12.3666666666667));
#362186=CARTESIAN_POINT('Ctrl Pts',(-1.35705080756887,3.81042077414052E-15,
-12.325));
#362187=CARTESIAN_POINT('Ctrl Pts',(-1.01778810567665,-0.58762023679041,
-12.2833333333333));
#362188=CARTESIAN_POINT('Ctrl Pts',(-0.678525403784435,-1.17524047358082,
-12.2416666666667));
#362189=CARTESIAN_POINT('Ctrl Pts',(-1.43925448419918E-16,-1.17524047358082,
-12.2));
#362190=CARTESIAN_POINT('Ctrl Pts',(0.678525403784434,-1.17524047358082,
-12.1583333333333));
#362191=CARTESIAN_POINT('Ctrl Pts',(1.01778810567665,-0.587620236790411,
-12.1166666666667));
#362192=CARTESIAN_POINT('Ctrl Pts',(1.35705080756887,3.36876526884004E-15,
-12.075));
#362193=CARTESIAN_POINT('Ctrl Pts',(1.01778810567665,0.587620236790417,
-12.0333333333333));
#362194=CARTESIAN_POINT('Ctrl Pts',(0.678525403784435,1.17524047358083,
-11.9916666666667));
#362195=CARTESIAN_POINT('Ctrl Pts',(0.,1.17524047358083,-11.95));
#362196=CARTESIAN_POINT('Ctrl Pts',(-0.678525403784434,1.17524047358083,
-11.9083333333333));
#362197=CARTESIAN_POINT('Ctrl Pts',(-1.01778810567665,0.587620236790418,
-11.8666666666667));
#362198=CARTESIAN_POINT('Ctrl Pts',(-1.35705080756887,3.59187293464738E-15,
-11.825));
#362199=CARTESIAN_POINT('Ctrl Pts',(-1.01778810567665,-0.58762023679041,
-11.7833333333333));
#362200=CARTESIAN_POINT('Ctrl Pts',(-0.678525403784435,-1.17524047358082,
-11.7416666666667));
#362201=CARTESIAN_POINT('Ctrl Pts',(-1.43925448419918E-16,-1.17524047358082,
-11.7));
#362202=CARTESIAN_POINT('Ctrl Pts',(0.678525403784434,-1.17524047358083,
-11.6583333333333));
#362203=CARTESIAN_POINT('Ctrl Pts',(1.01778810567665,-0.587620236790411,
-11.6166666666667));
#362204=CARTESIAN_POINT('Ctrl Pts',(1.35705080756887,3.1502174293469E-15,
-11.575));
#362205=CARTESIAN_POINT('Ctrl Pts',(1.01778810567665,0.587620236790417,
-11.5333333333333));
#362206=CARTESIAN_POINT('Ctrl Pts',(0.678525403784435,1.17524047358083,
-11.4916666666667));
#362207=CARTESIAN_POINT('Ctrl Pts',(0.,1.17524047358083,-11.45));
#362208=CARTESIAN_POINT('Ctrl Pts',(-0.678525403784434,1.17524047358083,
-11.4083333333333));
#362209=CARTESIAN_POINT('Ctrl Pts',(-1.01778810567665,0.587620236790417,
-11.3666666666667));
#362210=CARTESIAN_POINT('Ctrl Pts',(-1.35705080756887,3.37332509515423E-15,
-11.325));
#362211=CARTESIAN_POINT('Ctrl Pts',(-1.01778810567665,-0.587620236790411,
-11.2833333333333));
#362212=CARTESIAN_POINT('Ctrl Pts',(-0.678525403784435,-1.17524047358082,
-11.2416666666667));
#362213=CARTESIAN_POINT('Ctrl Pts',(-1.43925448419918E-16,-1.17524047358082,
-11.2));
#362214=CARTESIAN_POINT('Ctrl Pts',(0.678525403784434,-1.17524047358083,
-11.1583333333333));
#362215=CARTESIAN_POINT('Ctrl Pts',(1.01778810567665,-0.587620236790411,
-11.1166666666667));
#362216=CARTESIAN_POINT('Ctrl Pts',(1.35705080756887,2.93166958985376E-15,
-11.075));
#362217=CARTESIAN_POINT('Ctrl Pts',(1.01778810567665,0.587620236790416,
-11.0333333333333));
#362218=CARTESIAN_POINT('Ctrl Pts',(0.678525403784435,1.17524047358083,
-10.9916666666667));
#362219=CARTESIAN_POINT('Ctrl Pts',(0.,1.17524047358083,-10.95));
#362220=CARTESIAN_POINT('Ctrl Pts',(-0.678525403784434,1.17524047358083,
-10.9083333333333));
#362221=CARTESIAN_POINT('Ctrl Pts',(-1.01778810567665,0.587620236790417,
-10.8666666666667));
#362222=CARTESIAN_POINT('Ctrl Pts',(-1.35705080756887,3.15477725566109E-15,
-10.825));
#362223=CARTESIAN_POINT('Ctrl Pts',(-1.01778810567665,-0.587620236790411,
-10.7833333333333));
#362224=CARTESIAN_POINT('Ctrl Pts',(-0.678525403784435,-1.17524047358083,
-10.7416666666667));
#362225=CARTESIAN_POINT('Ctrl Pts',(-1.43925448419918E-16,-1.17524047358083,
-10.7));
#362226=CARTESIAN_POINT('Ctrl Pts',(0.678525403784434,-1.17524047358083,
-10.6583333333333));
#362227=CARTESIAN_POINT('Ctrl Pts',(1.01778810567665,-0.587620236790412,
-10.6166666666667));
#362228=CARTESIAN_POINT('Ctrl Pts',(1.35705080756887,2.71312175036062E-15,
-10.575));
#362229=CARTESIAN_POINT('Ctrl Pts',(1.01778810567665,0.587620236790416,
-10.5333333333333));
#362230=CARTESIAN_POINT('Ctrl Pts',(0.678525403784435,1.17524047358083,
-10.4916666666667));
#362231=CARTESIAN_POINT('Ctrl Pts',(0.,1.17524047358083,-10.45));
#362232=CARTESIAN_POINT('Ctrl Pts',(-0.678525403784434,1.17524047358083,
-10.4083333333333));
#362233=CARTESIAN_POINT('Ctrl Pts',(-1.01778810567665,0.587620236790417,
-10.3666666666667));
#362234=CARTESIAN_POINT('Ctrl Pts',(-1.35705080756887,2.93622941616795E-15,
-10.325));
#362235=CARTESIAN_POINT('Ctrl Pts',(-1.01778810567665,-0.587620236790411,
-10.2833333333333));
#362236=CARTESIAN_POINT('Ctrl Pts',(-0.678525403784435,-1.17524047358083,
-10.2416666666667));
#362237=CARTESIAN_POINT('Ctrl Pts',(-1.43925448419918E-16,-1.17524047358083,
-10.2));
#362238=CARTESIAN_POINT('Ctrl Pts',(0.678525403784434,-1.17524047358083,
-10.1583333333333));
#362239=CARTESIAN_POINT('Ctrl Pts',(1.01778810567665,-0.587620236790412,
-10.1166666666667));
#362240=CARTESIAN_POINT('Ctrl Pts',(1.35705080756887,2.49457391086747E-15,
-10.075));
#362241=CARTESIAN_POINT('Ctrl Pts',(1.01778810567665,0.587620236790416,
-10.0333333333333));
#362242=CARTESIAN_POINT('Ctrl Pts',(0.678525403784435,1.17524047358083,
-9.99166666666667));
#362243=CARTESIAN_POINT('Ctrl Pts',(0.,1.17524047358083,-9.95));
#362244=CARTESIAN_POINT('Ctrl Pts',(-0.678525403784434,1.17524047358083,
-9.90833333333333));
#362245=CARTESIAN_POINT('Ctrl Pts',(-1.01778810567665,0.587620236790417,
-9.86666666666667));
#362246=CARTESIAN_POINT('Ctrl Pts',(-1.35705080756887,2.71768157667481E-15,
-9.825));
#362247=CARTESIAN_POINT('Ctrl Pts',(-1.01778810567665,-0.587620236790411,
-9.78333333333333));
#362248=CARTESIAN_POINT('Ctrl Pts',(-0.678525403784435,-1.17524047358083,
-9.74166666666667));
#362249=CARTESIAN_POINT('Ctrl Pts',(-1.43925448419918E-16,-1.17524047358083,
-9.7));
#362250=CARTESIAN_POINT('Ctrl Pts',(0.678525403784434,-1.17524047358083,
-9.65833333333333));
#362251=CARTESIAN_POINT('Ctrl Pts',(1.01778810567665,-0.587620236790412,
-9.61666666666667));
#362252=CARTESIAN_POINT('Ctrl Pts',(1.35705080756887,2.27602607137433E-15,
-9.575));
#362253=CARTESIAN_POINT('Ctrl Pts',(1.01778810567665,0.587620236790416,
-9.53333333333333));
#362254=CARTESIAN_POINT('Ctrl Pts',(0.678525403784435,1.17524047358083,
-9.49166666666667));
#362255=CARTESIAN_POINT('Ctrl Pts',(0.,1.17524047358083,-9.45));
#362256=CARTESIAN_POINT('Ctrl Pts',(-0.678525403784434,1.17524047358083,
-9.40833333333333));
#362257=CARTESIAN_POINT('Ctrl Pts',(-1.01778810567665,0.587620236790417,
-9.36666666666667));
#362258=CARTESIAN_POINT('Ctrl Pts',(-1.35705080756887,2.49913373718167E-15,
-9.325));
#362259=CARTESIAN_POINT('Ctrl Pts',(-1.01778810567665,-0.587620236790411,
-9.28333333333333));
#362260=CARTESIAN_POINT('Ctrl Pts',(-0.678525403784435,-1.17524047358083,
-9.24166666666667));
#362261=CARTESIAN_POINT('Ctrl Pts',(-1.43925448419918E-16,-1.17524047358083,
-9.2));
#362262=CARTESIAN_POINT('Ctrl Pts',(0.678525403784434,-1.17524047358083,
-9.15833333333333));
#362263=CARTESIAN_POINT('Ctrl Pts',(1.01778810567665,-0.587620236790412,
-9.11666666666667));
#362264=CARTESIAN_POINT('Ctrl Pts',(1.35705080756887,2.05747823188119E-15,
-9.075));
#362265=CARTESIAN_POINT('Ctrl Pts',(1.01778810567665,0.587620236790415,
-9.03333333333333));
#362266=CARTESIAN_POINT('Ctrl Pts',(0.678525403784435,1.17524047358083,
-8.99166666666667));
#362267=CARTESIAN_POINT('Ctrl Pts',(0.,1.17524047358083,-8.95));
#362268=CARTESIAN_POINT('Ctrl Pts',(-0.678525403784434,1.17524047358083,
-8.90833333333333));
#362269=CARTESIAN_POINT('Ctrl Pts',(-1.01778810567665,0.587620236790416,
-8.86666666666667));
#362270=CARTESIAN_POINT('Ctrl Pts',(-1.35705080756887,2.28058589768853E-15,
-8.825));
#362271=CARTESIAN_POINT('Ctrl Pts',(-1.01778810567665,-0.587620236790412,
-8.78333333333333));
#362272=CARTESIAN_POINT('Ctrl Pts',(-0.678525403784435,-1.17524047358083,
-8.74166666666667));
#362273=CARTESIAN_POINT('Ctrl Pts',(-1.43925448419918E-16,-1.17524047358083,
-8.7));
#362274=CARTESIAN_POINT('Ctrl Pts',(0.678525403784434,-1.17524047358083,
-8.65833333333333));
#362275=CARTESIAN_POINT('Ctrl Pts',(1.01778810567665,-0.587620236790413,
-8.61666666666667));
#362276=CARTESIAN_POINT('Ctrl Pts',(1.35705080756887,1.83893039238805E-15,
-8.575));
#362277=CARTESIAN_POINT('Ctrl Pts',(1.01778810567665,0.587620236790415,
-8.53333333333333));
#362278=CARTESIAN_POINT('Ctrl Pts',(0.678525403784435,1.17524047358083,
-8.49166666666667));
#362279=CARTESIAN_POINT('Ctrl Pts',(0.,1.17524047358083,-8.45));
#362280=CARTESIAN_POINT('Ctrl Pts',(-0.678525403784434,1.17524047358083,
-8.40833333333333));
#362281=CARTESIAN_POINT('Ctrl Pts',(-1.01778810567665,0.587620236790416,
-8.36666666666667));
#362282=CARTESIAN_POINT('Ctrl Pts',(-1.35705080756887,2.06203805819539E-15,
-8.325));
#362283=CARTESIAN_POINT('Ctrl Pts',(-1.01778810567665,-0.587620236790412,
-8.28333333333333));
#362284=CARTESIAN_POINT('Ctrl Pts',(-0.678525403784435,-1.17524047358083,
-8.24166666666667));
#362285=CARTESIAN_POINT('Ctrl Pts',(-1.43925448419918E-16,-1.17524047358083,
-8.2));
#362286=CARTESIAN_POINT('Ctrl Pts',(0.678525403784434,-1.17524047358083,
-8.15833333333333));
#362287=CARTESIAN_POINT('Ctrl Pts',(1.01778810567665,-0.587620236790413,
-8.11666666666667));
#362288=CARTESIAN_POINT('Ctrl Pts',(1.35705080756887,1.62038255289491E-15,
-8.075));
#362289=CARTESIAN_POINT('Ctrl Pts',(1.01778810567665,0.587620236790415,
-8.03333333333333));
#362290=CARTESIAN_POINT('Ctrl Pts',(0.678525403784435,1.17524047358083,
-7.99166666666667));
#362291=CARTESIAN_POINT('Ctrl Pts',(0.,1.17524047358083,-7.95));
#362292=CARTESIAN_POINT('Ctrl Pts',(-0.678525403784434,1.17524047358083,
-7.90833333333333));
#362293=CARTESIAN_POINT('Ctrl Pts',(-1.01778810567665,0.587620236790416,
-7.86666666666667));
#362294=CARTESIAN_POINT('Ctrl Pts',(-1.35705080756887,1.84349021870225E-15,
-7.825));
#362295=CARTESIAN_POINT('Ctrl Pts',(-1.01778810567665,-0.587620236790412,
-7.78333333333333));
#362296=CARTESIAN_POINT('Ctrl Pts',(-0.678525403784435,-1.17524047358083,
-7.74166666666667));
#362297=CARTESIAN_POINT('Ctrl Pts',(-1.43925448419918E-16,-1.17524047358083,
-7.7));
#362298=CARTESIAN_POINT('Ctrl Pts',(0.678525403784434,-1.17524047358083,
-7.65833333333334));
#362299=CARTESIAN_POINT('Ctrl Pts',(1.01778810567665,-0.587620236790413,
-7.61666666666667));
#362300=CARTESIAN_POINT('Ctrl Pts',(1.35705080756887,1.40183471340177E-15,
-7.575));
#362301=CARTESIAN_POINT('Ctrl Pts',(1.01778810567665,0.587620236790415,
-7.53333333333333));
#362302=CARTESIAN_POINT('Ctrl Pts',(0.678525403784435,1.17524047358083,
-7.49166666666667));
#362303=CARTESIAN_POINT('Ctrl Pts',(0.,1.17524047358083,-7.45));
#362304=CARTESIAN_POINT('Ctrl Pts',(-0.678525403784434,1.17524047358083,
-7.40833333333333));
#362305=CARTESIAN_POINT('Ctrl Pts',(-1.01778810567665,0.587620236790416,
-7.36666666666667));
#362306=CARTESIAN_POINT('Ctrl Pts',(-1.35705080756887,1.62494237920911E-15,
-7.325));
#362307=CARTESIAN_POINT('Ctrl Pts',(-1.01778810567665,-0.587620236790412,
-7.28333333333333));
#362308=CARTESIAN_POINT('Ctrl Pts',(-0.678525403784435,-1.17524047358083,
-7.24166666666667));
#362309=CARTESIAN_POINT('Ctrl Pts',(-1.43925448419918E-16,-1.17524047358083,
-7.2));
#362310=CARTESIAN_POINT('Ctrl Pts',(0.678525403784434,-1.17524047358083,
-7.15833333333333));
#362311=CARTESIAN_POINT('Ctrl Pts',(1.01778810567665,-0.587620236790413,
-7.11666666666667));
#362312=CARTESIAN_POINT('Ctrl Pts',(1.35705080756887,1.18328687390863E-15,
-7.075));
#362313=CARTESIAN_POINT('Ctrl Pts',(1.01778810567665,0.587620236790415,
-7.03333333333333));
#362314=CARTESIAN_POINT('Ctrl Pts',(0.678525403784435,1.17524047358083,
-6.99166666666667));
#362315=CARTESIAN_POINT('Ctrl Pts',(0.,1.17524047358083,-6.95));
#362316=CARTESIAN_POINT('Ctrl Pts',(-0.678525403784434,1.17524047358083,
-6.90833333333333));
#362317=CARTESIAN_POINT('Ctrl Pts',(-1.01778810567665,0.587620236790415,
-6.86666666666667));
#362318=CARTESIAN_POINT('Ctrl Pts',(-1.35705080756887,1.40639453971596E-15,
-6.825));
#362319=CARTESIAN_POINT('Ctrl Pts',(-1.01778810567665,-0.587620236790413,
-6.78333333333333));
#362320=CARTESIAN_POINT('Ctrl Pts',(-0.678525403784435,-1.17524047358083,
-6.74166666666667));
#362321=CARTESIAN_POINT('Ctrl Pts',(-1.43925448419918E-16,-1.17524047358083,
-6.7));
#362322=CARTESIAN_POINT('Ctrl Pts',(0.678525403784434,-1.17524047358083,
-6.65833333333333));
#362323=CARTESIAN_POINT('Ctrl Pts',(1.01778810567665,-0.587620236790414,
-6.61666666666667));
#362324=CARTESIAN_POINT('Ctrl Pts',(1.35705080756887,9.64739034415485E-16,
-6.575));
#362325=CARTESIAN_POINT('Ctrl Pts',(1.01778810567665,0.587620236790414,
-6.53333333333333));
#362326=CARTESIAN_POINT('Ctrl Pts',(0.678525403784435,1.17524047358083,
-6.49166666666667));
#362327=CARTESIAN_POINT('Ctrl Pts',(0.,1.17524047358083,-6.45));
#362328=CARTESIAN_POINT('Ctrl Pts',(-0.678525403784434,1.17524047358083,
-6.40833333333334));
#362329=CARTESIAN_POINT('Ctrl Pts',(-1.01778810567665,0.587620236790415,
-6.36666666666667));
#362330=CARTESIAN_POINT('Ctrl Pts',(-1.35705080756887,1.18784670022282E-15,
-6.325));
#362331=CARTESIAN_POINT('Ctrl Pts',(-1.01778810567665,-0.587620236790413,
-6.28333333333333));
#362332=CARTESIAN_POINT('Ctrl Pts',(-0.678525403784435,-1.17524047358083,
-6.24166666666667));
#362333=CARTESIAN_POINT('Ctrl Pts',(-1.43925448419918E-16,-1.17524047358083,
-6.2));
#362334=CARTESIAN_POINT('Ctrl Pts',(0.678525403784434,-1.17524047358083,
-6.15833333333333));
#362335=CARTESIAN_POINT('Ctrl Pts',(1.01778810567665,-0.587620236790414,
-6.11666666666667));
#362336=CARTESIAN_POINT('Ctrl Pts',(1.35705080756887,7.46191194922343E-16,
-6.075));
#362337=CARTESIAN_POINT('Ctrl Pts',(1.01778810567665,0.587620236790414,
-6.03333333333333));
#362338=CARTESIAN_POINT('Ctrl Pts',(0.678525403784435,1.17524047358083,
-5.99166666666667));
#362339=CARTESIAN_POINT('Ctrl Pts',(0.,1.17524047358083,-5.95));
#362340=CARTESIAN_POINT('Ctrl Pts',(-0.678525403784434,1.17524047358083,
-5.90833333333333));
#362341=CARTESIAN_POINT('Ctrl Pts',(-1.01778810567665,0.587620236790415,
-5.86666666666667));
#362342=CARTESIAN_POINT('Ctrl Pts',(-1.35705080756887,9.69298860729681E-16,
-5.825));
#362343=CARTESIAN_POINT('Ctrl Pts',(-1.01778810567665,-0.587620236790413,
-5.78333333333333));
#362344=CARTESIAN_POINT('Ctrl Pts',(-0.678525403784435,-1.17524047358083,
-5.74166666666667));
#362345=CARTESIAN_POINT('Ctrl Pts',(-1.43925448419918E-16,-1.17524047358083,
-5.7));
#362346=CARTESIAN_POINT('Ctrl Pts',(0.678525403784434,-1.17524047358083,
-5.65833333333333));
#362347=CARTESIAN_POINT('Ctrl Pts',(1.01778810567665,-0.587620236790414,
-5.61666666666667));
#362348=CARTESIAN_POINT('Ctrl Pts',(1.35705080756887,5.27643355429203E-16,
-5.575));
#362349=CARTESIAN_POINT('Ctrl Pts',(1.01778810567665,0.587620236790414,
-5.53333333333334));
#362350=CARTESIAN_POINT('Ctrl Pts',(0.678525403784435,1.17524047358083,
-5.49166666666667));
#362351=CARTESIAN_POINT('Ctrl Pts',(0.,1.17524047358083,-5.45));
#362352=CARTESIAN_POINT('Ctrl Pts',(-0.678525403784434,1.17524047358083,
-5.40833333333333));
#362353=CARTESIAN_POINT('Ctrl Pts',(-1.01778810567665,0.587620236790415,
-5.36666666666667));
#362354=CARTESIAN_POINT('Ctrl Pts',(-1.35705080756887,7.50751021236542E-16,
-5.325));
#362355=CARTESIAN_POINT('Ctrl Pts',(-1.01778810567665,-0.587620236790413,
-5.28333333333333));
#362356=CARTESIAN_POINT('Ctrl Pts',(-0.678525403784435,-1.17524047358083,
-5.24166666666667));
#362357=CARTESIAN_POINT('Ctrl Pts',(-1.43925448419918E-16,-1.17524047358083,
-5.2));
#362358=CARTESIAN_POINT('Ctrl Pts',(0.678525403784434,-1.17524047358083,
-5.15833333333333));
#362359=CARTESIAN_POINT('Ctrl Pts',(1.01778810567665,-0.587620236790414,
-5.11666666666667));
#362360=CARTESIAN_POINT('Ctrl Pts',(1.35705080756887,3.09095515936061E-16,
-5.075));
#362361=CARTESIAN_POINT('Ctrl Pts',(1.01778810567665,0.587620236790414,
-5.03333333333333));
#362362=CARTESIAN_POINT('Ctrl Pts',(0.678525403784435,1.17524047358083,
-4.99166666666667));
#362363=CARTESIAN_POINT('Ctrl Pts',(0.,1.17524047358083,-4.95));
#362364=CARTESIAN_POINT('Ctrl Pts',(-0.678525403784434,1.17524047358083,
-4.90833333333333));
#362365=CARTESIAN_POINT('Ctrl Pts',(-1.01778810567665,0.587620236790415,
-4.86666666666667));
#362366=CARTESIAN_POINT('Ctrl Pts',(-1.35705080756887,5.322031817434E-16,
-4.825));
#362367=CARTESIAN_POINT('Ctrl Pts',(-1.01778810567665,-0.587620236790414,
-4.78333333333333));
#362368=CARTESIAN_POINT('Ctrl Pts',(-0.678525403784435,-1.17524047358083,
-4.74166666666667));
#362369=CARTESIAN_POINT('Ctrl Pts',(-1.43925448419918E-16,-1.17524047358083,
-4.7));
#362370=CARTESIAN_POINT('Ctrl Pts',(0.678525403784434,-1.17524047358083,
-4.65833333333333));
#362371=CARTESIAN_POINT('Ctrl Pts',(1.01778810567665,-0.587620236790414,
-4.61666666666667));
#362372=CARTESIAN_POINT('Ctrl Pts',(1.35705080756887,9.05476764429197E-17,
-4.575));
#362373=CARTESIAN_POINT('Ctrl Pts',(1.01778810567665,0.587620236790414,
-4.53333333333333));
#362374=CARTESIAN_POINT('Ctrl Pts',(0.678525403784435,1.17524047358083,
-4.49166666666667));
#362375=CARTESIAN_POINT('Ctrl Pts',(0.,1.17524047358083,-4.45));
#362376=CARTESIAN_POINT('Ctrl Pts',(-0.678525403784434,1.17524047358083,
-4.40833333333334));
#362377=CARTESIAN_POINT('Ctrl Pts',(-1.01778810567665,0.587620236790414,
-4.36666666666667));
#362378=CARTESIAN_POINT('Ctrl Pts',(-1.35705080756887,3.13655342250259E-16,
-4.325));
#362379=CARTESIAN_POINT('Ctrl Pts',(-1.01778810567665,-0.587620236790414,
-4.28333333333333));
#362380=CARTESIAN_POINT('Ctrl Pts',(-0.678525403784435,-1.17524047358083,
-4.24166666666667));
#362381=CARTESIAN_POINT('Ctrl Pts',(-1.43925448419918E-16,-1.17524047358083,
-4.2));
#362382=CARTESIAN_POINT('Ctrl Pts',(0.678525403784434,-1.17524047358083,
-4.15833333333334));
#362383=CARTESIAN_POINT('Ctrl Pts',(1.01778810567665,-0.587620236790415,
-4.11666666666667));
#362384=CARTESIAN_POINT('Ctrl Pts',(1.35705080756887,-1.28000163050222E-16,
-4.075));
#362385=CARTESIAN_POINT('Ctrl Pts',(1.01778810567665,0.587620236790413,
-4.03333333333333));
#362386=CARTESIAN_POINT('Ctrl Pts',(0.678525403784435,1.17524047358083,
-3.99166666666667));
#362387=CARTESIAN_POINT('Ctrl Pts',(0.,1.17524047358083,-3.95));
#362388=CARTESIAN_POINT('Ctrl Pts',(-0.678525403784434,1.17524047358083,
-3.90833333333334));
#362389=CARTESIAN_POINT('Ctrl Pts',(-1.01778810567665,0.587620236790414,
-3.86666666666667));
#362390=CARTESIAN_POINT('Ctrl Pts',(-1.35705080756887,9.5107502757118E-17,
-3.825));
#362391=CARTESIAN_POINT('Ctrl Pts',(-1.01778810567665,-0.587620236790414,
-3.78333333333333));
#362392=CARTESIAN_POINT('Ctrl Pts',(-0.678525403784435,-1.17524047358083,
-3.74166666666667));
#362393=CARTESIAN_POINT('Ctrl Pts',(-1.43925448419918E-16,-1.17524047358083,
-3.7));
#362394=CARTESIAN_POINT('Ctrl Pts',(0.678525403784434,-1.17524047358083,
-3.65833333333333));
#362395=CARTESIAN_POINT('Ctrl Pts',(1.01778810567665,-0.587620236790415,
-3.61666666666667));
#362396=CARTESIAN_POINT('Ctrl Pts',(1.35705080756887,-3.46548002543362E-16,
-3.575));
#362397=CARTESIAN_POINT('Ctrl Pts',(1.01778810567665,0.587620236790413,
-3.53333333333333));
#362398=CARTESIAN_POINT('Ctrl Pts',(0.678525403784435,1.17524047358083,
-3.49166666666667));
#362399=CARTESIAN_POINT('Ctrl Pts',(0.,1.17524047358083,-3.45));
#362400=CARTESIAN_POINT('Ctrl Pts',(-0.678525403784434,1.17524047358083,
-3.40833333333333));
#362401=CARTESIAN_POINT('Ctrl Pts',(-1.01778810567665,0.587620236790414,
-3.36666666666667));
#362402=CARTESIAN_POINT('Ctrl Pts',(-1.35705080756887,-1.23440336736023E-16,
-3.325));
#362403=CARTESIAN_POINT('Ctrl Pts',(-1.01778810567665,-0.587620236790414,
-3.28333333333333));
#362404=CARTESIAN_POINT('Ctrl Pts',(-0.678525403784435,-1.17524047358083,
-3.24166666666667));
#362405=CARTESIAN_POINT('Ctrl Pts',(-1.43925448419918E-16,-1.17524047358083,
-3.2));
#362406=CARTESIAN_POINT('Ctrl Pts',(0.678525403784434,-1.17524047358083,
-3.15833333333333));
#362407=CARTESIAN_POINT('Ctrl Pts',(1.01778810567665,-0.587620236790415,
-3.11666666666667));
#362408=CARTESIAN_POINT('Ctrl Pts',(1.35705080756887,-5.65095842036504E-16,
-3.075));
#362409=CARTESIAN_POINT('Ctrl Pts',(1.01778810567665,0.587620236790413,
-3.03333333333333));
#362410=CARTESIAN_POINT('Ctrl Pts',(0.678525403784435,1.17524047358083,
-2.99166666666667));
#362411=CARTESIAN_POINT('Ctrl Pts',(0.,1.17524047358083,-2.95));
#362412=CARTESIAN_POINT('Ctrl Pts',(-0.678525403784434,1.17524047358083,
-2.90833333333333));
#362413=CARTESIAN_POINT('Ctrl Pts',(-1.01778810567665,0.587620236790414,
-2.86666666666667));
#362414=CARTESIAN_POINT('Ctrl Pts',(-1.35705080756887,-3.41988176229165E-16,
-2.825));
#362415=CARTESIAN_POINT('Ctrl Pts',(-1.01778810567665,-0.587620236790414,
-2.78333333333333));
#362416=CARTESIAN_POINT('Ctrl Pts',(-0.678525403784435,-1.17524047358083,
-2.74166666666667));
#362417=CARTESIAN_POINT('Ctrl Pts',(-1.43925448419918E-16,-1.17524047358083,
-2.7));
#362418=CARTESIAN_POINT('Ctrl Pts',(0.678525403784434,-1.17524047358083,
-2.65833333333333));
#362419=CARTESIAN_POINT('Ctrl Pts',(1.01778810567665,-0.587620236790415,
-2.61666666666667));
#362420=CARTESIAN_POINT('Ctrl Pts',(1.35705080756887,-7.83643681529645E-16,
-2.575));
#362421=CARTESIAN_POINT('Ctrl Pts',(1.01778810567665,0.587620236790413,
-2.53333333333334));
#362422=CARTESIAN_POINT('Ctrl Pts',(0.678525403784435,1.17524047358083,
-2.49166666666667));
#362423=CARTESIAN_POINT('Ctrl Pts',(0.,1.17524047358083,-2.45));
#362424=CARTESIAN_POINT('Ctrl Pts',(-0.678525403784434,1.17524047358083,
-2.40833333333334));
#362425=CARTESIAN_POINT('Ctrl Pts',(-1.01778810567665,0.587620236790414,
-2.36666666666667));
#362426=CARTESIAN_POINT('Ctrl Pts',(-1.35705080756887,-5.60536015722306E-16,
-2.325));
#362427=CARTESIAN_POINT('Ctrl Pts',(-1.01778810567665,-0.587620236790415,
-2.28333333333333));
#362428=CARTESIAN_POINT('Ctrl Pts',(-0.678525403784435,-1.17524047358083,
-2.24166666666667));
#362429=CARTESIAN_POINT('Ctrl Pts',(-1.43925448419918E-16,-1.17524047358083,
-2.2));
#362430=CARTESIAN_POINT('Ctrl Pts',(0.678525403784434,-1.17524047358083,
-2.15833333333333));
#362431=CARTESIAN_POINT('Ctrl Pts',(1.01778810567665,-0.587620236790415,
-2.11666666666667));
#362432=CARTESIAN_POINT('Ctrl Pts',(1.35705080756887,-1.00219152102279E-15,
-2.075));
#362433=CARTESIAN_POINT('Ctrl Pts',(1.01778810567665,0.587620236790412,
-2.03333333333333));
#362434=CARTESIAN_POINT('Ctrl Pts',(0.678525403784435,1.17524047358083,
-1.99166666666667));
#362435=CARTESIAN_POINT('Ctrl Pts',(0.,1.17524047358083,-1.95));
#362436=CARTESIAN_POINT('Ctrl Pts',(-0.678525403784434,1.17524047358083,
-1.90833333333333));
#362437=CARTESIAN_POINT('Ctrl Pts',(-1.01778810567665,0.587620236790413,
-1.86666666666667));
#362438=CARTESIAN_POINT('Ctrl Pts',(-1.35705080756887,-7.79083855215448E-16,
-1.825));
#362439=CARTESIAN_POINT('Ctrl Pts',(-1.01778810567665,-0.587620236790415,
-1.78333333333333));
#362440=CARTESIAN_POINT('Ctrl Pts',(-0.678525403784435,-1.17524047358083,
-1.74166666666667));
#362441=CARTESIAN_POINT('Ctrl Pts',(-1.43925448419918E-16,-1.17524047358083,
-1.7));
#362442=CARTESIAN_POINT('Ctrl Pts',(0.678525403784434,-1.17524047358083,
-1.65833333333333));
#362443=CARTESIAN_POINT('Ctrl Pts',(1.01778810567665,-0.587620236790416,
-1.61666666666667));
#362444=CARTESIAN_POINT('Ctrl Pts',(1.35705080756887,-1.22073936051593E-15,
-1.575));
#362445=CARTESIAN_POINT('Ctrl Pts',(1.01778810567665,0.587620236790412,
-1.53333333333333));
#362446=CARTESIAN_POINT('Ctrl Pts',(0.678525403784435,1.17524047358083,
-1.49166666666667));
#362447=CARTESIAN_POINT('Ctrl Pts',(0.,1.17524047358083,-1.45));
#362448=CARTESIAN_POINT('Ctrl Pts',(0.,1.5,-18.1375));
#362449=CARTESIAN_POINT('Ctrl Pts',(-0.866025403784436,1.5,-18.0958333333333));
#362450=CARTESIAN_POINT('Ctrl Pts',(-1.29903810567665,0.750000000000004,
-18.0541666666667));
#362451=CARTESIAN_POINT('Ctrl Pts',(-1.73205080756887,6.31936457585901E-15,
-18.0125));
#362452=CARTESIAN_POINT('Ctrl Pts',(-1.29903810567665,-0.749999999999991,
-17.9708333333333));
#362453=CARTESIAN_POINT('Ctrl Pts',(-0.866025403784437,-1.49999999999999,
-17.9291666666667));
#362454=CARTESIAN_POINT('Ctrl Pts',(-1.83697019872102E-16,-1.49999999999999,
-17.8875));
#362455=CARTESIAN_POINT('Ctrl Pts',(0.866025403784436,-1.49999999999999,
-17.8458333333333));
#362456=CARTESIAN_POINT('Ctrl Pts',(1.29903810567665,-0.749999999999992,
-17.8041666666667));
#362457=CARTESIAN_POINT('Ctrl Pts',(1.73205080756887,5.78586056062248E-15,
-17.7625));
#362458=CARTESIAN_POINT('Ctrl Pts',(1.29903810567665,0.750000000000003,
-17.7208333333333));
#362459=CARTESIAN_POINT('Ctrl Pts',(0.866025403784437,1.5,-17.6791666666667));
#362460=CARTESIAN_POINT('Ctrl Pts',(0.,1.5,-17.6375));
#362461=CARTESIAN_POINT('Ctrl Pts',(-0.866025403784436,1.5,-17.5958333333333));
#362462=CARTESIAN_POINT('Ctrl Pts',(-1.29903810567665,0.750000000000004,
-17.5541666666667));
#362463=CARTESIAN_POINT('Ctrl Pts',(-1.73205080756887,6.10081673636587E-15,
-17.5125));
#362464=CARTESIAN_POINT('Ctrl Pts',(-1.29903810567665,-0.749999999999992,
-17.4708333333333));
#362465=CARTESIAN_POINT('Ctrl Pts',(-0.866025403784437,-1.49999999999999,
-17.4291666666667));
#362466=CARTESIAN_POINT('Ctrl Pts',(-1.83697019872102E-16,-1.49999999999999,
-17.3875));
#362467=CARTESIAN_POINT('Ctrl Pts',(0.866025403784436,-1.49999999999999,
-17.3458333333333));
#362468=CARTESIAN_POINT('Ctrl Pts',(1.29903810567665,-0.749999999999992,
-17.3041666666667));
#362469=CARTESIAN_POINT('Ctrl Pts',(1.73205080756887,5.56731272112934E-15,
-17.2625));
#362470=CARTESIAN_POINT('Ctrl Pts',(1.29903810567665,0.750000000000003,
-17.2208333333333));
#362471=CARTESIAN_POINT('Ctrl Pts',(0.866025403784437,1.5,-17.1791666666667));
#362472=CARTESIAN_POINT('Ctrl Pts',(0.,1.5,-17.1375));
#362473=CARTESIAN_POINT('Ctrl Pts',(-0.866025403784436,1.5,-17.0958333333333));
#362474=CARTESIAN_POINT('Ctrl Pts',(-1.29903810567665,0.750000000000004,
-17.0541666666667));
#362475=CARTESIAN_POINT('Ctrl Pts',(-1.73205080756887,5.88226889687273E-15,
-17.0125));
#362476=CARTESIAN_POINT('Ctrl Pts',(-1.29903810567665,-0.749999999999992,
-16.9708333333333));
#362477=CARTESIAN_POINT('Ctrl Pts',(-0.866025403784437,-1.49999999999999,
-16.9291666666667));
#362478=CARTESIAN_POINT('Ctrl Pts',(-1.83697019872102E-16,-1.49999999999999,
-16.8875));
#362479=CARTESIAN_POINT('Ctrl Pts',(0.866025403784436,-1.49999999999999,
-16.8458333333333));
#362480=CARTESIAN_POINT('Ctrl Pts',(1.29903810567665,-0.749999999999993,
-16.8041666666667));
#362481=CARTESIAN_POINT('Ctrl Pts',(1.73205080756887,5.3487648816362E-15,
-16.7625));
#362482=CARTESIAN_POINT('Ctrl Pts',(1.29903810567665,0.750000000000002,
-16.7208333333333));
#362483=CARTESIAN_POINT('Ctrl Pts',(0.866025403784437,1.5,-16.6791666666667));
#362484=CARTESIAN_POINT('Ctrl Pts',(0.,1.5,-16.6375));
#362485=CARTESIAN_POINT('Ctrl Pts',(-0.866025403784436,1.5,-16.5958333333333));
#362486=CARTESIAN_POINT('Ctrl Pts',(-1.29903810567665,0.750000000000004,
-16.5541666666667));
#362487=CARTESIAN_POINT('Ctrl Pts',(-1.73205080756887,5.66372105737959E-15,
-16.5125));
#362488=CARTESIAN_POINT('Ctrl Pts',(-1.29903810567665,-0.749999999999992,
-16.4708333333333));
#362489=CARTESIAN_POINT('Ctrl Pts',(-0.866025403784437,-1.49999999999999,
-16.4291666666667));
#362490=CARTESIAN_POINT('Ctrl Pts',(-1.83697019872102E-16,-1.49999999999999,
-16.3875));
#362491=CARTESIAN_POINT('Ctrl Pts',(0.866025403784436,-1.49999999999999,
-16.3458333333333));
#362492=CARTESIAN_POINT('Ctrl Pts',(1.29903810567665,-0.749999999999993,
-16.3041666666667));
#362493=CARTESIAN_POINT('Ctrl Pts',(1.73205080756887,5.13021704214306E-15,
-16.2625));
#362494=CARTESIAN_POINT('Ctrl Pts',(1.29903810567665,0.750000000000002,
-16.2208333333333));
#362495=CARTESIAN_POINT('Ctrl Pts',(0.866025403784437,1.5,-16.1791666666667));
#362496=CARTESIAN_POINT('Ctrl Pts',(0.,1.5,-16.1375));
#362497=CARTESIAN_POINT('Ctrl Pts',(-0.866025403784436,1.5,-16.0958333333333));
#362498=CARTESIAN_POINT('Ctrl Pts',(-1.29903810567665,0.750000000000003,
-16.0541666666667));
#362499=CARTESIAN_POINT('Ctrl Pts',(-1.73205080756887,5.44517321788645E-15,
-16.0125));
#362500=CARTESIAN_POINT('Ctrl Pts',(-1.29903810567665,-0.749999999999992,
-15.9708333333333));
#362501=CARTESIAN_POINT('Ctrl Pts',(-0.866025403784437,-1.49999999999999,
-15.9291666666667));
#362502=CARTESIAN_POINT('Ctrl Pts',(-1.83697019872102E-16,-1.49999999999999,
-15.8875));
#362503=CARTESIAN_POINT('Ctrl Pts',(0.866025403784436,-1.49999999999999,
-15.8458333333333));
#362504=CARTESIAN_POINT('Ctrl Pts',(1.29903810567665,-0.749999999999993,
-15.8041666666667));
#362505=CARTESIAN_POINT('Ctrl Pts',(1.73205080756887,4.91166920264992E-15,
-15.7625));
#362506=CARTESIAN_POINT('Ctrl Pts',(1.29903810567665,0.750000000000002,
-15.7208333333333));
#362507=CARTESIAN_POINT('Ctrl Pts',(0.866025403784437,1.5,-15.6791666666667));
#362508=CARTESIAN_POINT('Ctrl Pts',(0.,1.5,-15.6375));
#362509=CARTESIAN_POINT('Ctrl Pts',(-0.866025403784436,1.5,-15.5958333333333));
#362510=CARTESIAN_POINT('Ctrl Pts',(-1.29903810567665,0.750000000000003,
-15.5541666666667));
#362511=CARTESIAN_POINT('Ctrl Pts',(-1.73205080756887,5.22662537839331E-15,
-15.5125));
#362512=CARTESIAN_POINT('Ctrl Pts',(-1.29903810567665,-0.749999999999992,
-15.4708333333333));
#362513=CARTESIAN_POINT('Ctrl Pts',(-0.866025403784437,-1.49999999999999,
-15.4291666666667));
#362514=CARTESIAN_POINT('Ctrl Pts',(-1.83697019872102E-16,-1.49999999999999,
-15.3875));
#362515=CARTESIAN_POINT('Ctrl Pts',(0.866025403784436,-1.49999999999999,
-15.3458333333333));
#362516=CARTESIAN_POINT('Ctrl Pts',(1.29903810567665,-0.749999999999993,
-15.3041666666667));
#362517=CARTESIAN_POINT('Ctrl Pts',(1.73205080756887,4.69312136315677E-15,
-15.2625));
#362518=CARTESIAN_POINT('Ctrl Pts',(1.29903810567665,0.750000000000002,
-15.2208333333333));
#362519=CARTESIAN_POINT('Ctrl Pts',(0.866025403784437,1.5,-15.1791666666667));
#362520=CARTESIAN_POINT('Ctrl Pts',(0.,1.5,-15.1375));
#362521=CARTESIAN_POINT('Ctrl Pts',(-0.866025403784436,1.5,-15.0958333333333));
#362522=CARTESIAN_POINT('Ctrl Pts',(-1.29903810567665,0.750000000000003,
-15.0541666666667));
#362523=CARTESIAN_POINT('Ctrl Pts',(-1.73205080756887,5.00807753890017E-15,
-15.0125));
#362524=CARTESIAN_POINT('Ctrl Pts',(-1.29903810567665,-0.749999999999993,
-14.9708333333333));
#362525=CARTESIAN_POINT('Ctrl Pts',(-0.866025403784437,-1.49999999999999,
-14.9291666666667));
#362526=CARTESIAN_POINT('Ctrl Pts',(-1.83697019872102E-16,-1.49999999999999,
-14.8875));
#362527=CARTESIAN_POINT('Ctrl Pts',(0.866025403784436,-1.49999999999999,
-14.8458333333333));
#362528=CARTESIAN_POINT('Ctrl Pts',(1.29903810567665,-0.749999999999994,
-14.8041666666667));
#362529=CARTESIAN_POINT('Ctrl Pts',(1.73205080756887,4.47457352366363E-15,
-14.7625));
#362530=CARTESIAN_POINT('Ctrl Pts',(1.29903810567665,0.750000000000002,
-14.7208333333333));
#362531=CARTESIAN_POINT('Ctrl Pts',(0.866025403784437,1.5,-14.6791666666667));
#362532=CARTESIAN_POINT('Ctrl Pts',(0.,1.5,-14.6375));
#362533=CARTESIAN_POINT('Ctrl Pts',(-0.866025403784436,1.5,-14.5958333333333));
#362534=CARTESIAN_POINT('Ctrl Pts',(-1.29903810567665,0.750000000000003,
-14.5541666666667));
#362535=CARTESIAN_POINT('Ctrl Pts',(-1.73205080756887,4.78952969940702E-15,
-14.5125));
#362536=CARTESIAN_POINT('Ctrl Pts',(-1.29903810567665,-0.749999999999993,
-14.4708333333333));
#362537=CARTESIAN_POINT('Ctrl Pts',(-0.866025403784437,-1.49999999999999,
-14.4291666666667));
#362538=CARTESIAN_POINT('Ctrl Pts',(-1.83697019872102E-16,-1.49999999999999,
-14.3875));
#362539=CARTESIAN_POINT('Ctrl Pts',(0.866025403784436,-1.49999999999999,
-14.3458333333333));
#362540=CARTESIAN_POINT('Ctrl Pts',(1.29903810567665,-0.749999999999994,
-14.3041666666667));
#362541=CARTESIAN_POINT('Ctrl Pts',(1.73205080756887,4.25602568417049E-15,
-14.2625));
#362542=CARTESIAN_POINT('Ctrl Pts',(1.29903810567665,0.750000000000001,
-14.2208333333333));
#362543=CARTESIAN_POINT('Ctrl Pts',(0.866025403784437,1.5,-14.1791666666667));
#362544=CARTESIAN_POINT('Ctrl Pts',(0.,1.5,-14.1375));
#362545=CARTESIAN_POINT('Ctrl Pts',(-0.866025403784436,1.5,-14.0958333333333));
#362546=CARTESIAN_POINT('Ctrl Pts',(-1.29903810567665,0.750000000000003,
-14.0541666666667));
#362547=CARTESIAN_POINT('Ctrl Pts',(-1.73205080756887,4.57098185991388E-15,
-14.0125));
#362548=CARTESIAN_POINT('Ctrl Pts',(-1.29903810567665,-0.749999999999993,
-13.9708333333333));
#362549=CARTESIAN_POINT('Ctrl Pts',(-0.866025403784437,-1.49999999999999,
-13.9291666666667));
#362550=CARTESIAN_POINT('Ctrl Pts',(-1.83697019872102E-16,-1.49999999999999,
-13.8875));
#362551=CARTESIAN_POINT('Ctrl Pts',(0.866025403784436,-1.49999999999999,
-13.8458333333333));
#362552=CARTESIAN_POINT('Ctrl Pts',(1.29903810567665,-0.749999999999994,
-13.8041666666667));
#362553=CARTESIAN_POINT('Ctrl Pts',(1.73205080756887,4.03747784467735E-15,
-13.7625));
#362554=CARTESIAN_POINT('Ctrl Pts',(1.29903810567665,0.750000000000001,
-13.7208333333333));
#362555=CARTESIAN_POINT('Ctrl Pts',(0.866025403784437,1.5,-13.6791666666667));
#362556=CARTESIAN_POINT('Ctrl Pts',(0.,1.5,-13.6375));
#362557=CARTESIAN_POINT('Ctrl Pts',(-0.866025403784436,1.5,-13.5958333333333));
#362558=CARTESIAN_POINT('Ctrl Pts',(-1.29903810567665,0.750000000000002,
-13.5541666666667));
#362559=CARTESIAN_POINT('Ctrl Pts',(-1.73205080756887,4.35243402042074E-15,
-13.5125));
#362560=CARTESIAN_POINT('Ctrl Pts',(-1.29903810567665,-0.749999999999993,
-13.4708333333333));
#362561=CARTESIAN_POINT('Ctrl Pts',(-0.866025403784437,-1.49999999999999,
-13.4291666666667));
#362562=CARTESIAN_POINT('Ctrl Pts',(-1.83697019872102E-16,-1.49999999999999,
-13.3875));
#362563=CARTESIAN_POINT('Ctrl Pts',(0.866025403784436,-1.49999999999999,
-13.3458333333333));
#362564=CARTESIAN_POINT('Ctrl Pts',(1.29903810567665,-0.749999999999994,
-13.3041666666667));
#362565=CARTESIAN_POINT('Ctrl Pts',(1.73205080756887,3.81893000518421E-15,
-13.2625));
#362566=CARTESIAN_POINT('Ctrl Pts',(1.29903810567665,0.750000000000001,
-13.2208333333333));
#362567=CARTESIAN_POINT('Ctrl Pts',(0.866025403784437,1.5,-13.1791666666667));
#362568=CARTESIAN_POINT('Ctrl Pts',(0.,1.5,-13.1375));
#362569=CARTESIAN_POINT('Ctrl Pts',(-0.866025403784436,1.5,-13.0958333333333));
#362570=CARTESIAN_POINT('Ctrl Pts',(-1.29903810567665,0.750000000000002,
-13.0541666666667));
#362571=CARTESIAN_POINT('Ctrl Pts',(-1.73205080756887,4.1338861809276E-15,
-13.0125));
#362572=CARTESIAN_POINT('Ctrl Pts',(-1.29903810567665,-0.749999999999993,
-12.9708333333333));
#362573=CARTESIAN_POINT('Ctrl Pts',(-0.866025403784437,-1.49999999999999,
-12.9291666666667));
#362574=CARTESIAN_POINT('Ctrl Pts',(-1.83697019872102E-16,-1.49999999999999,
-12.8875));
#362575=CARTESIAN_POINT('Ctrl Pts',(0.866025403784436,-1.49999999999999,
-12.8458333333333));
#362576=CARTESIAN_POINT('Ctrl Pts',(1.29903810567665,-0.749999999999994,
-12.8041666666667));
#362577=CARTESIAN_POINT('Ctrl Pts',(1.73205080756887,3.60038216569107E-15,
-12.7625));
#362578=CARTESIAN_POINT('Ctrl Pts',(1.29903810567665,0.750000000000001,
-12.7208333333333));
#362579=CARTESIAN_POINT('Ctrl Pts',(0.866025403784437,1.5,-12.6791666666667));
#362580=CARTESIAN_POINT('Ctrl Pts',(0.,1.5,-12.6375));
#362581=CARTESIAN_POINT('Ctrl Pts',(-0.866025403784436,1.5,-12.5958333333333));
#362582=CARTESIAN_POINT('Ctrl Pts',(-1.29903810567665,0.750000000000002,
-12.5541666666667));
#362583=CARTESIAN_POINT('Ctrl Pts',(-1.73205080756887,3.91533834143446E-15,
-12.5125));
#362584=CARTESIAN_POINT('Ctrl Pts',(-1.29903810567665,-0.749999999999994,
-12.4708333333333));
#362585=CARTESIAN_POINT('Ctrl Pts',(-0.866025403784437,-1.49999999999999,
-12.4291666666667));
#362586=CARTESIAN_POINT('Ctrl Pts',(-1.83697019872102E-16,-1.49999999999999,
-12.3875));
#362587=CARTESIAN_POINT('Ctrl Pts',(0.866025403784436,-1.49999999999999,
-12.3458333333333));
#362588=CARTESIAN_POINT('Ctrl Pts',(1.29903810567665,-0.749999999999995,
-12.3041666666667));
#362589=CARTESIAN_POINT('Ctrl Pts',(1.73205080756887,3.38183432619793E-15,
-12.2625));
#362590=CARTESIAN_POINT('Ctrl Pts',(1.29903810567665,0.75,-12.2208333333333));
#362591=CARTESIAN_POINT('Ctrl Pts',(0.866025403784437,1.5,-12.1791666666667));
#362592=CARTESIAN_POINT('Ctrl Pts',(0.,1.5,-12.1375));
#362593=CARTESIAN_POINT('Ctrl Pts',(-0.866025403784436,1.5,-12.0958333333333));
#362594=CARTESIAN_POINT('Ctrl Pts',(-1.29903810567665,0.750000000000002,
-12.0541666666667));
#362595=CARTESIAN_POINT('Ctrl Pts',(-1.73205080756887,3.69679050194132E-15,
-12.0125));
#362596=CARTESIAN_POINT('Ctrl Pts',(-1.29903810567665,-0.749999999999994,
-11.9708333333333));
#362597=CARTESIAN_POINT('Ctrl Pts',(-0.866025403784437,-1.49999999999999,
-11.9291666666667));
#362598=CARTESIAN_POINT('Ctrl Pts',(-1.83697019872102E-16,-1.49999999999999,
-11.8875));
#362599=CARTESIAN_POINT('Ctrl Pts',(0.866025403784436,-1.49999999999999,
-11.8458333333333));
#362600=CARTESIAN_POINT('Ctrl Pts',(1.29903810567665,-0.749999999999995,
-11.8041666666667));
#362601=CARTESIAN_POINT('Ctrl Pts',(1.73205080756887,3.16328648670478E-15,
-11.7625));
#362602=CARTESIAN_POINT('Ctrl Pts',(1.29903810567665,0.75,-11.7208333333333));
#362603=CARTESIAN_POINT('Ctrl Pts',(0.866025403784437,1.5,-11.6791666666667));
#362604=CARTESIAN_POINT('Ctrl Pts',(0.,1.5,-11.6375));
#362605=CARTESIAN_POINT('Ctrl Pts',(-0.866025403784436,1.5,-11.5958333333333));
#362606=CARTESIAN_POINT('Ctrl Pts',(-1.29903810567665,0.750000000000001,
-11.5541666666667));
#362607=CARTESIAN_POINT('Ctrl Pts',(-1.73205080756887,3.47824266244818E-15,
-11.5125));
#362608=CARTESIAN_POINT('Ctrl Pts',(-1.29903810567665,-0.749999999999994,
-11.4708333333333));
#362609=CARTESIAN_POINT('Ctrl Pts',(-0.866025403784437,-1.49999999999999,
-11.4291666666667));
#362610=CARTESIAN_POINT('Ctrl Pts',(-1.83697019872102E-16,-1.49999999999999,
-11.3875));
#362611=CARTESIAN_POINT('Ctrl Pts',(0.866025403784436,-1.49999999999999,
-11.3458333333333));
#362612=CARTESIAN_POINT('Ctrl Pts',(1.29903810567665,-0.749999999999995,
-11.3041666666667));
#362613=CARTESIAN_POINT('Ctrl Pts',(1.73205080756887,2.94473864721164E-15,
-11.2625));
#362614=CARTESIAN_POINT('Ctrl Pts',(1.29903810567665,0.75,-11.2208333333333));
#362615=CARTESIAN_POINT('Ctrl Pts',(0.866025403784437,1.5,-11.1791666666667));
#362616=CARTESIAN_POINT('Ctrl Pts',(0.,1.5,-11.1375));
#362617=CARTESIAN_POINT('Ctrl Pts',(-0.866025403784436,1.5,-11.0958333333333));
#362618=CARTESIAN_POINT('Ctrl Pts',(-1.29903810567665,0.750000000000001,
-11.0541666666667));
#362619=CARTESIAN_POINT('Ctrl Pts',(-1.73205080756887,3.25969482295504E-15,
-11.0125));
#362620=CARTESIAN_POINT('Ctrl Pts',(-1.29903810567665,-0.749999999999994,
-10.9708333333333));
#362621=CARTESIAN_POINT('Ctrl Pts',(-0.866025403784437,-1.49999999999999,
-10.9291666666667));
#362622=CARTESIAN_POINT('Ctrl Pts',(-1.83697019872102E-16,-1.49999999999999,
-10.8875));
#362623=CARTESIAN_POINT('Ctrl Pts',(0.866025403784436,-1.49999999999999,
-10.8458333333333));
#362624=CARTESIAN_POINT('Ctrl Pts',(1.29903810567665,-0.749999999999995,
-10.8041666666667));
#362625=CARTESIAN_POINT('Ctrl Pts',(1.73205080756887,2.7261908077185E-15,
-10.7625));
#362626=CARTESIAN_POINT('Ctrl Pts',(1.29903810567665,0.75,-10.7208333333333));
#362627=CARTESIAN_POINT('Ctrl Pts',(0.866025403784437,1.5,-10.6791666666667));
#362628=CARTESIAN_POINT('Ctrl Pts',(0.,1.5,-10.6375));
#362629=CARTESIAN_POINT('Ctrl Pts',(-0.866025403784436,1.5,-10.5958333333333));
#362630=CARTESIAN_POINT('Ctrl Pts',(-1.29903810567665,0.750000000000001,
-10.5541666666667));
#362631=CARTESIAN_POINT('Ctrl Pts',(-1.73205080756887,3.04114698346189E-15,
-10.5125));
#362632=CARTESIAN_POINT('Ctrl Pts',(-1.29903810567665,-0.749999999999994,
-10.4708333333333));
#362633=CARTESIAN_POINT('Ctrl Pts',(-0.866025403784437,-1.49999999999999,
-10.4291666666667));
#362634=CARTESIAN_POINT('Ctrl Pts',(-1.83697019872102E-16,-1.49999999999999,
-10.3875));
#362635=CARTESIAN_POINT('Ctrl Pts',(0.866025403784436,-1.49999999999999,
-10.3458333333333));
#362636=CARTESIAN_POINT('Ctrl Pts',(1.29903810567665,-0.749999999999996,
-10.3041666666667));
#362637=CARTESIAN_POINT('Ctrl Pts',(1.73205080756887,2.50764296822536E-15,
-10.2625));
#362638=CARTESIAN_POINT('Ctrl Pts',(1.29903810567665,0.749999999999999,
-10.2208333333333));
#362639=CARTESIAN_POINT('Ctrl Pts',(0.866025403784437,1.5,-10.1791666666667));
#362640=CARTESIAN_POINT('Ctrl Pts',(0.,1.5,-10.1375));
#362641=CARTESIAN_POINT('Ctrl Pts',(-0.866025403784436,1.5,-10.0958333333333));
#362642=CARTESIAN_POINT('Ctrl Pts',(-1.29903810567665,0.750000000000001,
-10.0541666666667));
#362643=CARTESIAN_POINT('Ctrl Pts',(-1.73205080756887,2.82259914396875E-15,
-10.0125));
#362644=CARTESIAN_POINT('Ctrl Pts',(-1.29903810567665,-0.749999999999995,
-9.97083333333333));
#362645=CARTESIAN_POINT('Ctrl Pts',(-0.866025403784437,-1.49999999999999,
-9.92916666666667));
#362646=CARTESIAN_POINT('Ctrl Pts',(-1.83697019872102E-16,-1.49999999999999,
-9.8875));
#362647=CARTESIAN_POINT('Ctrl Pts',(0.866025403784436,-1.49999999999999,
-9.84583333333333));
#362648=CARTESIAN_POINT('Ctrl Pts',(1.29903810567665,-0.749999999999996,
-9.80416666666667));
#362649=CARTESIAN_POINT('Ctrl Pts',(1.73205080756887,2.28909512873222E-15,
-9.7625));
#362650=CARTESIAN_POINT('Ctrl Pts',(1.29903810567665,0.749999999999999,
-9.72083333333333));
#362651=CARTESIAN_POINT('Ctrl Pts',(0.866025403784437,1.5,-9.67916666666667));
#362652=CARTESIAN_POINT('Ctrl Pts',(0.,1.5,-9.6375));
#362653=CARTESIAN_POINT('Ctrl Pts',(-0.866025403784436,1.5,-9.59583333333333));
#362654=CARTESIAN_POINT('Ctrl Pts',(-1.29903810567665,0.750000000000001,
-9.55416666666667));
#362655=CARTESIAN_POINT('Ctrl Pts',(-1.73205080756887,2.60405130447561E-15,
-9.5125));
#362656=CARTESIAN_POINT('Ctrl Pts',(-1.29903810567665,-0.749999999999995,
-9.47083333333333));
#362657=CARTESIAN_POINT('Ctrl Pts',(-0.866025403784437,-1.49999999999999,
-9.42916666666667));
#362658=CARTESIAN_POINT('Ctrl Pts',(-1.83697019872102E-16,-1.49999999999999,
-9.3875));
#362659=CARTESIAN_POINT('Ctrl Pts',(0.866025403784436,-1.49999999999999,
-9.34583333333333));
#362660=CARTESIAN_POINT('Ctrl Pts',(1.29903810567665,-0.749999999999996,
-9.30416666666667));
#362661=CARTESIAN_POINT('Ctrl Pts',(1.73205080756887,2.07054728923908E-15,
-9.2625));
#362662=CARTESIAN_POINT('Ctrl Pts',(1.29903810567665,0.749999999999999,
-9.22083333333333));
#362663=CARTESIAN_POINT('Ctrl Pts',(0.866025403784437,1.5,-9.17916666666667));
#362664=CARTESIAN_POINT('Ctrl Pts',(0.,1.5,-9.1375));
#362665=CARTESIAN_POINT('Ctrl Pts',(-0.866025403784436,1.5,-9.09583333333333));
#362666=CARTESIAN_POINT('Ctrl Pts',(-1.29903810567665,0.75,-9.05416666666667));
#362667=CARTESIAN_POINT('Ctrl Pts',(-1.73205080756887,2.38550346498247E-15,
-9.0125));
#362668=CARTESIAN_POINT('Ctrl Pts',(-1.29903810567665,-0.749999999999995,
-8.97083333333333));
#362669=CARTESIAN_POINT('Ctrl Pts',(-0.866025403784437,-1.49999999999999,
-8.92916666666667));
#362670=CARTESIAN_POINT('Ctrl Pts',(-1.83697019872102E-16,-1.49999999999999,
-8.8875));
#362671=CARTESIAN_POINT('Ctrl Pts',(0.866025403784436,-1.49999999999999,
-8.84583333333333));
#362672=CARTESIAN_POINT('Ctrl Pts',(1.29903810567665,-0.749999999999996,
-8.80416666666667));
#362673=CARTESIAN_POINT('Ctrl Pts',(1.73205080756887,1.85199944974594E-15,
-8.7625));
#362674=CARTESIAN_POINT('Ctrl Pts',(1.29903810567665,0.749999999999999,
-8.72083333333333));
#362675=CARTESIAN_POINT('Ctrl Pts',(0.866025403784437,1.5,-8.67916666666667));
#362676=CARTESIAN_POINT('Ctrl Pts',(0.,1.5,-8.6375));
#362677=CARTESIAN_POINT('Ctrl Pts',(-0.866025403784436,1.5,-8.59583333333333));
#362678=CARTESIAN_POINT('Ctrl Pts',(-1.29903810567665,0.75,-8.55416666666667));
#362679=CARTESIAN_POINT('Ctrl Pts',(-1.73205080756887,2.16695562548933E-15,
-8.5125));
#362680=CARTESIAN_POINT('Ctrl Pts',(-1.29903810567665,-0.749999999999995,
-8.47083333333333));
#362681=CARTESIAN_POINT('Ctrl Pts',(-0.866025403784437,-1.49999999999999,
-8.42916666666667));
#362682=CARTESIAN_POINT('Ctrl Pts',(-1.83697019872102E-16,-1.49999999999999,
-8.3875));
#362683=CARTESIAN_POINT('Ctrl Pts',(0.866025403784436,-1.49999999999999,
-8.34583333333333));
#362684=CARTESIAN_POINT('Ctrl Pts',(1.29903810567665,-0.749999999999996,
-8.30416666666667));
#362685=CARTESIAN_POINT('Ctrl Pts',(1.73205080756887,1.6334516102528E-15,
-8.2625));
#362686=CARTESIAN_POINT('Ctrl Pts',(1.29903810567665,0.749999999999999,
-8.22083333333333));
#362687=CARTESIAN_POINT('Ctrl Pts',(0.866025403784437,1.5,-8.17916666666667));
#362688=CARTESIAN_POINT('Ctrl Pts',(0.,1.5,-8.1375));
#362689=CARTESIAN_POINT('Ctrl Pts',(-0.866025403784436,1.5,-8.09583333333333));
#362690=CARTESIAN_POINT('Ctrl Pts',(-1.29903810567665,0.75,-8.05416666666667));
#362691=CARTESIAN_POINT('Ctrl Pts',(-1.73205080756887,1.94840778599619E-15,
-8.0125));
#362692=CARTESIAN_POINT('Ctrl Pts',(-1.29903810567665,-0.749999999999996,
-7.97083333333334));
#362693=CARTESIAN_POINT('Ctrl Pts',(-0.866025403784437,-1.49999999999999,
-7.92916666666667));
#362694=CARTESIAN_POINT('Ctrl Pts',(-1.83697019872102E-16,-1.49999999999999,
-7.8875));
#362695=CARTESIAN_POINT('Ctrl Pts',(0.866025403784436,-1.49999999999999,
-7.84583333333333));
#362696=CARTESIAN_POINT('Ctrl Pts',(1.29903810567665,-0.749999999999997,
-7.80416666666667));
#362697=CARTESIAN_POINT('Ctrl Pts',(1.73205080756887,1.41490377075966E-15,
-7.7625));
#362698=CARTESIAN_POINT('Ctrl Pts',(1.29903810567665,0.749999999999998,
-7.72083333333334));
#362699=CARTESIAN_POINT('Ctrl Pts',(0.866025403784437,1.5,-7.67916666666667));
#362700=CARTESIAN_POINT('Ctrl Pts',(0.,1.5,-7.6375));
#362701=CARTESIAN_POINT('Ctrl Pts',(-0.866025403784436,1.5,-7.59583333333333));
#362702=CARTESIAN_POINT('Ctrl Pts',(-1.29903810567665,0.75,-7.55416666666667));
#362703=CARTESIAN_POINT('Ctrl Pts',(-1.73205080756887,1.72985994650305E-15,
-7.5125));
#362704=CARTESIAN_POINT('Ctrl Pts',(-1.29903810567665,-0.749999999999996,
-7.47083333333333));
#362705=CARTESIAN_POINT('Ctrl Pts',(-0.866025403784437,-1.49999999999999,
-7.42916666666667));
#362706=CARTESIAN_POINT('Ctrl Pts',(-1.83697019872102E-16,-1.49999999999999,
-7.3875));
#362707=CARTESIAN_POINT('Ctrl Pts',(0.866025403784436,-1.49999999999999,
-7.34583333333334));
#362708=CARTESIAN_POINT('Ctrl Pts',(1.29903810567665,-0.749999999999997,
-7.30416666666667));
#362709=CARTESIAN_POINT('Ctrl Pts',(1.73205080756887,1.19635593126651E-15,
-7.2625));
#362710=CARTESIAN_POINT('Ctrl Pts',(1.29903810567665,0.749999999999998,
-7.22083333333333));
#362711=CARTESIAN_POINT('Ctrl Pts',(0.866025403784437,1.5,-7.17916666666667));
#362712=CARTESIAN_POINT('Ctrl Pts',(0.,1.5,-7.1375));
#362713=CARTESIAN_POINT('Ctrl Pts',(-0.866025403784436,1.5,-7.09583333333333));
#362714=CARTESIAN_POINT('Ctrl Pts',(-1.29903810567665,0.749999999999999,
-7.05416666666667));
#362715=CARTESIAN_POINT('Ctrl Pts',(-1.73205080756887,1.51131210700991E-15,
-7.0125));
#362716=CARTESIAN_POINT('Ctrl Pts',(-1.29903810567665,-0.749999999999996,
-6.97083333333333));
#362717=CARTESIAN_POINT('Ctrl Pts',(-0.866025403784437,-1.49999999999999,
-6.92916666666667));
#362718=CARTESIAN_POINT('Ctrl Pts',(-1.83697019872102E-16,-1.49999999999999,
-6.8875));
#362719=CARTESIAN_POINT('Ctrl Pts',(0.866025403784436,-1.49999999999999,
-6.84583333333333));
#362720=CARTESIAN_POINT('Ctrl Pts',(1.29903810567665,-0.749999999999997,
-6.80416666666667));
#362721=CARTESIAN_POINT('Ctrl Pts',(1.73205080756887,9.77808091773373E-16,
-6.7625));
#362722=CARTESIAN_POINT('Ctrl Pts',(1.29903810567665,0.749999999999998,
-6.72083333333333));
#362723=CARTESIAN_POINT('Ctrl Pts',(0.866025403784437,1.5,-6.67916666666667));
#362724=CARTESIAN_POINT('Ctrl Pts',(0.,1.5,-6.6375));
#362725=CARTESIAN_POINT('Ctrl Pts',(-0.866025403784436,1.5,-6.59583333333333));
#362726=CARTESIAN_POINT('Ctrl Pts',(-1.29903810567665,0.749999999999999,
-6.55416666666667));
#362727=CARTESIAN_POINT('Ctrl Pts',(-1.73205080756887,1.29276426751676E-15,
-6.5125));
#362728=CARTESIAN_POINT('Ctrl Pts',(-1.29903810567665,-0.749999999999996,
-6.47083333333334));
#362729=CARTESIAN_POINT('Ctrl Pts',(-0.866025403784437,-1.49999999999999,
-6.42916666666667));
#362730=CARTESIAN_POINT('Ctrl Pts',(-1.83697019872102E-16,-1.49999999999999,
-6.3875));
#362731=CARTESIAN_POINT('Ctrl Pts',(0.866025403784436,-1.49999999999999,
-6.34583333333333));
#362732=CARTESIAN_POINT('Ctrl Pts',(1.29903810567665,-0.749999999999997,
-6.30416666666667));
#362733=CARTESIAN_POINT('Ctrl Pts',(1.73205080756887,7.59260252280232E-16,
-6.2625));
#362734=CARTESIAN_POINT('Ctrl Pts',(1.29903810567665,0.749999999999998,
-6.22083333333333));
#362735=CARTESIAN_POINT('Ctrl Pts',(0.866025403784437,1.5,-6.17916666666667));
#362736=CARTESIAN_POINT('Ctrl Pts',(0.,1.5,-6.1375));
#362737=CARTESIAN_POINT('Ctrl Pts',(-0.866025403784436,1.5,-6.09583333333334));
#362738=CARTESIAN_POINT('Ctrl Pts',(-1.29903810567665,0.749999999999999,
-6.05416666666667));
#362739=CARTESIAN_POINT('Ctrl Pts',(-1.73205080756887,1.07421642802362E-15,
-6.0125));
#362740=CARTESIAN_POINT('Ctrl Pts',(-1.29903810567665,-0.749999999999996,
-5.97083333333333));
#362741=CARTESIAN_POINT('Ctrl Pts',(-0.866025403784437,-1.49999999999999,
-5.92916666666667));
#362742=CARTESIAN_POINT('Ctrl Pts',(-1.83697019872102E-16,-1.49999999999999,
-5.8875));
#362743=CARTESIAN_POINT('Ctrl Pts',(0.866025403784436,-1.5,-5.84583333333334));
#362744=CARTESIAN_POINT('Ctrl Pts',(1.29903810567665,-0.749999999999998,
-5.80416666666667));
#362745=CARTESIAN_POINT('Ctrl Pts',(1.73205080756887,5.40712412787091E-16,
-5.7625));
#362746=CARTESIAN_POINT('Ctrl Pts',(1.29903810567665,0.749999999999998,
-5.72083333333333));
#362747=CARTESIAN_POINT('Ctrl Pts',(0.866025403784437,1.5,-5.67916666666667));
#362748=CARTESIAN_POINT('Ctrl Pts',(0.,1.5,-5.6375));
#362749=CARTESIAN_POINT('Ctrl Pts',(-0.866025403784436,1.5,-5.59583333333333));
#362750=CARTESIAN_POINT('Ctrl Pts',(-1.29903810567665,0.749999999999999,
-5.55416666666667));
#362751=CARTESIAN_POINT('Ctrl Pts',(-1.73205080756887,8.55668588530483E-16,
-5.5125));
#362752=CARTESIAN_POINT('Ctrl Pts',(-1.29903810567665,-0.749999999999997,
-5.47083333333333));
#362753=CARTESIAN_POINT('Ctrl Pts',(-0.866025403784437,-1.49999999999999,
-5.42916666666667));
#362754=CARTESIAN_POINT('Ctrl Pts',(-1.83697019872102E-16,-1.49999999999999,
-5.3875));
#362755=CARTESIAN_POINT('Ctrl Pts',(0.866025403784436,-1.5,-5.34583333333333));
#362756=CARTESIAN_POINT('Ctrl Pts',(1.29903810567665,-0.749999999999998,
-5.30416666666667));
#362757=CARTESIAN_POINT('Ctrl Pts',(1.73205080756887,3.2216457329395E-16,
-5.2625));
#362758=CARTESIAN_POINT('Ctrl Pts',(1.29903810567665,0.749999999999997,
-5.22083333333333));
#362759=CARTESIAN_POINT('Ctrl Pts',(0.866025403784437,1.5,-5.17916666666667));
#362760=CARTESIAN_POINT('Ctrl Pts',(0.,1.5,-5.1375));
#362761=CARTESIAN_POINT('Ctrl Pts',(-0.866025403784436,1.5,-5.09583333333333));
#362762=CARTESIAN_POINT('Ctrl Pts',(-1.29903810567665,0.749999999999998,
-5.05416666666667));
#362763=CARTESIAN_POINT('Ctrl Pts',(-1.73205080756887,6.37120749037341E-16,
-5.0125));
#362764=CARTESIAN_POINT('Ctrl Pts',(-1.29903810567665,-0.749999999999997,
-4.97083333333333));
#362765=CARTESIAN_POINT('Ctrl Pts',(-0.866025403784437,-1.49999999999999,
-4.92916666666667));
#362766=CARTESIAN_POINT('Ctrl Pts',(-1.83697019872102E-16,-1.5,-4.8875));
#362767=CARTESIAN_POINT('Ctrl Pts',(0.866025403784436,-1.5,-4.84583333333333));
#362768=CARTESIAN_POINT('Ctrl Pts',(1.29903810567665,-0.749999999999998,
-4.80416666666667));
#362769=CARTESIAN_POINT('Ctrl Pts',(1.73205080756887,1.03616733800808E-16,
-4.7625));
#362770=CARTESIAN_POINT('Ctrl Pts',(1.29903810567665,0.749999999999997,
-4.72083333333333));
#362771=CARTESIAN_POINT('Ctrl Pts',(0.866025403784437,1.5,-4.67916666666667));
#362772=CARTESIAN_POINT('Ctrl Pts',(0.,1.5,-4.6375));
#362773=CARTESIAN_POINT('Ctrl Pts',(-0.866025403784436,1.5,-4.59583333333333));
#362774=CARTESIAN_POINT('Ctrl Pts',(-1.29903810567665,0.749999999999998,
-4.55416666666667));
#362775=CARTESIAN_POINT('Ctrl Pts',(-1.73205080756887,4.185729095442E-16,
-4.5125));
#362776=CARTESIAN_POINT('Ctrl Pts',(-1.29903810567665,-0.749999999999997,
-4.47083333333333));
#362777=CARTESIAN_POINT('Ctrl Pts',(-0.866025403784437,-1.49999999999999,
-4.42916666666667));
#362778=CARTESIAN_POINT('Ctrl Pts',(-1.83697019872102E-16,-1.5,-4.3875));
#362779=CARTESIAN_POINT('Ctrl Pts',(0.866025403784436,-1.5,-4.34583333333333));
#362780=CARTESIAN_POINT('Ctrl Pts',(1.29903810567665,-0.749999999999998,
-4.30416666666667));
#362781=CARTESIAN_POINT('Ctrl Pts',(1.73205080756887,-1.14931105692333E-16,
-4.2625));
#362782=CARTESIAN_POINT('Ctrl Pts',(1.29903810567665,0.749999999999997,
-4.22083333333333));
#362783=CARTESIAN_POINT('Ctrl Pts',(0.866025403784437,1.5,-4.17916666666667));
#362784=CARTESIAN_POINT('Ctrl Pts',(0.,1.5,-4.1375));
#362785=CARTESIAN_POINT('Ctrl Pts',(-0.866025403784436,1.5,-4.09583333333333));
#362786=CARTESIAN_POINT('Ctrl Pts',(-1.29903810567665,0.749999999999998,
-4.05416666666667));
#362787=CARTESIAN_POINT('Ctrl Pts',(-1.73205080756887,2.00025070051059E-16,
-4.0125));
#362788=CARTESIAN_POINT('Ctrl Pts',(-1.29903810567665,-0.749999999999997,
-3.97083333333333));
#362789=CARTESIAN_POINT('Ctrl Pts',(-0.866025403784437,-1.5,-3.92916666666667));
#362790=CARTESIAN_POINT('Ctrl Pts',(-1.83697019872102E-16,-1.5,-3.8875));
#362791=CARTESIAN_POINT('Ctrl Pts',(0.866025403784436,-1.5,-3.84583333333333));
#362792=CARTESIAN_POINT('Ctrl Pts',(1.29903810567665,-0.749999999999998,
-3.80416666666667));
#362793=CARTESIAN_POINT('Ctrl Pts',(1.73205080756887,-3.33478945185474E-16,
-3.7625));
#362794=CARTESIAN_POINT('Ctrl Pts',(1.29903810567665,0.749999999999997,
-3.72083333333333));
#362795=CARTESIAN_POINT('Ctrl Pts',(0.866025403784437,1.5,-3.67916666666667));
#362796=CARTESIAN_POINT('Ctrl Pts',(0.,1.5,-3.6375));
#362797=CARTESIAN_POINT('Ctrl Pts',(-0.866025403784436,1.5,-3.59583333333333));
#362798=CARTESIAN_POINT('Ctrl Pts',(-1.29903810567665,0.749999999999998,
-3.55416666666667));
#362799=CARTESIAN_POINT('Ctrl Pts',(-1.73205080756887,-1.85227694420821E-17,
-3.5125));
#362800=CARTESIAN_POINT('Ctrl Pts',(-1.29903810567665,-0.749999999999998,
-3.47083333333333));
#362801=CARTESIAN_POINT('Ctrl Pts',(-0.866025403784437,-1.5,-3.42916666666667));
#362802=CARTESIAN_POINT('Ctrl Pts',(-1.83697019872102E-16,-1.5,-3.3875));
#362803=CARTESIAN_POINT('Ctrl Pts',(0.866025403784436,-1.5,-3.34583333333333));
#362804=CARTESIAN_POINT('Ctrl Pts',(1.29903810567665,-0.749999999999999,
-3.30416666666667));
#362805=CARTESIAN_POINT('Ctrl Pts',(1.73205080756887,-5.52026784678615E-16,
-3.2625));
#362806=CARTESIAN_POINT('Ctrl Pts',(1.29903810567665,0.749999999999996,
-3.22083333333333));
#362807=CARTESIAN_POINT('Ctrl Pts',(0.866025403784437,1.49999999999999,
-3.17916666666667));
#362808=CARTESIAN_POINT('Ctrl Pts',(0.,1.5,-3.1375));
#362809=CARTESIAN_POINT('Ctrl Pts',(-0.866025403784436,1.5,-3.09583333333333));
#362810=CARTESIAN_POINT('Ctrl Pts',(-1.29903810567665,0.749999999999998,
-3.05416666666667));
#362811=CARTESIAN_POINT('Ctrl Pts',(-1.73205080756887,-2.37070608935224E-16,
-3.0125));
#362812=CARTESIAN_POINT('Ctrl Pts',(-1.29903810567665,-0.749999999999998,
-2.97083333333333));
#362813=CARTESIAN_POINT('Ctrl Pts',(-0.866025403784437,-1.5,-2.92916666666667));
#362814=CARTESIAN_POINT('Ctrl Pts',(-1.83697019872102E-16,-1.5,-2.8875));
#362815=CARTESIAN_POINT('Ctrl Pts',(0.866025403784436,-1.5,-2.84583333333333));
#362816=CARTESIAN_POINT('Ctrl Pts',(1.29903810567665,-0.749999999999999,
-2.80416666666667));
#362817=CARTESIAN_POINT('Ctrl Pts',(1.73205080756887,-7.70574624171757E-16,
-2.7625));
#362818=CARTESIAN_POINT('Ctrl Pts',(1.29903810567665,0.749999999999996,
-2.72083333333334));
#362819=CARTESIAN_POINT('Ctrl Pts',(0.866025403784437,1.49999999999999,
-2.67916666666667));
#362820=CARTESIAN_POINT('Ctrl Pts',(0.,1.5,-2.6375));
#362821=CARTESIAN_POINT('Ctrl Pts',(-0.866025403784436,1.5,-2.59583333333334));
#362822=CARTESIAN_POINT('Ctrl Pts',(-1.29903810567665,0.749999999999997,
-2.55416666666667));
#362823=CARTESIAN_POINT('Ctrl Pts',(-1.73205080756887,-4.55618448428365E-16,
-2.5125));
#362824=CARTESIAN_POINT('Ctrl Pts',(-1.29903810567665,-0.749999999999998,
-2.47083333333334));
#362825=CARTESIAN_POINT('Ctrl Pts',(-0.866025403784437,-1.5,-2.42916666666667));
#362826=CARTESIAN_POINT('Ctrl Pts',(-1.83697019872102E-16,-1.5,-2.3875));
#362827=CARTESIAN_POINT('Ctrl Pts',(0.866025403784436,-1.5,-2.34583333333334));
#362828=CARTESIAN_POINT('Ctrl Pts',(1.29903810567665,-0.749999999999999,
-2.30416666666667));
#362829=CARTESIAN_POINT('Ctrl Pts',(1.73205080756887,-9.89122463664898E-16,
-2.2625));
#362830=CARTESIAN_POINT('Ctrl Pts',(1.29903810567665,0.749999999999996,
-2.22083333333333));
#362831=CARTESIAN_POINT('Ctrl Pts',(0.866025403784437,1.49999999999999,
-2.17916666666667));
#362832=CARTESIAN_POINT('Ctrl Pts',(0.,1.49999999999999,-2.1375));
#362833=CARTESIAN_POINT('Ctrl Pts',(-0.866025403784436,1.49999999999999,
-2.09583333333333));
#362834=CARTESIAN_POINT('Ctrl Pts',(-1.29903810567665,0.749999999999997,
-2.05416666666667));
#362835=CARTESIAN_POINT('Ctrl Pts',(-1.73205080756887,-6.74166287921507E-16,
-2.0125));
#362836=CARTESIAN_POINT('Ctrl Pts',(-1.29903810567665,-0.749999999999998,
-1.97083333333333));
#362837=CARTESIAN_POINT('Ctrl Pts',(-0.866025403784437,-1.5,-1.92916666666667));
#362838=CARTESIAN_POINT('Ctrl Pts',(-1.83697019872102E-16,-1.5,-1.8875));
#362839=CARTESIAN_POINT('Ctrl Pts',(0.866025403784436,-1.5,-1.84583333333334));
#362840=CARTESIAN_POINT('Ctrl Pts',(1.29903810567665,-0.749999999999999,
-1.80416666666667));
#362841=CARTESIAN_POINT('Ctrl Pts',(1.73205080756887,-1.20767030315804E-15,
-1.7625));
#362842=CARTESIAN_POINT('Ctrl Pts',(1.29903810567665,0.749999999999996,
-1.72083333333333));
#362843=CARTESIAN_POINT('Ctrl Pts',(0.866025403784437,1.49999999999999,
-1.67916666666667));
#362844=CARTESIAN_POINT('Ctrl Pts',(0.,1.49999999999999,-1.6375));
#362845=CARTESIAN_POINT('Origin',(-1.38777878078146E-16,-5.55111512312578E-15,
-17.91875));
#362846=CARTESIAN_POINT('Ctrl Pts',(-0.190653686693216,-1.15967294634856,
-17.6497595264192));
#362847=CARTESIAN_POINT('Ctrl Pts',(-0.0959624143348497,-1.17524047358082,
-17.6433928286374));
#362848=CARTESIAN_POINT('Ctrl Pts',(-1.43925448419918E-16,-1.17524047358082,
-17.6375));
#362849=CARTESIAN_POINT('Ctrl Pts',(0.,1.50000395501636,-17.6999977165702));
#362850=CARTESIAN_POINT('Ctrl Pts',(-0.866027687214197,1.50000395501636,
-17.6583310499036));
#362851=CARTESIAN_POINT('Ctrl Pts',(-1.2990415308213,0.750001977508185,
-17.6166643832369));
#362852=CARTESIAN_POINT('Ctrl Pts',(-1.73205537442839,6.12813449786473E-15,
-17.5749977165702));
#362853=CARTESIAN_POINT('Ctrl Pts',(-1.2990415308213,-0.750001977508172,
-17.5333310499036));
#362854=CARTESIAN_POINT('Ctrl Pts',(-0.866027687214197,-1.50000395501635,
-17.4916643832369));
#362855=CARTESIAN_POINT('Ctrl Pts',(-1.83697504221915E-16,-1.50000395501635,
-17.4499977165702));
#362856=CARTESIAN_POINT('Ctrl Pts',(0.866027687214196,-1.50000395501635,
-17.4083310499036));
#362857=CARTESIAN_POINT('Ctrl Pts',(1.29904153082129,-0.750001977508173,
-17.3666643832369));
#362858=CARTESIAN_POINT('Ctrl Pts',(1.73205537442839,5.59462936407022E-15,
-17.3249977165702));
#362859=CARTESIAN_POINT('Ctrl Pts',(1.2990415308213,0.750001977508183,-17.2833310499036));
#362860=CARTESIAN_POINT('Ctrl Pts',(0.866027687214198,1.50000395501636,
-17.2416643832369));
#362861=CARTESIAN_POINT('Ctrl Pts',(0.,1.50000395501636,-17.1999977165702));
#362862=CARTESIAN_POINT('Ctrl Pts',(-0.866027687214197,1.50000395501636,
-17.1583310499036));
#362863=CARTESIAN_POINT('Ctrl Pts',(-1.2990415308213,0.750001977508185,
-17.1166643832369));
#362864=CARTESIAN_POINT('Ctrl Pts',(-1.73205537442839,5.90958665837159E-15,
-17.0749977165702));
#362865=CARTESIAN_POINT('Ctrl Pts',(-1.2990415308213,-0.750001977508172,
-17.0333310499036));
#362866=CARTESIAN_POINT('Ctrl Pts',(-0.866027687214197,-1.50000395501635,
-16.9916643832369));
#362867=CARTESIAN_POINT('Ctrl Pts',(-1.83697504221915E-16,-1.50000395501635,
-16.9499977165702));
#362868=CARTESIAN_POINT('Ctrl Pts',(0.866027687214196,-1.50000395501635,
-16.9083310499036));
#362869=CARTESIAN_POINT('Ctrl Pts',(1.29904153082129,-0.750001977508173,
-16.8666643832369));
#362870=CARTESIAN_POINT('Ctrl Pts',(1.73205537442839,5.37608152457707E-15,
-16.8249977165702));
#362871=CARTESIAN_POINT('Ctrl Pts',(1.2990415308213,0.750001977508183,-16.7833310499036));
#362872=CARTESIAN_POINT('Ctrl Pts',(0.866027687214198,1.50000395501636,
-16.7416643832369));
#362873=CARTESIAN_POINT('Ctrl Pts',(0.,1.50000395501636,-16.6999977165702));
#362874=CARTESIAN_POINT('Ctrl Pts',(-0.866027687214197,1.50000395501636,
-16.6583310499036));
#362875=CARTESIAN_POINT('Ctrl Pts',(-1.2990415308213,0.750001977508184,
-16.6166643832369));
#362876=CARTESIAN_POINT('Ctrl Pts',(-1.73205537442839,5.69103881887844E-15,
-16.5749977165702));
#362877=CARTESIAN_POINT('Ctrl Pts',(-1.2990415308213,-0.750001977508173,
-16.5333310499036));
#362878=CARTESIAN_POINT('Ctrl Pts',(-0.866027687214197,-1.50000395501635,
-16.4916643832369));
#362879=CARTESIAN_POINT('Ctrl Pts',(-1.83697504221915E-16,-1.50000395501635,
-16.4499977165702));
#362880=CARTESIAN_POINT('Ctrl Pts',(0.866027687214196,-1.50000395501635,
-16.4083310499036));
#362881=CARTESIAN_POINT('Ctrl Pts',(1.29904153082129,-0.750001977508174,
-16.3666643832369));
#362882=CARTESIAN_POINT('Ctrl Pts',(1.73205537442839,5.15753368508393E-15,
-16.3249977165702));
#362883=CARTESIAN_POINT('Ctrl Pts',(1.2990415308213,0.750001977508183,-16.2833310499036));
#362884=CARTESIAN_POINT('Ctrl Pts',(0.866027687214198,1.50000395501636,
-16.2416643832369));
#362885=CARTESIAN_POINT('Ctrl Pts',(0.,1.50000395501636,-16.1999977165702));
#362886=CARTESIAN_POINT('Ctrl Pts',(-0.866027687214197,1.50000395501636,
-16.1583310499036));
#362887=CARTESIAN_POINT('Ctrl Pts',(-1.2990415308213,0.750001977508184,
-16.1166643832369));
#362888=CARTESIAN_POINT('Ctrl Pts',(-1.73205537442839,5.4724909793853E-15,
-16.0749977165702));
#362889=CARTESIAN_POINT('Ctrl Pts',(-1.2990415308213,-0.750001977508173,
-16.0333310499036));
#362890=CARTESIAN_POINT('Ctrl Pts',(-0.866027687214197,-1.50000395501635,
-15.9916643832369));
#362891=CARTESIAN_POINT('Ctrl Pts',(-1.83697504221915E-16,-1.50000395501635,
-15.9499977165702));
#362892=CARTESIAN_POINT('Ctrl Pts',(0.866027687214196,-1.50000395501635,
-15.9083310499036));
#362893=CARTESIAN_POINT('Ctrl Pts',(1.29904153082129,-0.750001977508174,
-15.8666643832369));
#362894=CARTESIAN_POINT('Ctrl Pts',(1.73205537442839,4.93898584559079E-15,
-15.8249977165702));
#362895=CARTESIAN_POINT('Ctrl Pts',(1.2990415308213,0.750001977508183,-15.7833310499036));
#362896=CARTESIAN_POINT('Ctrl Pts',(0.866027687214198,1.50000395501636,
-15.7416643832369));
#362897=CARTESIAN_POINT('Ctrl Pts',(0.,1.50000395501636,-15.6999977165702));
#362898=CARTESIAN_POINT('Ctrl Pts',(-0.866027687214197,1.50000395501636,
-15.6583310499036));
#362899=CARTESIAN_POINT('Ctrl Pts',(-1.2990415308213,0.750001977508184,
-15.6166643832369));
#362900=CARTESIAN_POINT('Ctrl Pts',(-1.73205537442839,5.25394313989216E-15,
-15.5749977165702));
#362901=CARTESIAN_POINT('Ctrl Pts',(-1.2990415308213,-0.750001977508173,
-15.5333310499036));
#362902=CARTESIAN_POINT('Ctrl Pts',(-0.866027687214197,-1.50000395501635,
-15.4916643832369));
#362903=CARTESIAN_POINT('Ctrl Pts',(-1.83697504221915E-16,-1.50000395501635,
-15.4499977165702));
#362904=CARTESIAN_POINT('Ctrl Pts',(0.866027687214196,-1.50000395501635,
-15.4083310499036));
#362905=CARTESIAN_POINT('Ctrl Pts',(1.29904153082129,-0.750001977508174,
-15.3666643832369));
#362906=CARTESIAN_POINT('Ctrl Pts',(1.73205537442839,4.72043800609765E-15,
-15.3249977165702));
#362907=CARTESIAN_POINT('Ctrl Pts',(1.2990415308213,0.750001977508182,-15.2833310499036));
#362908=CARTESIAN_POINT('Ctrl Pts',(0.866027687214198,1.50000395501636,
-15.2416643832369));
#362909=CARTESIAN_POINT('Ctrl Pts',(0.,1.50000395501636,-15.1999977165702));
#362910=CARTESIAN_POINT('Ctrl Pts',(-0.866027687214197,1.50000395501636,
-15.1583310499036));
#362911=CARTESIAN_POINT('Ctrl Pts',(-1.2990415308213,0.750001977508184,
-15.1166643832369));
#362912=CARTESIAN_POINT('Ctrl Pts',(-1.73205537442839,5.03539530039902E-15,
-15.0749977165702));
#362913=CARTESIAN_POINT('Ctrl Pts',(-1.2990415308213,-0.750001977508173,
-15.0333310499036));
#362914=CARTESIAN_POINT('Ctrl Pts',(-0.866027687214197,-1.50000395501635,
-14.9916643832369));
#362915=CARTESIAN_POINT('Ctrl Pts',(-1.83697504221915E-16,-1.50000395501635,
-14.9499977165702));
#362916=CARTESIAN_POINT('Ctrl Pts',(0.866027687214196,-1.50000395501635,
-14.9083310499036));
#362917=CARTESIAN_POINT('Ctrl Pts',(1.29904153082129,-0.750001977508174,
-14.8666643832369));
#362918=CARTESIAN_POINT('Ctrl Pts',(1.73205537442839,4.50189016660451E-15,
-14.8249977165702));
#362919=CARTESIAN_POINT('Ctrl Pts',(1.2990415308213,0.750001977508182,-14.7833310499036));
#362920=CARTESIAN_POINT('Ctrl Pts',(0.866027687214198,1.50000395501636,
-14.7416643832369));
#362921=CARTESIAN_POINT('Ctrl Pts',(0.,1.50000395501636,-14.6999977165702));
#362922=CARTESIAN_POINT('Ctrl Pts',(-0.866027687214197,1.50000395501636,
-14.6583310499036));
#362923=CARTESIAN_POINT('Ctrl Pts',(-1.2990415308213,0.750001977508183,
-14.6166643832369));
#362924=CARTESIAN_POINT('Ctrl Pts',(-1.73205537442839,4.81684746090588E-15,
-14.5749977165702));
#362925=CARTESIAN_POINT('Ctrl Pts',(-1.2990415308213,-0.750001977508173,
-14.5333310499036));
#362926=CARTESIAN_POINT('Ctrl Pts',(-0.866027687214197,-1.50000395501635,
-14.4916643832369));
#362927=CARTESIAN_POINT('Ctrl Pts',(-1.83697504221915E-16,-1.50000395501635,
-14.4499977165702));
#362928=CARTESIAN_POINT('Ctrl Pts',(0.866027687214196,-1.50000395501635,
-14.4083310499036));
#362929=CARTESIAN_POINT('Ctrl Pts',(1.29904153082129,-0.750001977508174,
-14.3666643832369));
#362930=CARTESIAN_POINT('Ctrl Pts',(1.73205537442839,4.28334232711137E-15,
-14.3249977165702));
#362931=CARTESIAN_POINT('Ctrl Pts',(1.2990415308213,0.750001977508182,-14.2833310499036));
#362932=CARTESIAN_POINT('Ctrl Pts',(0.866027687214198,1.50000395501636,
-14.2416643832369));
#362933=CARTESIAN_POINT('Ctrl Pts',(0.,1.50000395501636,-14.1999977165702));
#362934=CARTESIAN_POINT('Ctrl Pts',(-0.866027687214197,1.50000395501636,
-14.1583310499036));
#362935=CARTESIAN_POINT('Ctrl Pts',(-1.2990415308213,0.750001977508183,
-14.1166643832369));
#362936=CARTESIAN_POINT('Ctrl Pts',(-1.73205537442839,4.59829962141274E-15,
-14.0749977165702));
#362937=CARTESIAN_POINT('Ctrl Pts',(-1.2990415308213,-0.750001977508174,
-14.0333310499036));
#362938=CARTESIAN_POINT('Ctrl Pts',(-0.866027687214197,-1.50000395501635,
-13.9916643832369));
#362939=CARTESIAN_POINT('Ctrl Pts',(-1.83697504221915E-16,-1.50000395501635,
-13.9499977165702));
#362940=CARTESIAN_POINT('Ctrl Pts',(0.866027687214196,-1.50000395501635,
-13.9083310499036));
#362941=CARTESIAN_POINT('Ctrl Pts',(1.29904153082129,-0.750001977508175,
-13.8666643832369));
#362942=CARTESIAN_POINT('Ctrl Pts',(1.73205537442839,4.06479448761823E-15,
-13.8249977165702));
#362943=CARTESIAN_POINT('Ctrl Pts',(1.2990415308213,0.750001977508182,-13.7833310499036));
#362944=CARTESIAN_POINT('Ctrl Pts',(0.866027687214198,1.50000395501636,
-13.7416643832369));
#362945=CARTESIAN_POINT('Ctrl Pts',(0.,1.50000395501636,-13.6999977165702));
#362946=CARTESIAN_POINT('Ctrl Pts',(-0.866027687214197,1.50000395501636,
-13.6583310499036));
#362947=CARTESIAN_POINT('Ctrl Pts',(-1.2990415308213,0.750001977508183,
-13.6166643832369));
#362948=CARTESIAN_POINT('Ctrl Pts',(-1.73205537442839,4.3797517819196E-15,
-13.5749977165702));
#362949=CARTESIAN_POINT('Ctrl Pts',(-1.2990415308213,-0.750001977508174,
-13.5333310499036));
#362950=CARTESIAN_POINT('Ctrl Pts',(-0.866027687214197,-1.50000395501635,
-13.4916643832369));
#362951=CARTESIAN_POINT('Ctrl Pts',(-1.83697504221915E-16,-1.50000395501635,
-13.4499977165702));
#362952=CARTESIAN_POINT('Ctrl Pts',(0.866027687214196,-1.50000395501635,
-13.4083310499036));
#362953=CARTESIAN_POINT('Ctrl Pts',(1.29904153082129,-0.750001977508175,
-13.3666643832369));
#362954=CARTESIAN_POINT('Ctrl Pts',(1.73205537442839,3.84624664812509E-15,
-13.3249977165702));
#362955=CARTESIAN_POINT('Ctrl Pts',(1.2990415308213,0.750001977508181,-13.2833310499036));
#362956=CARTESIAN_POINT('Ctrl Pts',(0.866027687214198,1.50000395501636,
-13.2416643832369));
#362957=CARTESIAN_POINT('Ctrl Pts',(0.,1.50000395501636,-13.1999977165702));
#362958=CARTESIAN_POINT('Ctrl Pts',(-0.866027687214197,1.50000395501636,
-13.1583310499036));
#362959=CARTESIAN_POINT('Ctrl Pts',(-1.2990415308213,0.750001977508183,
-13.1166643832369));
#362960=CARTESIAN_POINT('Ctrl Pts',(-1.73205537442839,4.16120394242646E-15,
-13.0749977165702));
#362961=CARTESIAN_POINT('Ctrl Pts',(-1.2990415308213,-0.750001977508174,
-13.0333310499036));
#362962=CARTESIAN_POINT('Ctrl Pts',(-0.866027687214197,-1.50000395501635,
-12.9916643832369));
#362963=CARTESIAN_POINT('Ctrl Pts',(-1.83697504221915E-16,-1.50000395501635,
-12.9499977165702));
#362964=CARTESIAN_POINT('Ctrl Pts',(0.866027687214196,-1.50000395501635,
-12.9083310499036));
#362965=CARTESIAN_POINT('Ctrl Pts',(1.29904153082129,-0.750001977508175,
-12.8666643832369));
#362966=CARTESIAN_POINT('Ctrl Pts',(1.73205537442839,3.62769880863194E-15,
-12.8249977165702));
#362967=CARTESIAN_POINT('Ctrl Pts',(1.2990415308213,0.750001977508181,-12.7833310499036));
#362968=CARTESIAN_POINT('Ctrl Pts',(0.866027687214198,1.50000395501636,
-12.7416643832369));
#362969=CARTESIAN_POINT('Ctrl Pts',(0.,1.50000395501636,-12.6999977165702));
#362970=CARTESIAN_POINT('Ctrl Pts',(-0.866027687214197,1.50000395501636,
-12.6583310499036));
#362971=CARTESIAN_POINT('Ctrl Pts',(-1.2990415308213,0.750001977508183,
-12.6166643832369));
#362972=CARTESIAN_POINT('Ctrl Pts',(-1.73205537442839,3.94265610293331E-15,
-12.5749977165702));
#362973=CARTESIAN_POINT('Ctrl Pts',(-1.2990415308213,-0.750001977508174,
-12.5333310499036));
#362974=CARTESIAN_POINT('Ctrl Pts',(-0.866027687214197,-1.50000395501635,
-12.4916643832369));
#362975=CARTESIAN_POINT('Ctrl Pts',(-1.83697504221915E-16,-1.50000395501635,
-12.4499977165702));
#362976=CARTESIAN_POINT('Ctrl Pts',(0.866027687214196,-1.50000395501635,
-12.4083310499036));
#362977=CARTESIAN_POINT('Ctrl Pts',(1.29904153082129,-0.750001977508175,
-12.3666643832369));
#362978=CARTESIAN_POINT('Ctrl Pts',(1.73205537442839,3.4091509691388E-15,
-12.3249977165702));
#362979=CARTESIAN_POINT('Ctrl Pts',(1.2990415308213,0.750001977508181,-12.2833310499036));
#362980=CARTESIAN_POINT('Ctrl Pts',(0.866027687214198,1.50000395501636,
-12.2416643832369));
#362981=CARTESIAN_POINT('Ctrl Pts',(0.,1.50000395501636,-12.1999977165702));
#362982=CARTESIAN_POINT('Ctrl Pts',(-0.866027687214197,1.50000395501636,
-12.1583310499036));
#362983=CARTESIAN_POINT('Ctrl Pts',(-1.2990415308213,0.750001977508182,
-12.1166643832369));
#362984=CARTESIAN_POINT('Ctrl Pts',(-1.73205537442839,3.72410826344017E-15,
-12.0749977165702));
#362985=CARTESIAN_POINT('Ctrl Pts',(-1.2990415308213,-0.750001977508174,
-12.0333310499036));
#362986=CARTESIAN_POINT('Ctrl Pts',(-0.866027687214197,-1.50000395501635,
-11.9916643832369));
#362987=CARTESIAN_POINT('Ctrl Pts',(-1.83697504221915E-16,-1.50000395501635,
-11.9499977165702));
#362988=CARTESIAN_POINT('Ctrl Pts',(0.866027687214196,-1.50000395501635,
-11.9083310499036));
#362989=CARTESIAN_POINT('Ctrl Pts',(1.29904153082129,-0.750001977508176,
-11.8666643832369));
#362990=CARTESIAN_POINT('Ctrl Pts',(1.73205537442839,3.19060312964566E-15,
-11.8249977165702));
#362991=CARTESIAN_POINT('Ctrl Pts',(1.2990415308213,0.750001977508181,-11.7833310499036));
#362992=CARTESIAN_POINT('Ctrl Pts',(0.866027687214198,1.50000395501636,
-11.7416643832369));
#362993=CARTESIAN_POINT('Ctrl Pts',(0.,1.50000395501636,-11.6999977165702));
#362994=CARTESIAN_POINT('Ctrl Pts',(-0.866027687214197,1.50000395501636,
-11.6583310499036));
#362995=CARTESIAN_POINT('Ctrl Pts',(-1.2990415308213,0.750001977508182,
-11.6166643832369));
#362996=CARTESIAN_POINT('Ctrl Pts',(-1.73205537442839,3.50556042394703E-15,
-11.5749977165702));
#362997=CARTESIAN_POINT('Ctrl Pts',(-1.2990415308213,-0.750001977508175,
-11.5333310499036));
#362998=CARTESIAN_POINT('Ctrl Pts',(-0.866027687214197,-1.50000395501635,
-11.4916643832369));
#362999=CARTESIAN_POINT('Ctrl Pts',(-1.83697504221915E-16,-1.50000395501635,
-11.4499977165702));
#363000=CARTESIAN_POINT('Ctrl Pts',(0.866027687214196,-1.50000395501635,
-11.4083310499036));
#363001=CARTESIAN_POINT('Ctrl Pts',(1.29904153082129,-0.750001977508176,
-11.3666643832369));
#363002=CARTESIAN_POINT('Ctrl Pts',(1.73205537442839,2.97205529015252E-15,
-11.3249977165702));
#363003=CARTESIAN_POINT('Ctrl Pts',(1.2990415308213,0.750001977508181,-11.2833310499036));
#363004=CARTESIAN_POINT('Ctrl Pts',(0.866027687214198,1.50000395501636,
-11.2416643832369));
#363005=CARTESIAN_POINT('Ctrl Pts',(0.,1.50000395501636,-11.1999977165702));
#363006=CARTESIAN_POINT('Ctrl Pts',(-0.866027687214197,1.50000395501636,
-11.1583310499036));
#363007=CARTESIAN_POINT('Ctrl Pts',(-1.2990415308213,0.750001977508182,
-11.1166643832369));
#363008=CARTESIAN_POINT('Ctrl Pts',(-1.73205537442839,3.28701258445389E-15,
-11.0749977165702));
#363009=CARTESIAN_POINT('Ctrl Pts',(-1.2990415308213,-0.750001977508175,
-11.0333310499036));
#363010=CARTESIAN_POINT('Ctrl Pts',(-0.866027687214197,-1.50000395501635,
-10.9916643832369));
#363011=CARTESIAN_POINT('Ctrl Pts',(-1.83697504221915E-16,-1.50000395501635,
-10.9499977165702));
#363012=CARTESIAN_POINT('Ctrl Pts',(0.866027687214196,-1.50000395501635,
-10.9083310499036));
#363013=CARTESIAN_POINT('Ctrl Pts',(1.29904153082129,-0.750001977508176,
-10.8666643832369));
#363014=CARTESIAN_POINT('Ctrl Pts',(1.73205537442839,2.75350745065938E-15,
-10.8249977165702));
#363015=CARTESIAN_POINT('Ctrl Pts',(1.2990415308213,0.75000197750818,-10.7833310499036));
#363016=CARTESIAN_POINT('Ctrl Pts',(0.866027687214198,1.50000395501636,
-10.7416643832369));
#363017=CARTESIAN_POINT('Ctrl Pts',(0.,1.50000395501636,-10.6999977165702));
#363018=CARTESIAN_POINT('Ctrl Pts',(-0.866027687214197,1.50000395501636,
-10.6583310499036));
#363019=CARTESIAN_POINT('Ctrl Pts',(-1.2990415308213,0.750001977508182,
-10.6166643832369));
#363020=CARTESIAN_POINT('Ctrl Pts',(-1.73205537442839,3.06846474496075E-15,
-10.5749977165702));
#363021=CARTESIAN_POINT('Ctrl Pts',(-1.2990415308213,-0.750001977508175,
-10.5333310499036));
#363022=CARTESIAN_POINT('Ctrl Pts',(-0.866027687214197,-1.50000395501635,
-10.4916643832369));
#363023=CARTESIAN_POINT('Ctrl Pts',(-1.83697504221915E-16,-1.50000395501635,
-10.4499977165702));
#363024=CARTESIAN_POINT('Ctrl Pts',(0.866027687214196,-1.50000395501635,
-10.4083310499036));
#363025=CARTESIAN_POINT('Ctrl Pts',(1.29904153082129,-0.750001977508176,
-10.3666643832369));
#363026=CARTESIAN_POINT('Ctrl Pts',(1.73205537442839,2.53495961116624E-15,
-10.3249977165702));
#363027=CARTESIAN_POINT('Ctrl Pts',(1.2990415308213,0.75000197750818,-10.2833310499036));
#363028=CARTESIAN_POINT('Ctrl Pts',(0.866027687214198,1.50000395501636,
-10.2416643832369));
#363029=CARTESIAN_POINT('Ctrl Pts',(0.,1.50000395501636,-10.1999977165702));
#363030=CARTESIAN_POINT('Ctrl Pts',(-0.866027687214197,1.50000395501636,
-10.1583310499036));
#363031=CARTESIAN_POINT('Ctrl Pts',(-1.2990415308213,0.750001977508181,
-10.1166643832369));
#363032=CARTESIAN_POINT('Ctrl Pts',(-1.73205537442839,2.84991690546761E-15,
-10.0749977165702));
#363033=CARTESIAN_POINT('Ctrl Pts',(-1.2990415308213,-0.750001977508175,
-10.0333310499036));
#363034=CARTESIAN_POINT('Ctrl Pts',(-0.866027687214197,-1.50000395501635,
-9.99166438323691));
#363035=CARTESIAN_POINT('Ctrl Pts',(-1.83697504221915E-16,-1.50000395501635,
-9.94999771657024));
#363036=CARTESIAN_POINT('Ctrl Pts',(0.866027687214196,-1.50000395501635,
-9.90833104990357));
#363037=CARTESIAN_POINT('Ctrl Pts',(1.29904153082129,-0.750001977508177,
-9.86666438323691));
#363038=CARTESIAN_POINT('Ctrl Pts',(1.73205537442839,2.3164117716731E-15,
-9.82499771657024));
#363039=CARTESIAN_POINT('Ctrl Pts',(1.2990415308213,0.75000197750818,-9.78333104990358));
#363040=CARTESIAN_POINT('Ctrl Pts',(0.866027687214198,1.50000395501636,
-9.74166438323691));
#363041=CARTESIAN_POINT('Ctrl Pts',(0.,1.50000395501636,-9.69999771657024));
#363042=CARTESIAN_POINT('Ctrl Pts',(-0.866027687214197,1.50000395501636,
-9.65833104990358));
#363043=CARTESIAN_POINT('Ctrl Pts',(-1.2990415308213,0.750001977508181,
-9.61666438323691));
#363044=CARTESIAN_POINT('Ctrl Pts',(-1.73205537442839,2.63136906597447E-15,
-9.57499771657024));
#363045=CARTESIAN_POINT('Ctrl Pts',(-1.2990415308213,-0.750001977508176,
-9.53333104990358));
#363046=CARTESIAN_POINT('Ctrl Pts',(-0.866027687214197,-1.50000395501635,
-9.49166438323691));
#363047=CARTESIAN_POINT('Ctrl Pts',(-1.83697504221915E-16,-1.50000395501635,
-9.44999771657024));
#363048=CARTESIAN_POINT('Ctrl Pts',(0.866027687214196,-1.50000395501635,
-9.40833104990358));
#363049=CARTESIAN_POINT('Ctrl Pts',(1.29904153082129,-0.750001977508177,
-9.36666438323691));
#363050=CARTESIAN_POINT('Ctrl Pts',(1.73205537442839,2.09786393217996E-15,
-9.32499771657024));
#363051=CARTESIAN_POINT('Ctrl Pts',(1.2990415308213,0.75000197750818,-9.28333104990358));
#363052=CARTESIAN_POINT('Ctrl Pts',(0.866027687214198,1.50000395501636,
-9.24166438323691));
#363053=CARTESIAN_POINT('Ctrl Pts',(0.,1.50000395501636,-9.19999771657024));
#363054=CARTESIAN_POINT('Ctrl Pts',(-0.866027687214197,1.50000395501636,
-9.15833104990357));
#363055=CARTESIAN_POINT('Ctrl Pts',(-1.2990415308213,0.750001977508181,
-9.11666438323691));
#363056=CARTESIAN_POINT('Ctrl Pts',(-1.73205537442839,2.41282122648133E-15,
-9.07499771657024));
#363057=CARTESIAN_POINT('Ctrl Pts',(-1.2990415308213,-0.750001977508176,
-9.03333104990358));
#363058=CARTESIAN_POINT('Ctrl Pts',(-0.866027687214197,-1.50000395501635,
-8.99166438323691));
#363059=CARTESIAN_POINT('Ctrl Pts',(-1.83697504221915E-16,-1.50000395501635,
-8.94999771657024));
#363060=CARTESIAN_POINT('Ctrl Pts',(0.866027687214196,-1.50000395501635,
-8.90833104990357));
#363061=CARTESIAN_POINT('Ctrl Pts',(1.29904153082129,-0.750001977508177,
-8.86666438323691));
#363062=CARTESIAN_POINT('Ctrl Pts',(1.73205537442839,1.87931609268682E-15,
-8.82499771657024));
#363063=CARTESIAN_POINT('Ctrl Pts',(1.2990415308213,0.750001977508179,-8.78333104990358));
#363064=CARTESIAN_POINT('Ctrl Pts',(0.866027687214198,1.50000395501636,
-8.74166438323691));
#363065=CARTESIAN_POINT('Ctrl Pts',(0.,1.50000395501636,-8.69999771657024));
#363066=CARTESIAN_POINT('Ctrl Pts',(-0.866027687214197,1.50000395501636,
-8.65833104990357));
#363067=CARTESIAN_POINT('Ctrl Pts',(-1.2990415308213,0.750001977508181,
-8.61666438323691));
#363068=CARTESIAN_POINT('Ctrl Pts',(-1.73205537442839,2.19427338698818E-15,
-8.57499771657024));
#363069=CARTESIAN_POINT('Ctrl Pts',(-1.2990415308213,-0.750001977508176,
-8.53333104990357));
#363070=CARTESIAN_POINT('Ctrl Pts',(-0.866027687214197,-1.50000395501635,
-8.49166438323691));
#363071=CARTESIAN_POINT('Ctrl Pts',(-1.83697504221915E-16,-1.50000395501635,
-8.44999771657024));
#363072=CARTESIAN_POINT('Ctrl Pts',(0.866027687214196,-1.50000395501635,
-8.40833104990357));
#363073=CARTESIAN_POINT('Ctrl Pts',(1.29904153082129,-0.750001977508177,
-8.36666438323691));
#363074=CARTESIAN_POINT('Ctrl Pts',(1.73205537442839,1.66076825319367E-15,
-8.32499771657024));
#363075=CARTESIAN_POINT('Ctrl Pts',(1.2990415308213,0.750001977508179,-8.28333104990357));
#363076=CARTESIAN_POINT('Ctrl Pts',(0.866027687214198,1.50000395501636,
-8.24166438323691));
#363077=CARTESIAN_POINT('Ctrl Pts',(0.,1.50000395501636,-8.19999771657024));
#363078=CARTESIAN_POINT('Ctrl Pts',(-0.866027687214197,1.50000395501636,
-8.15833104990357));
#363079=CARTESIAN_POINT('Ctrl Pts',(-1.2990415308213,0.750001977508181,
-8.11666438323691));
#363080=CARTESIAN_POINT('Ctrl Pts',(-1.73205537442839,1.97572554749504E-15,
-8.07499771657024));
#363081=CARTESIAN_POINT('Ctrl Pts',(-1.2990415308213,-0.750001977508176,
-8.03333104990357));
#363082=CARTESIAN_POINT('Ctrl Pts',(-0.866027687214197,-1.50000395501635,
-7.99166438323691));
#363083=CARTESIAN_POINT('Ctrl Pts',(-1.83697504221915E-16,-1.50000395501636,
-7.94999771657024));
#363084=CARTESIAN_POINT('Ctrl Pts',(0.866027687214196,-1.50000395501636,
-7.90833104990357));
#363085=CARTESIAN_POINT('Ctrl Pts',(1.29904153082129,-0.750001977508177,
-7.86666438323691));
#363086=CARTESIAN_POINT('Ctrl Pts',(1.73205537442839,1.44222041370053E-15,
-7.82499771657024));
#363087=CARTESIAN_POINT('Ctrl Pts',(1.2990415308213,0.750001977508179,-7.78333104990358));
#363088=CARTESIAN_POINT('Ctrl Pts',(0.866027687214198,1.50000395501636,
-7.74166438323691));
#363089=CARTESIAN_POINT('Ctrl Pts',(0.,1.50000395501636,-7.69999771657024));
#363090=CARTESIAN_POINT('Ctrl Pts',(-0.866027687214197,1.50000395501636,
-7.65833104990358));
#363091=CARTESIAN_POINT('Ctrl Pts',(-1.2990415308213,0.75000197750818,-7.61666438323691));
#363092=CARTESIAN_POINT('Ctrl Pts',(-1.73205537442839,1.7571777080019E-15,
-7.57499771657024));
#363093=CARTESIAN_POINT('Ctrl Pts',(-1.2990415308213,-0.750001977508177,
-7.53333104990358));
#363094=CARTESIAN_POINT('Ctrl Pts',(-0.866027687214197,-1.50000395501635,
-7.49166438323691));
#363095=CARTESIAN_POINT('Ctrl Pts',(-1.83697504221915E-16,-1.50000395501636,
-7.44999771657024));
#363096=CARTESIAN_POINT('Ctrl Pts',(0.866027687214196,-1.50000395501636,
-7.40833104990358));
#363097=CARTESIAN_POINT('Ctrl Pts',(1.29904153082129,-0.750001977508178,
-7.36666438323691));
#363098=CARTESIAN_POINT('Ctrl Pts',(1.73205537442839,1.22367257420739E-15,
-7.32499771657024));
#363099=CARTESIAN_POINT('Ctrl Pts',(1.2990415308213,0.750001977508179,-7.28333104990358));
#363100=CARTESIAN_POINT('Ctrl Pts',(0.866027687214198,1.50000395501636,
-7.24166438323691));
#363101=CARTESIAN_POINT('Ctrl Pts',(0.,1.50000395501636,-7.19999771657024));
#363102=CARTESIAN_POINT('Ctrl Pts',(-0.866027687214197,1.50000395501636,
-7.15833104990358));
#363103=CARTESIAN_POINT('Ctrl Pts',(-1.2990415308213,0.75000197750818,-7.11666438323691));
#363104=CARTESIAN_POINT('Ctrl Pts',(-1.73205537442839,1.53862986850876E-15,
-7.07499771657024));
#363105=CARTESIAN_POINT('Ctrl Pts',(-1.2990415308213,-0.750001977508177,
-7.03333104990358));
#363106=CARTESIAN_POINT('Ctrl Pts',(-0.866027687214197,-1.50000395501635,
-6.99166438323691));
#363107=CARTESIAN_POINT('Ctrl Pts',(-1.83697504221915E-16,-1.50000395501636,
-6.94999771657024));
#363108=CARTESIAN_POINT('Ctrl Pts',(0.866027687214196,-1.50000395501636,
-6.90833104990358));
#363109=CARTESIAN_POINT('Ctrl Pts',(1.29904153082129,-0.750001977508178,
-6.86666438323691));
#363110=CARTESIAN_POINT('Ctrl Pts',(1.73205537442839,1.00512473471425E-15,
-6.82499771657024));
#363111=CARTESIAN_POINT('Ctrl Pts',(1.2990415308213,0.750001977508179,-6.78333104990358));
#363112=CARTESIAN_POINT('Ctrl Pts',(0.866027687214198,1.50000395501636,
-6.74166438323691));
#363113=CARTESIAN_POINT('Ctrl Pts',(0.,1.50000395501636,-6.69999771657024));
#363114=CARTESIAN_POINT('Ctrl Pts',(-0.866027687214197,1.50000395501636,
-6.65833104990358));
#363115=CARTESIAN_POINT('Ctrl Pts',(-1.2990415308213,0.75000197750818,-6.61666438323691));
#363116=CARTESIAN_POINT('Ctrl Pts',(-1.73205537442839,1.32008202901562E-15,
-6.57499771657024));
#363117=CARTESIAN_POINT('Ctrl Pts',(-1.2990415308213,-0.750001977508177,
-6.53333104990357));
#363118=CARTESIAN_POINT('Ctrl Pts',(-0.866027687214197,-1.50000395501635,
-6.49166438323691));
#363119=CARTESIAN_POINT('Ctrl Pts',(-1.83697504221915E-16,-1.50000395501636,
-6.44999771657024));
#363120=CARTESIAN_POINT('Ctrl Pts',(0.866027687214196,-1.50000395501636,
-6.40833104990358));
#363121=CARTESIAN_POINT('Ctrl Pts',(1.29904153082129,-0.750001977508178,
-6.36666438323691));
#363122=CARTESIAN_POINT('Ctrl Pts',(1.73205537442839,7.86576895221109E-16,
-6.32499771657024));
#363123=CARTESIAN_POINT('Ctrl Pts',(1.2990415308213,0.750001977508178,-6.28333104990357));
#363124=CARTESIAN_POINT('Ctrl Pts',(0.866027687214198,1.50000395501636,
-6.24166438323691));
#363125=CARTESIAN_POINT('Ctrl Pts',(0.,1.50000395501636,-6.19999771657024));
#363126=CARTESIAN_POINT('Ctrl Pts',(-0.866027687214197,1.50000395501636,
-6.15833104990357));
#363127=CARTESIAN_POINT('Ctrl Pts',(-1.2990415308213,0.75000197750818,-6.11666438323691));
#363128=CARTESIAN_POINT('Ctrl Pts',(-1.73205537442839,1.10153418952248E-15,
-6.07499771657024));
#363129=CARTESIAN_POINT('Ctrl Pts',(-1.2990415308213,-0.750001977508177,
-6.03333104990357));
#363130=CARTESIAN_POINT('Ctrl Pts',(-0.866027687214197,-1.50000395501636,
-5.99166438323691));
#363131=CARTESIAN_POINT('Ctrl Pts',(-1.83697504221915E-16,-1.50000395501636,
-5.94999771657024));
#363132=CARTESIAN_POINT('Ctrl Pts',(0.866027687214196,-1.50000395501636,
-5.90833104990358));
#363133=CARTESIAN_POINT('Ctrl Pts',(1.29904153082129,-0.750001977508178,
-5.86666438323691));
#363134=CARTESIAN_POINT('Ctrl Pts',(1.73205537442839,5.68029055727967E-16,
-5.82499771657024));
#363135=CARTESIAN_POINT('Ctrl Pts',(1.2990415308213,0.750001977508178,-5.78333104990358));
#363136=CARTESIAN_POINT('Ctrl Pts',(0.866027687214198,1.50000395501636,
-5.74166438323691));
#363137=CARTESIAN_POINT('Ctrl Pts',(0.,1.50000395501636,-5.69999771657024));
#363138=CARTESIAN_POINT('Ctrl Pts',(-0.866027687214197,1.50000395501636,
-5.65833104990357));
#363139=CARTESIAN_POINT('Ctrl Pts',(-1.2990415308213,0.750001977508179,
-5.61666438323691));
#363140=CARTESIAN_POINT('Ctrl Pts',(-1.73205537442839,8.82986350029337E-16,
-5.57499771657024));
#363141=CARTESIAN_POINT('Ctrl Pts',(-1.2990415308213,-0.750001977508177,
-5.53333104990358));
#363142=CARTESIAN_POINT('Ctrl Pts',(-0.866027687214197,-1.50000395501636,
-5.49166438323691));
#363143=CARTESIAN_POINT('Ctrl Pts',(-1.83697504221915E-16,-1.50000395501636,
-5.44999771657024));
#363144=CARTESIAN_POINT('Ctrl Pts',(0.866027687214196,-1.50000395501636,
-5.40833104990357));
#363145=CARTESIAN_POINT('Ctrl Pts',(1.29904153082129,-0.750001977508178,
-5.36666438323691));
#363146=CARTESIAN_POINT('Ctrl Pts',(1.73205537442839,3.49481216234826E-16,
-5.32499771657024));
#363147=CARTESIAN_POINT('Ctrl Pts',(1.2990415308213,0.750001977508178,-5.28333104990358));
#363148=CARTESIAN_POINT('Ctrl Pts',(0.866027687214198,1.50000395501636,
-5.24166438323691));
#363149=CARTESIAN_POINT('Ctrl Pts',(0.,1.50000395501636,-5.19999771657024));
#363150=CARTESIAN_POINT('Ctrl Pts',(-0.866027687214197,1.50000395501636,
-5.15833104990357));
#363151=CARTESIAN_POINT('Ctrl Pts',(-1.2990415308213,0.750001977508179,
-5.11666438323691));
#363152=CARTESIAN_POINT('Ctrl Pts',(-1.73205537442839,6.64438510536197E-16,
-5.07499771657024));
#363153=CARTESIAN_POINT('Ctrl Pts',(-1.2990415308213,-0.750001977508178,
-5.03333104990357));
#363154=CARTESIAN_POINT('Ctrl Pts',(-0.866027687214197,-1.50000395501636,
-4.99166438323691));
#363155=CARTESIAN_POINT('Ctrl Pts',(-1.83697504221915E-16,-1.50000395501636,
-4.94999771657024));
#363156=CARTESIAN_POINT('Ctrl Pts',(0.866027687214196,-1.50000395501636,
-4.90833104990357));
#363157=CARTESIAN_POINT('Ctrl Pts',(1.29904153082129,-0.750001977508179,
-4.86666438323691));
#363158=CARTESIAN_POINT('Ctrl Pts',(1.73205537442839,1.30933376741685E-16,
-4.82499771657024));
#363159=CARTESIAN_POINT('Ctrl Pts',(1.2990415308213,0.750001977508178,-4.78333104990357));
#363160=CARTESIAN_POINT('Ctrl Pts',(0.866027687214198,1.50000395501636,
-4.74166438323691));
#363161=CARTESIAN_POINT('Ctrl Pts',(0.,1.50000395501636,-4.69999771657024));
#363162=CARTESIAN_POINT('Ctrl Pts',(-0.866027687214197,1.50000395501636,
-4.65833104990357));
#363163=CARTESIAN_POINT('Ctrl Pts',(-1.2990415308213,0.750001977508179,
-4.61666438323691));
#363164=CARTESIAN_POINT('Ctrl Pts',(-1.73205537442839,4.45890671043056E-16,
-4.57499771657024));
#363165=CARTESIAN_POINT('Ctrl Pts',(-1.2990415308213,-0.750001977508178,
-4.53333104990357));
#363166=CARTESIAN_POINT('Ctrl Pts',(-0.866027687214197,-1.50000395501636,
-4.49166438323691));
#363167=CARTESIAN_POINT('Ctrl Pts',(-1.83697504221915E-16,-1.50000395501636,
-4.44999771657024));
#363168=CARTESIAN_POINT('Ctrl Pts',(0.866027687214196,-1.50000395501636,
-4.40833104990357));
#363169=CARTESIAN_POINT('Ctrl Pts',(1.29904153082129,-0.750001977508179,
-4.36666438323691));
#363170=CARTESIAN_POINT('Ctrl Pts',(1.73205537442839,-8.76144627514565E-17,
-4.32499771657024));
#363171=CARTESIAN_POINT('Ctrl Pts',(1.2990415308213,0.750001977508178,-4.28333104990357));
#363172=CARTESIAN_POINT('Ctrl Pts',(0.866027687214198,1.50000395501636,
-4.24166438323691));
#363173=CARTESIAN_POINT('Ctrl Pts',(0.,1.50000395501636,-4.19999771657024));
#363174=CARTESIAN_POINT('Ctrl Pts',(-0.866027687214197,1.50000395501636,
-4.15833104990358));
#363175=CARTESIAN_POINT('Ctrl Pts',(-1.2990415308213,0.750001977508179,
-4.11666438323691));
#363176=CARTESIAN_POINT('Ctrl Pts',(-1.73205537442839,2.27342831549914E-16,
-4.07499771657024));
#363177=CARTESIAN_POINT('Ctrl Pts',(-1.2990415308213,-0.750001977508178,
-4.03333104990358));
#363178=CARTESIAN_POINT('Ctrl Pts',(-0.866027687214197,-1.50000395501636,
-3.99166438323691));
#363179=CARTESIAN_POINT('Ctrl Pts',(-1.83697504221915E-16,-1.50000395501636,
-3.94999771657024));
#363180=CARTESIAN_POINT('Ctrl Pts',(0.866027687214196,-1.50000395501636,
-3.90833104990358));
#363181=CARTESIAN_POINT('Ctrl Pts',(1.29904153082129,-0.750001977508179,
-3.86666438323691));
#363182=CARTESIAN_POINT('Ctrl Pts',(1.73205537442839,-3.06162302244598E-16,
-3.82499771657024));
#363183=CARTESIAN_POINT('Ctrl Pts',(1.2990415308213,0.750001977508177,-3.78333104990357));
#363184=CARTESIAN_POINT('Ctrl Pts',(0.866027687214198,1.50000395501636,
-3.74166438323691));
#363185=CARTESIAN_POINT('Ctrl Pts',(0.,1.50000395501636,-3.69999771657024));
#363186=CARTESIAN_POINT('Ctrl Pts',(-0.866027687214197,1.50000395501636,
-3.65833104990357));
#363187=CARTESIAN_POINT('Ctrl Pts',(-1.2990415308213,0.750001977508179,
-3.61666438323691));
#363188=CARTESIAN_POINT('Ctrl Pts',(-1.73205537442839,8.79499205677354E-18,
-3.57499771657024));
#363189=CARTESIAN_POINT('Ctrl Pts',(-1.2990415308213,-0.750001977508178,
-3.53333104990357));
#363190=CARTESIAN_POINT('Ctrl Pts',(-0.866027687214197,-1.50000395501636,
-3.49166438323691));
#363191=CARTESIAN_POINT('Ctrl Pts',(-1.83697504221915E-16,-1.50000395501636,
-3.44999771657024));
#363192=CARTESIAN_POINT('Ctrl Pts',(0.866027687214196,-1.50000395501636,
-3.40833104990357));
#363193=CARTESIAN_POINT('Ctrl Pts',(1.29904153082129,-0.750001977508179,
-3.36666438323691));
#363194=CARTESIAN_POINT('Ctrl Pts',(1.73205537442839,-5.24710141737739E-16,
-3.32499771657024));
#363195=CARTESIAN_POINT('Ctrl Pts',(1.2990415308213,0.750001977508177,-3.28333104990357));
#363196=CARTESIAN_POINT('Ctrl Pts',(0.866027687214198,1.50000395501636,
-3.24166438323691));
#363197=CARTESIAN_POINT('Ctrl Pts',(0.,1.50000395501636,-3.19999771657024));
#363198=CARTESIAN_POINT('Ctrl Pts',(-0.866027687214197,1.50000395501636,
-3.15833104990357));
#363199=CARTESIAN_POINT('Ctrl Pts',(-1.2990415308213,0.750001977508178,
-3.11666438323691));
#363200=CARTESIAN_POINT('Ctrl Pts',(-1.73205537442839,-2.09752847436368E-16,
-3.07499771657024));
#363201=CARTESIAN_POINT('Ctrl Pts',(-1.2990415308213,-0.750001977508178,
-3.03333104990357));
#363202=CARTESIAN_POINT('Ctrl Pts',(-0.866027687214197,-1.50000395501636,
-2.99166438323691));
#363203=CARTESIAN_POINT('Ctrl Pts',(-1.83697504221915E-16,-1.50000395501636,
-2.94999771657024));
#363204=CARTESIAN_POINT('Ctrl Pts',(0.866027687214196,-1.50000395501636,
-2.90833104990357));
#363205=CARTESIAN_POINT('Ctrl Pts',(1.29904153082129,-0.750001977508179,
-2.86666438323691));
#363206=CARTESIAN_POINT('Ctrl Pts',(1.73205537442839,-7.4325798123088E-16,
-2.82499771657024));
#363207=CARTESIAN_POINT('Ctrl Pts',(1.2990415308213,0.750001977508177,-2.78333104990357));
#363208=CARTESIAN_POINT('Ctrl Pts',(0.866027687214198,1.50000395501636,
-2.74166438323691));
#363209=CARTESIAN_POINT('Ctrl Pts',(0.,1.50000395501636,-2.69999771657024));
#363210=CARTESIAN_POINT('Ctrl Pts',(-0.866027687214197,1.50000395501636,
-2.65833104990357));
#363211=CARTESIAN_POINT('Ctrl Pts',(-1.2990415308213,0.750001977508178,
-2.61666438323691));
#363212=CARTESIAN_POINT('Ctrl Pts',(-1.73205537442839,-4.28300686929509E-16,
-2.57499771657024));
#363213=CARTESIAN_POINT('Ctrl Pts',(-1.2990415308213,-0.750001977508179,
-2.53333104990357));
#363214=CARTESIAN_POINT('Ctrl Pts',(-0.866027687214197,-1.50000395501636,
-2.49166438323691));
#363215=CARTESIAN_POINT('Ctrl Pts',(-1.83697504221915E-16,-1.50000395501636,
-2.44999771657024));
#363216=CARTESIAN_POINT('Ctrl Pts',(0.866027687214196,-1.50000395501636,
-2.40833104990357));
#363217=CARTESIAN_POINT('Ctrl Pts',(1.29904153082129,-0.75000197750818,
-2.36666438323691));
#363218=CARTESIAN_POINT('Ctrl Pts',(1.73205537442839,-9.61805820724022E-16,
-2.32499771657024));
#363219=CARTESIAN_POINT('Ctrl Pts',(1.2990415308213,0.750001977508177,-2.28333104990357));
#363220=CARTESIAN_POINT('Ctrl Pts',(0.866027687214198,1.50000395501636,
-2.24166438323691));
#363221=CARTESIAN_POINT('Ctrl Pts',(0.,1.50000395501636,-2.19999771657024));
#363222=CARTESIAN_POINT('Ctrl Pts',(-0.866027687214197,1.50000395501636,
-2.15833104990357));
#363223=CARTESIAN_POINT('Ctrl Pts',(-1.2990415308213,0.750001977508178,
-2.11666438323691));
#363224=CARTESIAN_POINT('Ctrl Pts',(-1.73205537442839,-6.46848526422651E-16,
-2.07499771657024));
#363225=CARTESIAN_POINT('Ctrl Pts',(-1.2990415308213,-0.750001977508179,
-2.03333104990357));
#363226=CARTESIAN_POINT('Ctrl Pts',(-0.866027687214197,-1.50000395501636,
-1.99166438323691));
#363227=CARTESIAN_POINT('Ctrl Pts',(-1.83697504221915E-16,-1.50000395501636,
-1.94999771657024));
#363228=CARTESIAN_POINT('Ctrl Pts',(0.866027687214196,-1.50000395501636,
-1.90833104990357));
#363229=CARTESIAN_POINT('Ctrl Pts',(1.29904153082129,-0.75000197750818,
-1.86666438323691));
#363230=CARTESIAN_POINT('Ctrl Pts',(1.73205537442839,-1.18035366021716E-15,
-1.82499771657024));
#363231=CARTESIAN_POINT('Ctrl Pts',(1.2990415308213,0.750001977508177,-1.78333104990357));
#363232=CARTESIAN_POINT('Ctrl Pts',(0.866027687214198,1.50000395501636,
-1.74166438323691));
#363233=CARTESIAN_POINT('Ctrl Pts',(0.,1.50000395501636,-1.69999771657024));
#363234=CARTESIAN_POINT('Ctrl Pts',(-0.866027687214197,1.50000395501636,
-1.65833104990357));
#363235=CARTESIAN_POINT('Ctrl Pts',(-1.2990415308213,0.750001977508178,
-1.61666438323691));
#363236=CARTESIAN_POINT('Ctrl Pts',(-1.73205537442839,-8.65396365915792E-16,
-1.57499771657024));
#363237=CARTESIAN_POINT('Ctrl Pts',(-1.2990415308213,-0.750001977508179,
-1.53333104990357));
#363238=CARTESIAN_POINT('Ctrl Pts',(-0.866027687214197,-1.50000395501636,
-1.49166438323691));
#363239=CARTESIAN_POINT('Ctrl Pts',(-1.83697504221915E-16,-1.50000395501636,
-1.44999771657024));
#363240=CARTESIAN_POINT('Ctrl Pts',(0.866027687214196,-1.50000395501636,
-1.40833104990357));
#363241=CARTESIAN_POINT('Ctrl Pts',(1.29904153082129,-0.75000197750818,
-1.36666438323691));
#363242=CARTESIAN_POINT('Ctrl Pts',(1.73205537442839,-1.3989014997103E-15,
-1.32499771657024));
#363243=CARTESIAN_POINT('Ctrl Pts',(1.2990415308213,0.750001977508176,-1.28333104990357));
#363244=CARTESIAN_POINT('Ctrl Pts',(0.866027687214198,1.50000395501635,
-1.24166438323691));
#363245=CARTESIAN_POINT('Ctrl Pts',(0.,1.50000395501636,-1.19999771657024));
#363246=CARTESIAN_POINT('Ctrl Pts',(0.,1.17524047358083,-17.8875));
#363247=CARTESIAN_POINT('Ctrl Pts',(-0.678525403784434,1.17524047358083,
-17.8458333333333));
#363248=CARTESIAN_POINT('Ctrl Pts',(-1.01778810567665,0.58762023679042,
-17.8041666666667));
#363249=CARTESIAN_POINT('Ctrl Pts',(-1.35705080756887,6.18712852862843E-15,
-17.7625));
#363250=CARTESIAN_POINT('Ctrl Pts',(-1.01778810567665,-0.587620236790408,
-17.7208333333333));
#363251=CARTESIAN_POINT('Ctrl Pts',(-0.678525403784435,-1.17524047358082,
-17.6791666666667));
#363252=CARTESIAN_POINT('Ctrl Pts',(-1.43925448419918E-16,-1.17524047358082,
-17.6375));
#363253=CARTESIAN_POINT('Ctrl Pts',(0.678525403784434,-1.17524047358082,
-17.5958333333333));
#363254=CARTESIAN_POINT('Ctrl Pts',(1.01778810567665,-0.587620236790409,
-17.5541666666667));
#363255=CARTESIAN_POINT('Ctrl Pts',(1.35705080756887,5.74547302332795E-15,
-17.5125));
#363256=CARTESIAN_POINT('Ctrl Pts',(1.01778810567665,0.587620236790419,
-17.4708333333333));
#363257=CARTESIAN_POINT('Ctrl Pts',(0.678525403784435,1.17524047358083,
-17.4291666666667));
#363258=CARTESIAN_POINT('Ctrl Pts',(0.,1.17524047358083,-17.3875));
#363259=CARTESIAN_POINT('Ctrl Pts',(-0.678525403784434,1.17524047358083,
-17.3458333333333));
#363260=CARTESIAN_POINT('Ctrl Pts',(-1.01778810567665,0.58762023679042,
-17.3041666666667));
#363261=CARTESIAN_POINT('Ctrl Pts',(-1.35705080756887,5.96858068913529E-15,
-17.2625));
#363262=CARTESIAN_POINT('Ctrl Pts',(-1.01778810567665,-0.587620236790408,
-17.2208333333333));
#363263=CARTESIAN_POINT('Ctrl Pts',(-0.678525403784435,-1.17524047358082,
-17.1791666666667));
#363264=CARTESIAN_POINT('Ctrl Pts',(-1.43925448419918E-16,-1.17524047358082,
-17.1375));
#363265=CARTESIAN_POINT('Ctrl Pts',(0.678525403784434,-1.17524047358082,
-17.0958333333333));
#363266=CARTESIAN_POINT('Ctrl Pts',(1.01778810567665,-0.587620236790409,
-17.0541666666667));
#363267=CARTESIAN_POINT('Ctrl Pts',(1.35705080756887,5.52692518383481E-15,
-17.0125));
#363268=CARTESIAN_POINT('Ctrl Pts',(1.01778810567665,0.587620236790419,
-16.9708333333333));
#363269=CARTESIAN_POINT('Ctrl Pts',(0.678525403784435,1.17524047358083,
-16.9291666666667));
#363270=CARTESIAN_POINT('Ctrl Pts',(0.,1.17524047358083,-16.8875));
#363271=CARTESIAN_POINT('Ctrl Pts',(-0.678525403784434,1.17524047358083,
-16.8458333333333));
#363272=CARTESIAN_POINT('Ctrl Pts',(-1.01778810567665,0.58762023679042,
-16.8041666666667));
#363273=CARTESIAN_POINT('Ctrl Pts',(-1.35705080756887,5.75003284964215E-15,
-16.7625));
#363274=CARTESIAN_POINT('Ctrl Pts',(-1.01778810567665,-0.587620236790408,
-16.7208333333333));
#363275=CARTESIAN_POINT('Ctrl Pts',(-0.678525403784435,-1.17524047358082,
-16.6791666666667));
#363276=CARTESIAN_POINT('Ctrl Pts',(-1.43925448419918E-16,-1.17524047358082,
-16.6375));
#363277=CARTESIAN_POINT('Ctrl Pts',(0.678525403784434,-1.17524047358082,
-16.5958333333333));
#363278=CARTESIAN_POINT('Ctrl Pts',(1.01778810567665,-0.587620236790409,
-16.5541666666667));
#363279=CARTESIAN_POINT('Ctrl Pts',(1.35705080756887,5.30837734434166E-15,
-16.5125));
#363280=CARTESIAN_POINT('Ctrl Pts',(1.01778810567665,0.587620236790419,
-16.4708333333333));
#363281=CARTESIAN_POINT('Ctrl Pts',(0.678525403784435,1.17524047358083,
-16.4291666666667));
#363282=CARTESIAN_POINT('Ctrl Pts',(0.,1.17524047358083,-16.3875));
#363283=CARTESIAN_POINT('Ctrl Pts',(-0.678525403784434,1.17524047358083,
-16.3458333333333));
#363284=CARTESIAN_POINT('Ctrl Pts',(-1.01778810567665,0.58762023679042,
-16.3041666666667));
#363285=CARTESIAN_POINT('Ctrl Pts',(-1.35705080756887,5.53148501014901E-15,
-16.2625));
#363286=CARTESIAN_POINT('Ctrl Pts',(-1.01778810567665,-0.587620236790409,
-16.2208333333333));
#363287=CARTESIAN_POINT('Ctrl Pts',(-0.678525403784435,-1.17524047358082,
-16.1791666666667));
#363288=CARTESIAN_POINT('Ctrl Pts',(-1.43925448419918E-16,-1.17524047358082,
-16.1375));
#363289=CARTESIAN_POINT('Ctrl Pts',(0.678525403784434,-1.17524047358082,
-16.0958333333333));
#363290=CARTESIAN_POINT('Ctrl Pts',(1.01778810567665,-0.587620236790409,
-16.0541666666667));
#363291=CARTESIAN_POINT('Ctrl Pts',(1.35705080756887,5.08982950484852E-15,
-16.0125));
#363292=CARTESIAN_POINT('Ctrl Pts',(1.01778810567665,0.587620236790419,
-15.9708333333333));
#363293=CARTESIAN_POINT('Ctrl Pts',(0.678525403784435,1.17524047358083,
-15.9291666666667));
#363294=CARTESIAN_POINT('Ctrl Pts',(0.,1.17524047358083,-15.8875));
#363295=CARTESIAN_POINT('Ctrl Pts',(-0.678525403784434,1.17524047358083,
-15.8458333333333));
#363296=CARTESIAN_POINT('Ctrl Pts',(-1.01778810567665,0.58762023679042,
-15.8041666666667));
#363297=CARTESIAN_POINT('Ctrl Pts',(-1.35705080756887,5.31293717065586E-15,
-15.7625));
#363298=CARTESIAN_POINT('Ctrl Pts',(-1.01778810567665,-0.587620236790409,
-15.7208333333333));
#363299=CARTESIAN_POINT('Ctrl Pts',(-0.678525403784435,-1.17524047358082,
-15.6791666666667));
#363300=CARTESIAN_POINT('Ctrl Pts',(-1.43925448419918E-16,-1.17524047358082,
-15.6375));
#363301=CARTESIAN_POINT('Ctrl Pts',(0.678525403784434,-1.17524047358082,
-15.5958333333333));
#363302=CARTESIAN_POINT('Ctrl Pts',(1.01778810567665,-0.58762023679041,
-15.5541666666667));
#363303=CARTESIAN_POINT('Ctrl Pts',(1.35705080756887,4.87128166535538E-15,
-15.5125));
#363304=CARTESIAN_POINT('Ctrl Pts',(1.01778810567665,0.587620236790418,
-15.4708333333333));
#363305=CARTESIAN_POINT('Ctrl Pts',(0.678525403784435,1.17524047358083,
-15.4291666666667));
#363306=CARTESIAN_POINT('Ctrl Pts',(0.,1.17524047358083,-15.3875));
#363307=CARTESIAN_POINT('Ctrl Pts',(-0.678525403784434,1.17524047358083,
-15.3458333333333));
#363308=CARTESIAN_POINT('Ctrl Pts',(-1.01778810567665,0.587620236790419,
-15.3041666666667));
#363309=CARTESIAN_POINT('Ctrl Pts',(-1.35705080756887,5.09438933116272E-15,
-15.2625));
#363310=CARTESIAN_POINT('Ctrl Pts',(-1.01778810567665,-0.587620236790409,
-15.2208333333333));
#363311=CARTESIAN_POINT('Ctrl Pts',(-0.678525403784435,-1.17524047358082,
-15.1791666666667));
#363312=CARTESIAN_POINT('Ctrl Pts',(-1.43925448419918E-16,-1.17524047358082,
-15.1375));
#363313=CARTESIAN_POINT('Ctrl Pts',(0.678525403784434,-1.17524047358082,
-15.0958333333333));
#363314=CARTESIAN_POINT('Ctrl Pts',(1.01778810567665,-0.58762023679041,
-15.0541666666667));
#363315=CARTESIAN_POINT('Ctrl Pts',(1.35705080756887,4.65273382586224E-15,
-15.0125));
#363316=CARTESIAN_POINT('Ctrl Pts',(1.01778810567665,0.587620236790418,
-14.9708333333333));
#363317=CARTESIAN_POINT('Ctrl Pts',(0.678525403784435,1.17524047358083,
-14.9291666666667));
#363318=CARTESIAN_POINT('Ctrl Pts',(0.,1.17524047358083,-14.8875));
#363319=CARTESIAN_POINT('Ctrl Pts',(-0.678525403784434,1.17524047358083,
-14.8458333333333));
#363320=CARTESIAN_POINT('Ctrl Pts',(-1.01778810567665,0.587620236790419,
-14.8041666666667));
#363321=CARTESIAN_POINT('Ctrl Pts',(-1.35705080756887,4.87584149166958E-15,
-14.7625));
#363322=CARTESIAN_POINT('Ctrl Pts',(-1.01778810567665,-0.587620236790409,
-14.7208333333333));
#363323=CARTESIAN_POINT('Ctrl Pts',(-0.678525403784435,-1.17524047358082,
-14.6791666666667));
#363324=CARTESIAN_POINT('Ctrl Pts',(-1.43925448419918E-16,-1.17524047358082,
-14.6375));
#363325=CARTESIAN_POINT('Ctrl Pts',(0.678525403784434,-1.17524047358082,
-14.5958333333333));
#363326=CARTESIAN_POINT('Ctrl Pts',(1.01778810567665,-0.58762023679041,
-14.5541666666667));
#363327=CARTESIAN_POINT('Ctrl Pts',(1.35705080756887,4.4341859863691E-15,
-14.5125));
#363328=CARTESIAN_POINT('Ctrl Pts',(1.01778810567665,0.587620236790418,
-14.4708333333333));
#363329=CARTESIAN_POINT('Ctrl Pts',(0.678525403784435,1.17524047358083,
-14.4291666666667));
#363330=CARTESIAN_POINT('Ctrl Pts',(0.,1.17524047358083,-14.3875));
#363331=CARTESIAN_POINT('Ctrl Pts',(-0.678525403784434,1.17524047358083,
-14.3458333333333));
#363332=CARTESIAN_POINT('Ctrl Pts',(-1.01778810567665,0.587620236790419,
-14.3041666666667));
#363333=CARTESIAN_POINT('Ctrl Pts',(-1.35705080756887,4.65729365217644E-15,
-14.2625));
#363334=CARTESIAN_POINT('Ctrl Pts',(-1.01778810567665,-0.587620236790409,
-14.2208333333333));
#363335=CARTESIAN_POINT('Ctrl Pts',(-0.678525403784435,-1.17524047358082,
-14.1791666666667));
#363336=CARTESIAN_POINT('Ctrl Pts',(-1.43925448419918E-16,-1.17524047358082,
-14.1375));
#363337=CARTESIAN_POINT('Ctrl Pts',(0.678525403784434,-1.17524047358082,
-14.0958333333333));
#363338=CARTESIAN_POINT('Ctrl Pts',(1.01778810567665,-0.58762023679041,
-14.0541666666667));
#363339=CARTESIAN_POINT('Ctrl Pts',(1.35705080756887,4.21563814687596E-15,
-14.0125));
#363340=CARTESIAN_POINT('Ctrl Pts',(1.01778810567665,0.587620236790418,
-13.9708333333333));
#363341=CARTESIAN_POINT('Ctrl Pts',(0.678525403784435,1.17524047358083,
-13.9291666666667));
#363342=CARTESIAN_POINT('Ctrl Pts',(0.,1.17524047358083,-13.8875));
#363343=CARTESIAN_POINT('Ctrl Pts',(-0.678525403784434,1.17524047358083,
-13.8458333333333));
#363344=CARTESIAN_POINT('Ctrl Pts',(-1.01778810567665,0.587620236790419,
-13.8041666666667));
#363345=CARTESIAN_POINT('Ctrl Pts',(-1.35705080756887,4.4387458126833E-15,
-13.7625));
#363346=CARTESIAN_POINT('Ctrl Pts',(-1.01778810567665,-0.58762023679041,
-13.7208333333333));
#363347=CARTESIAN_POINT('Ctrl Pts',(-0.678525403784435,-1.17524047358082,
-13.6791666666667));
#363348=CARTESIAN_POINT('Ctrl Pts',(-1.43925448419918E-16,-1.17524047358082,
-13.6375));
#363349=CARTESIAN_POINT('Ctrl Pts',(0.678525403784434,-1.17524047358082,
-13.5958333333333));
#363350=CARTESIAN_POINT('Ctrl Pts',(1.01778810567665,-0.58762023679041,
-13.5541666666667));
#363351=CARTESIAN_POINT('Ctrl Pts',(1.35705080756887,3.99709030738282E-15,
-13.5125));
#363352=CARTESIAN_POINT('Ctrl Pts',(1.01778810567665,0.587620236790418,
-13.4708333333333));
#363353=CARTESIAN_POINT('Ctrl Pts',(0.678525403784435,1.17524047358083,
-13.4291666666667));
#363354=CARTESIAN_POINT('Ctrl Pts',(0.,1.17524047358083,-13.3875));
#363355=CARTESIAN_POINT('Ctrl Pts',(-0.678525403784434,1.17524047358083,
-13.3458333333333));
#363356=CARTESIAN_POINT('Ctrl Pts',(-1.01778810567665,0.587620236790419,
-13.3041666666667));
#363357=CARTESIAN_POINT('Ctrl Pts',(-1.35705080756887,4.22019797319016E-15,
-13.2625));
#363358=CARTESIAN_POINT('Ctrl Pts',(-1.01778810567665,-0.58762023679041,
-13.2208333333333));
#363359=CARTESIAN_POINT('Ctrl Pts',(-0.678525403784435,-1.17524047358082,
-13.1791666666667));
#363360=CARTESIAN_POINT('Ctrl Pts',(-1.43925448419918E-16,-1.17524047358082,
-13.1375));
#363361=CARTESIAN_POINT('Ctrl Pts',(0.678525403784434,-1.17524047358082,
-13.0958333333333));
#363362=CARTESIAN_POINT('Ctrl Pts',(1.01778810567665,-0.587620236790411,
-13.0541666666667));
#363363=CARTESIAN_POINT('Ctrl Pts',(1.35705080756887,3.77854246788968E-15,
-13.0125));
#363364=CARTESIAN_POINT('Ctrl Pts',(1.01778810567665,0.587620236790417,
-12.9708333333333));
#363365=CARTESIAN_POINT('Ctrl Pts',(0.678525403784435,1.17524047358083,
-12.9291666666667));
#363366=CARTESIAN_POINT('Ctrl Pts',(0.,1.17524047358083,-12.8875));
#363367=CARTESIAN_POINT('Ctrl Pts',(-0.678525403784434,1.17524047358083,
-12.8458333333333));
#363368=CARTESIAN_POINT('Ctrl Pts',(-1.01778810567665,0.587620236790418,
-12.8041666666667));
#363369=CARTESIAN_POINT('Ctrl Pts',(-1.35705080756887,4.00165013369702E-15,
-12.7625));
#363370=CARTESIAN_POINT('Ctrl Pts',(-1.01778810567665,-0.58762023679041,
-12.7208333333333));
#363371=CARTESIAN_POINT('Ctrl Pts',(-0.678525403784435,-1.17524047358082,
-12.6791666666667));
#363372=CARTESIAN_POINT('Ctrl Pts',(-1.43925448419918E-16,-1.17524047358082,
-12.6375));
#363373=CARTESIAN_POINT('Ctrl Pts',(0.678525403784434,-1.17524047358083,
-12.5958333333333));
#363374=CARTESIAN_POINT('Ctrl Pts',(1.01778810567665,-0.587620236790411,
-12.5541666666667));
#363375=CARTESIAN_POINT('Ctrl Pts',(1.35705080756887,3.55999462839654E-15,
-12.5125));
#363376=CARTESIAN_POINT('Ctrl Pts',(1.01778810567665,0.587620236790417,
-12.4708333333333));
#363377=CARTESIAN_POINT('Ctrl Pts',(0.678525403784435,1.17524047358083,
-12.4291666666667));
#363378=CARTESIAN_POINT('Ctrl Pts',(0.,1.17524047358083,-12.3875));
#363379=CARTESIAN_POINT('Ctrl Pts',(-0.678525403784434,1.17524047358083,
-12.3458333333333));
#363380=CARTESIAN_POINT('Ctrl Pts',(-1.01778810567665,0.587620236790418,
-12.3041666666667));
#363381=CARTESIAN_POINT('Ctrl Pts',(-1.35705080756887,3.78310229420388E-15,
-12.2625));
#363382=CARTESIAN_POINT('Ctrl Pts',(-1.01778810567665,-0.58762023679041,
-12.2208333333333));
#363383=CARTESIAN_POINT('Ctrl Pts',(-0.678525403784435,-1.17524047358082,
-12.1791666666667));
#363384=CARTESIAN_POINT('Ctrl Pts',(-1.43925448419918E-16,-1.17524047358082,
-12.1375));
#363385=CARTESIAN_POINT('Ctrl Pts',(0.678525403784434,-1.17524047358083,
-12.0958333333333));
#363386=CARTESIAN_POINT('Ctrl Pts',(1.01778810567665,-0.587620236790411,
-12.0541666666667));
#363387=CARTESIAN_POINT('Ctrl Pts',(1.35705080756887,3.34144678890339E-15,
-12.0125));
#363388=CARTESIAN_POINT('Ctrl Pts',(1.01778810567665,0.587620236790417,
-11.9708333333333));
#363389=CARTESIAN_POINT('Ctrl Pts',(0.678525403784435,1.17524047358083,
-11.9291666666667));
#363390=CARTESIAN_POINT('Ctrl Pts',(0.,1.17524047358083,-11.8875));
#363391=CARTESIAN_POINT('Ctrl Pts',(-0.678525403784434,1.17524047358083,
-11.8458333333333));
#363392=CARTESIAN_POINT('Ctrl Pts',(-1.01778810567665,0.587620236790418,
-11.8041666666667));
#363393=CARTESIAN_POINT('Ctrl Pts',(-1.35705080756887,3.56455445471073E-15,
-11.7625));
#363394=CARTESIAN_POINT('Ctrl Pts',(-1.01778810567665,-0.587620236790411,
-11.7208333333333));
#363395=CARTESIAN_POINT('Ctrl Pts',(-0.678525403784435,-1.17524047358083,
-11.6791666666667));
#363396=CARTESIAN_POINT('Ctrl Pts',(-1.43925448419918E-16,-1.17524047358083,
-11.6375));
#363397=CARTESIAN_POINT('Ctrl Pts',(0.678525403784434,-1.17524047358083,
-11.5958333333333));
#363398=CARTESIAN_POINT('Ctrl Pts',(1.01778810567665,-0.587620236790411,
-11.5541666666667));
#363399=CARTESIAN_POINT('Ctrl Pts',(1.35705080756887,3.12289894941025E-15,
-11.5125));
#363400=CARTESIAN_POINT('Ctrl Pts',(1.01778810567665,0.587620236790417,
-11.4708333333333));
#363401=CARTESIAN_POINT('Ctrl Pts',(0.678525403784435,1.17524047358083,
-11.4291666666667));
#363402=CARTESIAN_POINT('Ctrl Pts',(0.,1.17524047358083,-11.3875));
#363403=CARTESIAN_POINT('Ctrl Pts',(-0.678525403784434,1.17524047358083,
-11.3458333333333));
#363404=CARTESIAN_POINT('Ctrl Pts',(-1.01778810567665,0.587620236790418,
-11.3041666666667));
#363405=CARTESIAN_POINT('Ctrl Pts',(-1.35705080756887,3.34600661521759E-15,
-11.2625));
#363406=CARTESIAN_POINT('Ctrl Pts',(-1.01778810567665,-0.587620236790411,
-11.2208333333333));
#363407=CARTESIAN_POINT('Ctrl Pts',(-0.678525403784435,-1.17524047358083,
-11.1791666666667));
#363408=CARTESIAN_POINT('Ctrl Pts',(-1.43925448419918E-16,-1.17524047358083,
-11.1375));
#363409=CARTESIAN_POINT('Ctrl Pts',(0.678525403784434,-1.17524047358083,
-11.0958333333333));
#363410=CARTESIAN_POINT('Ctrl Pts',(1.01778810567665,-0.587620236790412,
-11.0541666666667));
#363411=CARTESIAN_POINT('Ctrl Pts',(1.35705080756887,2.90435110991711E-15,
-11.0125));
#363412=CARTESIAN_POINT('Ctrl Pts',(1.01778810567665,0.587620236790416,
-10.9708333333333));
#363413=CARTESIAN_POINT('Ctrl Pts',(0.678525403784435,1.17524047358083,
-10.9291666666667));
#363414=CARTESIAN_POINT('Ctrl Pts',(0.,1.17524047358083,-10.8875));
#363415=CARTESIAN_POINT('Ctrl Pts',(-0.678525403784434,1.17524047358083,
-10.8458333333333));
#363416=CARTESIAN_POINT('Ctrl Pts',(-1.01778810567665,0.587620236790417,
-10.8041666666667));
#363417=CARTESIAN_POINT('Ctrl Pts',(-1.35705080756887,3.12745877572445E-15,
-10.7625));
#363418=CARTESIAN_POINT('Ctrl Pts',(-1.01778810567665,-0.587620236790411,
-10.7208333333333));
#363419=CARTESIAN_POINT('Ctrl Pts',(-0.678525403784435,-1.17524047358083,
-10.6791666666667));
#363420=CARTESIAN_POINT('Ctrl Pts',(-1.43925448419918E-16,-1.17524047358083,
-10.6375));
#363421=CARTESIAN_POINT('Ctrl Pts',(0.678525403784434,-1.17524047358083,
-10.5958333333333));
#363422=CARTESIAN_POINT('Ctrl Pts',(1.01778810567665,-0.587620236790412,
-10.5541666666667));
#363423=CARTESIAN_POINT('Ctrl Pts',(1.35705080756887,2.68580327042397E-15,
-10.5125));
#363424=CARTESIAN_POINT('Ctrl Pts',(1.01778810567665,0.587620236790416,
-10.4708333333333));
#363425=CARTESIAN_POINT('Ctrl Pts',(0.678525403784435,1.17524047358083,
-10.4291666666667));
#363426=CARTESIAN_POINT('Ctrl Pts',(0.,1.17524047358083,-10.3875));
#363427=CARTESIAN_POINT('Ctrl Pts',(-0.678525403784434,1.17524047358083,
-10.3458333333333));
#363428=CARTESIAN_POINT('Ctrl Pts',(-1.01778810567665,0.587620236790417,
-10.3041666666667));
#363429=CARTESIAN_POINT('Ctrl Pts',(-1.35705080756887,2.90891093623131E-15,
-10.2625));
#363430=CARTESIAN_POINT('Ctrl Pts',(-1.01778810567665,-0.587620236790411,
-10.2208333333333));
#363431=CARTESIAN_POINT('Ctrl Pts',(-0.678525403784435,-1.17524047358083,
-10.1791666666667));
#363432=CARTESIAN_POINT('Ctrl Pts',(-1.43925448419918E-16,-1.17524047358083,
-10.1375));
#363433=CARTESIAN_POINT('Ctrl Pts',(0.678525403784434,-1.17524047358083,
-10.0958333333333));
#363434=CARTESIAN_POINT('Ctrl Pts',(1.01778810567665,-0.587620236790412,
-10.0541666666667));
#363435=CARTESIAN_POINT('Ctrl Pts',(1.35705080756887,2.46725543093083E-15,
-10.0125));
#363436=CARTESIAN_POINT('Ctrl Pts',(1.01778810567665,0.587620236790416,
-9.97083333333333));
#363437=CARTESIAN_POINT('Ctrl Pts',(0.678525403784435,1.17524047358083,
-9.92916666666667));
#363438=CARTESIAN_POINT('Ctrl Pts',(0.,1.17524047358083,-9.8875));
#363439=CARTESIAN_POINT('Ctrl Pts',(-0.678525403784434,1.17524047358083,
-9.84583333333333));
#363440=CARTESIAN_POINT('Ctrl Pts',(-1.01778810567665,0.587620236790417,
-9.80416666666667));
#363441=CARTESIAN_POINT('Ctrl Pts',(-1.35705080756887,2.69036309673817E-15,
-9.7625));
#363442=CARTESIAN_POINT('Ctrl Pts',(-1.01778810567665,-0.587620236790411,
-9.72083333333333));
#363443=CARTESIAN_POINT('Ctrl Pts',(-0.678525403784435,-1.17524047358083,
-9.67916666666667));
#363444=CARTESIAN_POINT('Ctrl Pts',(-1.43925448419918E-16,-1.17524047358083,
-9.6375));
#363445=CARTESIAN_POINT('Ctrl Pts',(0.678525403784434,-1.17524047358083,
-9.59583333333333));
#363446=CARTESIAN_POINT('Ctrl Pts',(1.01778810567665,-0.587620236790412,
-9.55416666666667));
#363447=CARTESIAN_POINT('Ctrl Pts',(1.35705080756887,2.24870759143769E-15,
-9.5125));
#363448=CARTESIAN_POINT('Ctrl Pts',(1.01778810567665,0.587620236790416,
-9.47083333333333));
#363449=CARTESIAN_POINT('Ctrl Pts',(0.678525403784435,1.17524047358083,
-9.42916666666667));
#363450=CARTESIAN_POINT('Ctrl Pts',(0.,1.17524047358083,-9.3875));
#363451=CARTESIAN_POINT('Ctrl Pts',(-0.678525403784434,1.17524047358083,
-9.34583333333333));
#363452=CARTESIAN_POINT('Ctrl Pts',(-1.01778810567665,0.587620236790417,
-9.30416666666667));
#363453=CARTESIAN_POINT('Ctrl Pts',(-1.35705080756887,2.47181525724503E-15,
-9.2625));
#363454=CARTESIAN_POINT('Ctrl Pts',(-1.01778810567665,-0.587620236790412,
-9.22083333333333));
#363455=CARTESIAN_POINT('Ctrl Pts',(-0.678525403784435,-1.17524047358083,
-9.17916666666667));
#363456=CARTESIAN_POINT('Ctrl Pts',(-1.43925448419918E-16,-1.17524047358083,
-9.1375));
#363457=CARTESIAN_POINT('Ctrl Pts',(0.678525403784434,-1.17524047358083,
-9.09583333333333));
#363458=CARTESIAN_POINT('Ctrl Pts',(1.01778810567665,-0.587620236790412,
-9.05416666666667));
#363459=CARTESIAN_POINT('Ctrl Pts',(1.35705080756887,2.03015975194455E-15,
-9.0125));
#363460=CARTESIAN_POINT('Ctrl Pts',(1.01778810567665,0.587620236790416,
-8.97083333333333));
#363461=CARTESIAN_POINT('Ctrl Pts',(0.678525403784435,1.17524047358083,
-8.92916666666667));
#363462=CARTESIAN_POINT('Ctrl Pts',(0.,1.17524047358083,-8.8875));
#363463=CARTESIAN_POINT('Ctrl Pts',(-0.678525403784434,1.17524047358083,
-8.84583333333333));
#363464=CARTESIAN_POINT('Ctrl Pts',(-1.01778810567665,0.587620236790416,
-8.80416666666667));
#363465=CARTESIAN_POINT('Ctrl Pts',(-1.35705080756887,2.25326741775189E-15,
-8.7625));
#363466=CARTESIAN_POINT('Ctrl Pts',(-1.01778810567665,-0.587620236790412,
-8.72083333333333));
#363467=CARTESIAN_POINT('Ctrl Pts',(-0.678525403784435,-1.17524047358083,
-8.67916666666667));
#363468=CARTESIAN_POINT('Ctrl Pts',(-1.43925448419918E-16,-1.17524047358083,
-8.6375));
#363469=CARTESIAN_POINT('Ctrl Pts',(0.678525403784434,-1.17524047358083,
-8.59583333333333));
#363470=CARTESIAN_POINT('Ctrl Pts',(1.01778810567665,-0.587620236790413,
-8.55416666666667));
#363471=CARTESIAN_POINT('Ctrl Pts',(1.35705080756887,1.81161191245141E-15,
-8.5125));
#363472=CARTESIAN_POINT('Ctrl Pts',(1.01778810567665,0.587620236790415,
-8.47083333333333));
#363473=CARTESIAN_POINT('Ctrl Pts',(0.678525403784435,1.17524047358083,
-8.42916666666667));
#363474=CARTESIAN_POINT('Ctrl Pts',(0.,1.17524047358083,-8.3875));
#363475=CARTESIAN_POINT('Ctrl Pts',(-0.678525403784434,1.17524047358083,
-8.34583333333333));
#363476=CARTESIAN_POINT('Ctrl Pts',(-1.01778810567665,0.587620236790416,
-8.30416666666667));
#363477=CARTESIAN_POINT('Ctrl Pts',(-1.35705080756887,2.03471957825875E-15,
-8.2625));
#363478=CARTESIAN_POINT('Ctrl Pts',(-1.01778810567665,-0.587620236790412,
-8.22083333333333));
#363479=CARTESIAN_POINT('Ctrl Pts',(-0.678525403784435,-1.17524047358083,
-8.17916666666667));
#363480=CARTESIAN_POINT('Ctrl Pts',(-1.43925448419918E-16,-1.17524047358083,
-8.1375));
#363481=CARTESIAN_POINT('Ctrl Pts',(0.678525403784434,-1.17524047358083,
-8.09583333333333));
#363482=CARTESIAN_POINT('Ctrl Pts',(1.01778810567665,-0.587620236790413,
-8.05416666666667));
#363483=CARTESIAN_POINT('Ctrl Pts',(1.35705080756887,1.59306407295827E-15,
-8.0125));
#363484=CARTESIAN_POINT('Ctrl Pts',(1.01778810567665,0.587620236790415,
-7.97083333333334));
#363485=CARTESIAN_POINT('Ctrl Pts',(0.678525403784435,1.17524047358083,
-7.92916666666667));
#363486=CARTESIAN_POINT('Ctrl Pts',(0.,1.17524047358083,-7.8875));
#363487=CARTESIAN_POINT('Ctrl Pts',(-0.678525403784434,1.17524047358083,
-7.84583333333333));
#363488=CARTESIAN_POINT('Ctrl Pts',(-1.01778810567665,0.587620236790416,
-7.80416666666667));
#363489=CARTESIAN_POINT('Ctrl Pts',(-1.35705080756887,1.8161717387656E-15,
-7.7625));
#363490=CARTESIAN_POINT('Ctrl Pts',(-1.01778810567665,-0.587620236790412,
-7.72083333333334));
#363491=CARTESIAN_POINT('Ctrl Pts',(-0.678525403784435,-1.17524047358083,
-7.67916666666667));
#363492=CARTESIAN_POINT('Ctrl Pts',(-1.43925448419918E-16,-1.17524047358083,
-7.6375));
#363493=CARTESIAN_POINT('Ctrl Pts',(0.678525403784434,-1.17524047358083,
-7.59583333333333));
#363494=CARTESIAN_POINT('Ctrl Pts',(1.01778810567665,-0.587620236790413,
-7.55416666666667));
#363495=CARTESIAN_POINT('Ctrl Pts',(1.35705080756887,1.37451623346513E-15,
-7.5125));
#363496=CARTESIAN_POINT('Ctrl Pts',(1.01778810567665,0.587620236790415,
-7.47083333333333));
#363497=CARTESIAN_POINT('Ctrl Pts',(0.678525403784435,1.17524047358083,
-7.42916666666667));
#363498=CARTESIAN_POINT('Ctrl Pts',(0.,1.17524047358083,-7.3875));
#363499=CARTESIAN_POINT('Ctrl Pts',(-0.678525403784434,1.17524047358083,
-7.34583333333334));
#363500=CARTESIAN_POINT('Ctrl Pts',(-1.01778810567665,0.587620236790416,
-7.30416666666667));
#363501=CARTESIAN_POINT('Ctrl Pts',(-1.35705080756887,1.59762389927246E-15,
-7.2625));
#363502=CARTESIAN_POINT('Ctrl Pts',(-1.01778810567665,-0.587620236790412,
-7.22083333333333));
#363503=CARTESIAN_POINT('Ctrl Pts',(-0.678525403784435,-1.17524047358083,
-7.17916666666667));
#363504=CARTESIAN_POINT('Ctrl Pts',(-1.43925448419918E-16,-1.17524047358083,
-7.1375));
#363505=CARTESIAN_POINT('Ctrl Pts',(0.678525403784434,-1.17524047358083,
-7.09583333333333));
#363506=CARTESIAN_POINT('Ctrl Pts',(1.01778810567665,-0.587620236790413,
-7.05416666666667));
#363507=CARTESIAN_POINT('Ctrl Pts',(1.35705080756887,1.15596839397198E-15,
-7.0125));
#363508=CARTESIAN_POINT('Ctrl Pts',(1.01778810567665,0.587620236790415,
-6.97083333333333));
#363509=CARTESIAN_POINT('Ctrl Pts',(0.678525403784435,1.17524047358083,
-6.92916666666667));
#363510=CARTESIAN_POINT('Ctrl Pts',(0.,1.17524047358083,-6.8875));
#363511=CARTESIAN_POINT('Ctrl Pts',(-0.678525403784434,1.17524047358083,
-6.84583333333333));
#363512=CARTESIAN_POINT('Ctrl Pts',(-1.01778810567665,0.587620236790416,
-6.80416666666667));
#363513=CARTESIAN_POINT('Ctrl Pts',(-1.35705080756887,1.37907605977932E-15,
-6.7625));
#363514=CARTESIAN_POINT('Ctrl Pts',(-1.01778810567665,-0.587620236790413,
-6.72083333333333));
#363515=CARTESIAN_POINT('Ctrl Pts',(-0.678525403784435,-1.17524047358083,
-6.67916666666667));
#363516=CARTESIAN_POINT('Ctrl Pts',(-1.43925448419918E-16,-1.17524047358083,
-6.6375));
#363517=CARTESIAN_POINT('Ctrl Pts',(0.678525403784434,-1.17524047358083,
-6.59583333333333));
#363518=CARTESIAN_POINT('Ctrl Pts',(1.01778810567665,-0.587620236790414,
-6.55416666666667));
#363519=CARTESIAN_POINT('Ctrl Pts',(1.35705080756887,9.37420554478842E-16,
-6.5125));
#363520=CARTESIAN_POINT('Ctrl Pts',(1.01778810567665,0.587620236790415,
-6.47083333333333));
#363521=CARTESIAN_POINT('Ctrl Pts',(0.678525403784435,1.17524047358083,
-6.42916666666667));
#363522=CARTESIAN_POINT('Ctrl Pts',(0.,1.17524047358083,-6.3875));
#363523=CARTESIAN_POINT('Ctrl Pts',(-0.678525403784434,1.17524047358083,
-6.34583333333333));
#363524=CARTESIAN_POINT('Ctrl Pts',(-1.01778810567665,0.587620236790415,
-6.30416666666667));
#363525=CARTESIAN_POINT('Ctrl Pts',(-1.35705080756887,1.16052822028618E-15,
-6.2625));
#363526=CARTESIAN_POINT('Ctrl Pts',(-1.01778810567665,-0.587620236790413,
-6.22083333333333));
#363527=CARTESIAN_POINT('Ctrl Pts',(-0.678525403784435,-1.17524047358083,
-6.17916666666667));
#363528=CARTESIAN_POINT('Ctrl Pts',(-1.43925448419918E-16,-1.17524047358083,
-6.1375));
#363529=CARTESIAN_POINT('Ctrl Pts',(0.678525403784434,-1.17524047358083,
-6.09583333333334));
#363530=CARTESIAN_POINT('Ctrl Pts',(1.01778810567665,-0.587620236790414,
-6.05416666666667));
#363531=CARTESIAN_POINT('Ctrl Pts',(1.35705080756887,7.18872714985701E-16,
-6.0125));
#363532=CARTESIAN_POINT('Ctrl Pts',(1.01778810567665,0.587620236790414,
-5.97083333333333));
#363533=CARTESIAN_POINT('Ctrl Pts',(0.678525403784435,1.17524047358083,
-5.92916666666667));
#363534=CARTESIAN_POINT('Ctrl Pts',(0.,1.17524047358083,-5.8875));
#363535=CARTESIAN_POINT('Ctrl Pts',(-0.678525403784434,1.17524047358083,
-5.84583333333334));
#363536=CARTESIAN_POINT('Ctrl Pts',(-1.01778810567665,0.587620236790415,
-5.80416666666667));
#363537=CARTESIAN_POINT('Ctrl Pts',(-1.35705080756887,9.41980380793039E-16,
-5.7625));
#363538=CARTESIAN_POINT('Ctrl Pts',(-1.01778810567665,-0.587620236790413,
-5.72083333333333));
#363539=CARTESIAN_POINT('Ctrl Pts',(-0.678525403784435,-1.17524047358083,
-5.67916666666667));
#363540=CARTESIAN_POINT('Ctrl Pts',(-1.43925448419918E-16,-1.17524047358083,
-5.6375));
#363541=CARTESIAN_POINT('Ctrl Pts',(0.678525403784434,-1.17524047358083,
-5.59583333333333));
#363542=CARTESIAN_POINT('Ctrl Pts',(1.01778810567665,-0.587620236790414,
-5.55416666666667));
#363543=CARTESIAN_POINT('Ctrl Pts',(1.35705080756887,5.0032487549256E-16,
-5.5125));
#363544=CARTESIAN_POINT('Ctrl Pts',(1.01778810567665,0.587620236790414,
-5.47083333333333));
#363545=CARTESIAN_POINT('Ctrl Pts',(0.678525403784435,1.17524047358083,
-5.42916666666667));
#363546=CARTESIAN_POINT('Ctrl Pts',(0.,1.17524047358083,-5.3875));
#363547=CARTESIAN_POINT('Ctrl Pts',(-0.678525403784434,1.17524047358083,
-5.34583333333333));
#363548=CARTESIAN_POINT('Ctrl Pts',(-1.01778810567665,0.587620236790415,
-5.30416666666667));
#363549=CARTESIAN_POINT('Ctrl Pts',(-1.35705080756887,7.23432541299899E-16,
-5.2625));
#363550=CARTESIAN_POINT('Ctrl Pts',(-1.01778810567665,-0.587620236790413,
-5.22083333333333));
#363551=CARTESIAN_POINT('Ctrl Pts',(-0.678525403784435,-1.17524047358083,
-5.17916666666667));
#363552=CARTESIAN_POINT('Ctrl Pts',(-1.43925448419918E-16,-1.17524047358083,
-5.1375));
#363553=CARTESIAN_POINT('Ctrl Pts',(0.678525403784434,-1.17524047358083,
-5.09583333333333));
#363554=CARTESIAN_POINT('Ctrl Pts',(1.01778810567665,-0.587620236790414,
-5.05416666666667));
#363555=CARTESIAN_POINT('Ctrl Pts',(1.35705080756887,2.81777035999419E-16,
-5.0125));
#363556=CARTESIAN_POINT('Ctrl Pts',(1.01778810567665,0.587620236790414,
-4.97083333333333));
#363557=CARTESIAN_POINT('Ctrl Pts',(0.678525403784435,1.17524047358083,
-4.92916666666667));
#363558=CARTESIAN_POINT('Ctrl Pts',(0.,1.17524047358083,-4.8875));
#363559=CARTESIAN_POINT('Ctrl Pts',(-0.678525403784434,1.17524047358083,
-4.84583333333333));
#363560=CARTESIAN_POINT('Ctrl Pts',(-1.01778810567665,0.587620236790415,
-4.80416666666667));
#363561=CARTESIAN_POINT('Ctrl Pts',(-1.35705080756887,5.04884701806757E-16,
-4.7625));
#363562=CARTESIAN_POINT('Ctrl Pts',(-1.01778810567665,-0.587620236790414,
-4.72083333333333));
#363563=CARTESIAN_POINT('Ctrl Pts',(-0.678525403784435,-1.17524047358083,
-4.67916666666667));
#363564=CARTESIAN_POINT('Ctrl Pts',(-1.43925448419918E-16,-1.17524047358083,
-4.6375));
#363565=CARTESIAN_POINT('Ctrl Pts',(0.678525403784434,-1.17524047358083,
-4.59583333333333));
#363566=CARTESIAN_POINT('Ctrl Pts',(1.01778810567665,-0.587620236790414,
-4.55416666666667));
#363567=CARTESIAN_POINT('Ctrl Pts',(1.35705080756887,6.32291965062771E-17,
-4.5125));
#363568=CARTESIAN_POINT('Ctrl Pts',(1.01778810567665,0.587620236790414,
-4.47083333333333));
#363569=CARTESIAN_POINT('Ctrl Pts',(0.678525403784435,1.17524047358083,
-4.42916666666667));
#363570=CARTESIAN_POINT('Ctrl Pts',(0.,1.17524047358083,-4.3875));
#363571=CARTESIAN_POINT('Ctrl Pts',(-0.678525403784434,1.17524047358083,
-4.34583333333333));
#363572=CARTESIAN_POINT('Ctrl Pts',(-1.01778810567665,0.587620236790415,
-4.30416666666667));
#363573=CARTESIAN_POINT('Ctrl Pts',(-1.35705080756887,2.86336862313616E-16,
-4.2625));
#363574=CARTESIAN_POINT('Ctrl Pts',(-1.01778810567665,-0.587620236790414,
-4.22083333333333));
#363575=CARTESIAN_POINT('Ctrl Pts',(-0.678525403784435,-1.17524047358083,
-4.17916666666667));
#363576=CARTESIAN_POINT('Ctrl Pts',(-1.43925448419918E-16,-1.17524047358083,
-4.1375));
#363577=CARTESIAN_POINT('Ctrl Pts',(0.678525403784434,-1.17524047358083,
-4.09583333333333));
#363578=CARTESIAN_POINT('Ctrl Pts',(1.01778810567665,-0.587620236790415,
-4.05416666666667));
#363579=CARTESIAN_POINT('Ctrl Pts',(1.35705080756887,-1.55318642986864E-16,
-4.0125));
#363580=CARTESIAN_POINT('Ctrl Pts',(1.01778810567665,0.587620236790414,
-3.97083333333333));
#363581=CARTESIAN_POINT('Ctrl Pts',(0.678525403784435,1.17524047358083,
-3.92916666666667));
#363582=CARTESIAN_POINT('Ctrl Pts',(0.,1.17524047358083,-3.8875));
#363583=CARTESIAN_POINT('Ctrl Pts',(-0.678525403784434,1.17524047358083,
-3.84583333333333));
#363584=CARTESIAN_POINT('Ctrl Pts',(-1.01778810567665,0.587620236790414,
-3.80416666666667));
#363585=CARTESIAN_POINT('Ctrl Pts',(-1.35705080756887,6.77890228204754E-17,
-3.7625));
#363586=CARTESIAN_POINT('Ctrl Pts',(-1.01778810567665,-0.587620236790414,
-3.72083333333333));
#363587=CARTESIAN_POINT('Ctrl Pts',(-0.678525403784435,-1.17524047358083,
-3.67916666666667));
#363588=CARTESIAN_POINT('Ctrl Pts',(-1.43925448419918E-16,-1.17524047358083,
-3.6375));
#363589=CARTESIAN_POINT('Ctrl Pts',(0.678525403784434,-1.17524047358083,
-3.59583333333333));
#363590=CARTESIAN_POINT('Ctrl Pts',(1.01778810567665,-0.587620236790415,
-3.55416666666667));
#363591=CARTESIAN_POINT('Ctrl Pts',(1.35705080756887,-3.73866482480005E-16,
-3.5125));
#363592=CARTESIAN_POINT('Ctrl Pts',(1.01778810567665,0.587620236790413,
-3.47083333333333));
#363593=CARTESIAN_POINT('Ctrl Pts',(0.678525403784435,1.17524047358083,
-3.42916666666667));
#363594=CARTESIAN_POINT('Ctrl Pts',(0.,1.17524047358083,-3.3875));
#363595=CARTESIAN_POINT('Ctrl Pts',(-0.678525403784434,1.17524047358083,
-3.34583333333333));
#363596=CARTESIAN_POINT('Ctrl Pts',(-1.01778810567665,0.587620236790414,
-3.30416666666667));
#363597=CARTESIAN_POINT('Ctrl Pts',(-1.35705080756887,-1.50758816672666E-16,
-3.2625));
#363598=CARTESIAN_POINT('Ctrl Pts',(-1.01778810567665,-0.587620236790414,
-3.22083333333333));
#363599=CARTESIAN_POINT('Ctrl Pts',(-0.678525403784435,-1.17524047358083,
-3.17916666666667));
#363600=CARTESIAN_POINT('Ctrl Pts',(-1.43925448419918E-16,-1.17524047358083,
-3.1375));
#363601=CARTESIAN_POINT('Ctrl Pts',(0.678525403784434,-1.17524047358083,
-3.09583333333333));
#363602=CARTESIAN_POINT('Ctrl Pts',(1.01778810567665,-0.587620236790415,
-3.05416666666667));
#363603=CARTESIAN_POINT('Ctrl Pts',(1.35705080756887,-5.92414321973146E-16,
-3.0125));
#363604=CARTESIAN_POINT('Ctrl Pts',(1.01778810567665,0.587620236790413,
-2.97083333333333));
#363605=CARTESIAN_POINT('Ctrl Pts',(0.678525403784435,1.17524047358083,
-2.92916666666667));
#363606=CARTESIAN_POINT('Ctrl Pts',(0.,1.17524047358083,-2.8875));
#363607=CARTESIAN_POINT('Ctrl Pts',(-0.678525403784434,1.17524047358083,
-2.84583333333333));
#363608=CARTESIAN_POINT('Ctrl Pts',(-1.01778810567665,0.587620236790414,
-2.80416666666667));
#363609=CARTESIAN_POINT('Ctrl Pts',(-1.35705080756887,-3.69306656165808E-16,
-2.7625));
#363610=CARTESIAN_POINT('Ctrl Pts',(-1.01778810567665,-0.587620236790414,
-2.72083333333333));
#363611=CARTESIAN_POINT('Ctrl Pts',(-0.678525403784435,-1.17524047358083,
-2.67916666666667));
#363612=CARTESIAN_POINT('Ctrl Pts',(-1.43925448419918E-16,-1.17524047358083,
-2.6375));
#363613=CARTESIAN_POINT('Ctrl Pts',(0.678525403784434,-1.17524047358083,
-2.59583333333333));
#363614=CARTESIAN_POINT('Ctrl Pts',(1.01778810567665,-0.587620236790415,
-2.55416666666667));
#363615=CARTESIAN_POINT('Ctrl Pts',(1.35705080756887,-8.10962161466288E-16,
-2.5125));
#363616=CARTESIAN_POINT('Ctrl Pts',(1.01778810567665,0.587620236790413,
-2.47083333333334));
#363617=CARTESIAN_POINT('Ctrl Pts',(0.678525403784435,1.17524047358083,
-2.42916666666667));
#363618=CARTESIAN_POINT('Ctrl Pts',(0.,1.17524047358083,-2.3875));
#363619=CARTESIAN_POINT('Ctrl Pts',(-0.678525403784434,1.17524047358083,
-2.34583333333334));
#363620=CARTESIAN_POINT('Ctrl Pts',(-1.01778810567665,0.587620236790414,
-2.30416666666667));
#363621=CARTESIAN_POINT('Ctrl Pts',(-1.35705080756887,-5.87854495658949E-16,
-2.2625));
#363622=CARTESIAN_POINT('Ctrl Pts',(-1.01778810567665,-0.587620236790415,
-2.22083333333333));
#363623=CARTESIAN_POINT('Ctrl Pts',(-0.678525403784435,-1.17524047358083,
-2.17916666666667));
#363624=CARTESIAN_POINT('Ctrl Pts',(-1.43925448419918E-16,-1.17524047358083,
-2.1375));
#363625=CARTESIAN_POINT('Ctrl Pts',(0.678525403784434,-1.17524047358083,
-2.09583333333333));
#363626=CARTESIAN_POINT('Ctrl Pts',(1.01778810567665,-0.587620236790415,
-2.05416666666667));
#363627=CARTESIAN_POINT('Ctrl Pts',(1.35705080756887,-1.02951000095943E-15,
-2.0125));
#363628=CARTESIAN_POINT('Ctrl Pts',(1.01778810567665,0.587620236790413,
-1.97083333333333));
#363629=CARTESIAN_POINT('Ctrl Pts',(0.678525403784435,1.17524047358083,
-1.92916666666667));
#363630=CARTESIAN_POINT('Ctrl Pts',(0.,1.17524047358083,-1.8875));
#363631=CARTESIAN_POINT('Ctrl Pts',(-0.678525403784434,1.17524047358083,
-1.84583333333334));
#363632=CARTESIAN_POINT('Ctrl Pts',(-1.01778810567665,0.587620236790414,
-1.80416666666667));
#363633=CARTESIAN_POINT('Ctrl Pts',(-1.35705080756887,-8.0640233515209E-16,
-1.7625));
#363634=CARTESIAN_POINT('Ctrl Pts',(-1.01778810567665,-0.587620236790415,
-1.72083333333333));
#363635=CARTESIAN_POINT('Ctrl Pts',(-0.678525403784435,-1.17524047358083,
-1.67916666666667));
#363636=CARTESIAN_POINT('Ctrl Pts',(-1.43925448419918E-16,-1.17524047358083,
-1.6375));
#363637=CARTESIAN_POINT('Ctrl Pts',(0.678525403784434,-1.17524047358083,
-1.59583333333333));
#363638=CARTESIAN_POINT('Ctrl Pts',(1.01778810567665,-0.587620236790416,
-1.55416666666667));
#363639=CARTESIAN_POINT('Ctrl Pts',(1.35705080756887,-1.24805784045257E-15,
-1.5125));
#363640=CARTESIAN_POINT('Ctrl Pts',(1.01778810567665,0.587620236790412,
-1.47083333333333));
#363641=CARTESIAN_POINT('Ctrl Pts',(0.678525403784435,1.17524047358083,
-1.42916666666667));
#363642=CARTESIAN_POINT('Ctrl Pts',(0.,1.17524047358083,-1.3875));
#459203=UNCERTAINTY_MEASURE_WITH_UNIT(LENGTH_MEASURE(0.01),#459243,
'DISTANCE_ACCURACY_VALUE',
'Maximum model space distance between geometric entities at asserted c
onnectivities');
#459216=UNCERTAINTY_MEASURE_WITH_UNIT(LENGTH_MEASURE(0.01),#459243,
'DISTANCE_ACCURACY_VALUE',
'Maximum model space distance between geometric entities at asserted c
onnectivities');
#459229=(
GEOMETRIC_REPRESENTATION_CONTEXT(3)
GLOBAL_UNCERTAINTY_ASSIGNED_CONTEXT((#459203))
GLOBAL_UNIT_ASSIGNED_CONTEXT((#459243,#459245,#459246))
REPRESENTATION_CONTEXT('','3D')
);
#459242=(
GEOMETRIC_REPRESENTATION_CONTEXT(3)
GLOBAL_UNCERTAINTY_ASSIGNED_CONTEXT((#459216))
GLOBAL_UNIT_ASSIGNED_CONTEXT((#459243,#459245,#459246))
REPRESENTATION_CONTEXT('','3D')
);
#459243=(
LENGTH_UNIT()
NAMED_UNIT(*)
SI_UNIT(.MILLI.,.METRE.)
);
#459245=(
NAMED_UNIT(*)
PLANE_ANGLE_UNIT()
SI_UNIT($,.RADIAN.)
);
#459246=(
NAMED_UNIT(*)
SI_UNIT($,.STERADIAN.)
SOLID_ANGLE_UNIT()
);
#459259=SHAPE_DEFINITION_REPRESENTATION(#459284,#459340);
#459284=PRODUCT_DEFINITION_SHAPE('',$,#459366);
#459340=SHAPE_REPRESENTATION('',(#99052),#459229);
#459353=PRODUCT_DEFINITION_CONTEXT('part definition',#459430,'design');
#459366=PRODUCT_DEFINITION('Flanged Screw M3x16','Flanged Screw M3x16',
#459391,#459353);
#459391=PRODUCT_DEFINITION_FORMATION('',$,#459444);
#459430=APPLICATION_CONTEXT(
'Core Data for Automotive Mechanical Design Process');
#459431=PRODUCT_CONTEXT('part definition',#459430,'mechanical');
#459444=PRODUCT('Flanged Screw M3x16','Flanged Screw M3x16',$,(#459431));
#459527=COLOUR_RGB('Black',0.12,0.14,0.17);
#459528=FILL_AREA_STYLE_COLOUR('',#459527);
#459529=FILL_AREA_STYLE('',(#459528));
#459530=SURFACE_STYLE_FILL_AREA(#459529);
#459531=SURFACE_SIDE_STYLE('',(#459530));
#459532=SURFACE_STYLE_USAGE(.BOTH.,#459531);
#459533=PRESENTATION_STYLE_ASSIGNMENT((#459532));
ENDSEC;
END-ISO-10303-21;
